ISO-10303-21;
HEADER;
FILE_DESCRIPTION (('STEP AP214'),
    '1' );
FILE_NAME ('1. Base.step',
    '2026-10-09T08:13:37',
    ( '' ),
    ( '' ),
    'SwSTEP 2.0',
    'SolidWorks 2021',
    '' );
FILE_SCHEMA (( 'AUTOMOTIVE_DESIGN' ));
ENDSEC;

DATA;
#3=CIRCLE ( 'NONE', #24760, 5.000000000000004441 ) ;
#10=DIRECTION ( 'NONE',  ( 1.298988366203102052E-16, 0.05527174654752588928, 0.9984713486292864371 ) ) ;
#14=ORIENTED_EDGE ( 'NONE', *, *, #46779, .F. ) ;
#30=COLOUR_RGB ( '', 0.09019608, 0.27058824, 0.51372549) ;
#32=MECHANICAL_DESIGN_GEOMETRIC_PRESENTATION_REPRESENTATION('',(#66376),#38375);
#49=COLOUR_RGB ( '', 0.72549020, 0.75294118, 0.79215686) ;
#55=DIRECTION ( 'NONE',  ( 1.000000000000000000, -0.000000000000000000, -1.300977106640434891E-16 ) ) ;
#70=DIRECTION ( 'NONE',  ( -1.000000000000000000, 0.000000000000000000, 0.000000000000000000 ) ) ;
#71=( NAMED_UNIT ( * ) SI_UNIT ( $, .STERADIAN. ) SOLID_ANGLE_UNIT ( ) );
#75=SURFACE_SIDE_STYLE ('',( #32169 ) ) ;
#81=CARTESIAN_POINT ( 'NONE',  ( 2.999999999999990230, 5.000000000000000000, 37.00402776293829277 ) ) ;
#83=SURFACE_STYLE_FILL_AREA ( #58559 ) ;
#84=EDGE_LOOP ( 'NONE', ( #18925, #54897, #57059, #45162 ) ) ;
#87=ADVANCED_FACE ( 'NONE', ( #15409 ), #58281, .T. ) ;
#90=CARTESIAN_POINT ( 'NONE',  ( 31.64575850060272089, 42.77450856510287025, -45.47201648568074006 ) ) ;
#96=EDGE_CURVE ( 'NONE', #24376, #48365, #62535, .T. ) ;
#100=AXIS2_PLACEMENT_3D ( 'NONE', #41019, #61382, #57148 ) ;
#102=VECTOR ( 'NONE', #57920, 1000.000000000000000 ) ;
#114=MECHANICAL_DESIGN_GEOMETRIC_PRESENTATION_REPRESENTATION('',(#15946),#36167);
#119=SURFACE_STYLE_USAGE ( .BOTH. , #59618 ) ;
#120=UNCERTAINTY_MEASURE_WITH_UNIT (LENGTH_MEASURE( 1.000000000000000082E-05 ), #23829, 'distance_accuracy_value', 'NONE');
#133=FILL_AREA_STYLE_COLOUR ( '', #46192 ) ;
#136=DIRECTION ( 'NONE',  ( -1.000000000000000000, 0.000000000000000000, 0.000000000000000000 ) ) ;
#137=AXIS2_PLACEMENT_3D ( 'NONE', #11267, #39426, #17620 ) ;
#152=( NAMED_UNIT ( * ) SI_UNIT ( $, .STERADIAN. ) SOLID_ANGLE_UNIT ( ) );
#153=PLANE ( 'NONE',  #33814 ) ;
#154=ORIENTED_EDGE ( 'NONE', *, *, #42387, .F. ) ;
#156=( LENGTH_UNIT ( ) NAMED_UNIT ( * ) SI_UNIT ( .MILLI., .METRE. ) );
#167=CARTESIAN_POINT ( 'NONE',  ( 98.00000000000000000, 5.000000000000000000, 0.000000000000000000 ) ) ;
#171=( GEOMETRIC_REPRESENTATION_CONTEXT ( 3 ) GLOBAL_UNCERTAINTY_ASSIGNED_CONTEXT ( ( #48298 ) ) GLOBAL_UNIT_ASSIGNED_CONTEXT ( ( #9974, #68031, #14535 ) ) REPRESENTATION_CONTEXT ( 'NONE', 'WORKASPACE' ) );
#182=CARTESIAN_POINT ( 'NONE',  ( 57.00000000000000000, 16.00000000000000000, 47.50402776293824303 ) ) ;
#196=SURFACE_STYLE_USAGE ( .BOTH. , #38639 ) ;
#207=CARTESIAN_POINT ( 'NONE',  ( 98.00000000000000000, 16.00000000000000000, 0.000000000000000000 ) ) ;
#234=CARTESIAN_POINT ( 'NONE',  ( 0.000000000000000000, 0.9999999999999991118, 79.00402776293826435 ) ) ;
#241=CARTESIAN_POINT ( 'NONE',  ( 32.00000000000001421, 42.00000000000000000, 45.61250543006183022 ) ) ;
#243=EDGE_CURVE ( 'NONE', #42679, #46237, #35432, .T. ) ;
#247=VECTOR ( 'NONE', #43567, 1000.000000000000000 ) ;
#261=STYLED_ITEM ( 'NONE', ( #11744 ), #23739 ) ;
#262=SURFACE_STYLE_FILL_AREA ( #59071 ) ;
#264=ORIENTED_EDGE ( 'NONE', *, *, #62719, .T. ) ;
#270=SURFACE_SIDE_STYLE ('',( #10898 ) ) ;
#275=UNCERTAINTY_MEASURE_WITH_UNIT (LENGTH_MEASURE( 1.000000000000000082E-05 ), #13075, 'distance_accuracy_value', 'NONE');
#276=MECHANICAL_DESIGN_GEOMETRIC_PRESENTATION_REPRESENTATION('',(#28426),#30651);
#284=MECHANICAL_DESIGN_GEOMETRIC_PRESENTATION_REPRESENTATION('',(#21680),#66580);
#286=MECHANICAL_DESIGN_GEOMETRIC_PRESENTATION_REPRESENTATION('',(#23945),#46493);
#290=CARTESIAN_POINT ( 'NONE',  ( 57.00000000000000000, 5.000000000000000000, -60.00402776293827145 ) ) ;
#309=UNCERTAINTY_MEASURE_WITH_UNIT (LENGTH_MEASURE( 1.000000000000000082E-05 ), #35446, 'distance_accuracy_value', 'NONE');
#312=ORIENTED_EDGE ( 'NONE', *, *, #24526, .F. ) ;
#316=CIRCLE ( 'NONE', #9392, 2.000000000000001776 ) ;
#325=DIRECTION ( 'NONE',  ( 0.000000000000000000, 0.000000000000000000, -1.000000000000000000 ) ) ;
#330=VERTEX_POINT ( 'NONE', #26529 ) ;
#343=SURFACE_STYLE_FILL_AREA ( #48645 ) ;
#356=SURFACE_SIDE_STYLE ('',( #48656 ) ) ;
#360=VERTEX_POINT ( 'NONE', #25837 ) ;
#362=AXIS2_PLACEMENT_3D ( 'NONE', #9506, #4167, #25641 ) ;
#381=EDGE_CURVE ( 'NONE', #57733, #8059, #64170, .T. ) ;
#387=FILL_AREA_STYLE_COLOUR ( '', #30374 ) ;
#388=SURFACE_SIDE_STYLE ('',( #27504 ) ) ;
#389=DIRECTION ( 'NONE',  ( -0.000000000000000000, 1.000000000000000000, -0.000000000000000000 ) ) ;
#391=CIRCLE ( 'NONE', #1543, 2.499999999999998668 ) ;
#402=VECTOR ( 'NONE', #43226, 1000.000000000000000 ) ;
#404=COLOUR_RGB ( '', 0.72549020, 0.75294118, 0.79215686) ;
#405=DIRECTION ( 'NONE',  ( -0.000000000000000000, 1.000000000000000000, -0.000000000000000000 ) ) ;
#408=VERTEX_POINT ( 'NONE', #20929 ) ;
#413=ADVANCED_FACE ( 'NONE', ( #42770 ), #52941, .F. ) ;
#417=VERTEX_POINT ( 'NONE', #64528 ) ;
#425=DIRECTION ( 'NONE',  ( -1.000000000000000000, 0.000000000000000000, 0.000000000000000000 ) ) ;
#431=AXIS2_PLACEMENT_3D ( 'NONE', #40119, #61508, #29524 ) ;
#432=UNCERTAINTY_MEASURE_WITH_UNIT (LENGTH_MEASURE( 1.000000000000000082E-05 ), #8140, 'distance_accuracy_value', 'NONE');
#433=DIRECTION ( 'NONE',  ( 0.000000000000000000, 0.000000000000000000, 1.000000000000000000 ) ) ;
#437=AXIS2_PLACEMENT_3D ( 'NONE', #17639, #69690, #49288 ) ;
#441=CARTESIAN_POINT ( 'NONE',  ( 1.000000000000000000, 14.00000000000000000, -79.00402776293826435 ) ) ;
#448=ORIENTED_EDGE ( 'NONE', *, *, #48910, .F. ) ;
#484=CARTESIAN_POINT ( 'NONE',  ( 4.000000000000002665, 38.70020753820971748, -89.00000000000000000 ) ) ;
#485=EDGE_CURVE ( 'NONE', #67224, #42847, #8634, .T. ) ;
#488=CIRCLE ( 'NONE', #21959, 112.9999999999981526 ) ;
#490=AXIS2_PLACEMENT_3D ( 'NONE', #45726, #67139, #13310 ) ;
#492=SURFACE_SIDE_STYLE ('',( #43527 ) ) ;
#500=MECHANICAL_DESIGN_GEOMETRIC_PRESENTATION_REPRESENTATION('',(#7305),#9589);
#514=CARTESIAN_POINT ( 'NONE',  ( 10.00000000000000178, 43.00000000000000000, -90.00000000000000000 ) ) ;
#518=ORIENTED_EDGE ( 'NONE', *, *, #44832, .T. ) ;
#519=( BOUNDED_CURVE ( )  B_SPLINE_CURVE ( 3, ( #46857, #68263, #20043, #8814 ),
 .UNSPECIFIED., .F., .F. ) 
 B_SPLINE_CURVE_WITH_KNOTS ( ( 4, 4 ),
 ( 4.712388980384689674, 6.283185307179586232 ),
 .UNSPECIFIED. ) 
 CURVE ( )  GEOMETRIC_REPRESENTATION_ITEM ( )  RATIONAL_B_SPLINE_CURVE ( ( 1.000000000000000000, 0.8047378541243649375, 0.8047378541243649375, 1.000000000000000000 ) ) 
 REPRESENTATION_ITEM ( '' )  );
#522=ORIENTED_EDGE ( 'NONE', *, *, #64472, .T. ) ;
#524=SURFACE_STYLE_FILL_AREA ( #22748 ) ;
#533=SURFACE_STYLE_USAGE ( .BOTH. , #23107 ) ;
#534=DIRECTION ( 'NONE',  ( 0.000000000000000000, 0.000000000000000000, -1.000000000000000000 ) ) ;
#540=ORIENTED_EDGE ( 'NONE', *, *, #37095, .F. ) ;
#551=STYLED_ITEM ( 'NONE', ( #61712 ), #49528 ) ;
#561=CARTESIAN_POINT ( 'NONE',  ( 24.58105220659400203, 26.69229804232007197, 27.43511223479084293 ) ) ;
#562=CARTESIAN_POINT ( 'NONE',  ( 57.00000000000000000, 16.00000000000000000, -60.00402776293825724 ) ) ;
#569=FILL_AREA_STYLE ('',( #28734 ) ) ;
#570=EDGE_CURVE ( 'NONE', #54537, #8864, #15015, .T. ) ;
#571=PRESENTATION_STYLE_ASSIGNMENT (( #38313 ) ) ;
#574=STYLED_ITEM ( 'NONE', ( #44469 ), #32799 ) ;
#575=CARTESIAN_POINT ( 'NONE',  ( 31.00000000000001421, 15.00000000000000000, 35.50000000000000000 ) ) ;
#576=DIRECTION ( 'NONE',  ( 1.000000000000000000, 0.000000000000000000, 0.000000000000000000 ) ) ;
#582=VERTEX_POINT ( 'NONE', #12774 ) ;
#592=EDGE_LOOP ( 'NONE', ( #33276, #36266, #62240, #1238 ) ) ;
#609=EDGE_LOOP ( 'NONE', ( #63299, #42577, #64965, #23489 ) ) ;
#616=ORIENTED_EDGE ( 'NONE', *, *, #63159, .F. ) ;
#637=( NAMED_UNIT ( * ) SI_UNIT ( $, .STERADIAN. ) SOLID_ANGLE_UNIT ( ) );
#638=DIRECTION ( 'NONE',  ( -1.000000000000000000, 0.000000000000000000, 0.000000000000000000 ) ) ;
#639=CARTESIAN_POINT ( 'NONE',  ( 73.01088739851485343, 5.000000000000000000, 65.71817553072288831 ) ) ;
#664=ORIENTED_EDGE ( 'NONE', *, *, #56214, .F. ) ;
#667=EDGE_CURVE ( 'NONE', #26396, #31733, #51240, .T. ) ;
#671=SURFACE_SIDE_STYLE ('',( #26751 ) ) ;
#689=CARTESIAN_POINT ( 'NONE',  ( 20.00000000000001776, 15.00000000000000000, 29.68999999999999417 ) ) ;
#700=ORIENTED_EDGE ( 'NONE', *, *, #2572, .T. ) ;
#705=ORIENTED_EDGE ( 'NONE', *, *, #22573, .F. ) ;
#712=( NAMED_UNIT ( * ) PLANE_ANGLE_UNIT ( ) SI_UNIT ( $, .RADIAN. ) );
#718=SURFACE_STYLE_USAGE ( .BOTH. , #388 ) ;
#732=ADVANCED_FACE ( 'NONE', ( #34413 ), #28058, .F. ) ;
#740=SURFACE_SIDE_STYLE ('',( #49709 ) ) ;
#746=ORIENTED_EDGE ( 'NONE', *, *, #25332, .F. ) ;
#748=ORIENTED_EDGE ( 'NONE', *, *, #23356, .F. ) ;
#751=( NAMED_UNIT ( * ) PLANE_ANGLE_UNIT ( ) SI_UNIT ( $, .RADIAN. ) );
#756=CARTESIAN_POINT ( 'NONE',  ( 10.00000000000001776, 17.04554193418302788, 0.6691306063588585706 ) ) ;
#766=EDGE_CURVE ( 'NONE', #54457, #36334, #60105, .T. ) ;
#771=( NAMED_UNIT ( * ) SI_UNIT ( $, .STERADIAN. ) SOLID_ANGLE_UNIT ( ) );
#773=COLOUR_RGB ( '', 0.31764706, 0.68627451, 0.89019608) ;
#777=ORIENTED_EDGE ( 'NONE', *, *, #69425, .F. ) ;
#784=CARTESIAN_POINT ( 'NONE',  ( 22.00000000000002132, 42.00000000000000000, -29.68999999999999417 ) ) ;
#786=( LENGTH_UNIT ( ) NAMED_UNIT ( * ) SI_UNIT ( .MILLI., .METRE. ) );
#787=( GEOMETRIC_REPRESENTATION_CONTEXT ( 3 ) GLOBAL_UNCERTAINTY_ASSIGNED_CONTEXT ( ( #12911 ) ) GLOBAL_UNIT_ASSIGNED_CONTEXT ( ( #5440, #36832, #37544 ) ) REPRESENTATION_CONTEXT ( 'NONE', 'WORKASPACE' ) );
#802=( LENGTH_UNIT ( ) NAMED_UNIT ( * ) SI_UNIT ( .MILLI., .METRE. ) );
#803=UNCERTAINTY_MEASURE_WITH_UNIT (LENGTH_MEASURE( 1.000000000000000082E-05 ), #47965, 'distance_accuracy_value', 'NONE');
#805=SHAPE_REPRESENTATION_RELATIONSHIP ( 'NONE' , 'NONE' ,  #40670, #34624 ) ;
#822=EDGE_CURVE ( 'NONE', #3091, #51817, #9685, .T. ) ;
#824=SURFACE_STYLE_FILL_AREA ( #32223 ) ;
#826=ORIENTED_EDGE ( 'NONE', *, *, #29866, .F. ) ;
#827=CARTESIAN_POINT ( 'NONE',  ( 57.00000000000000000, 16.00000000000000000, -65.00402776293825013 ) ) ;
#833=AXIS2_PLACEMENT_3D ( 'NONE', #13505, #64129, #9660 ) ;
#834=EDGE_LOOP ( 'NONE', ( #4085, #26069, #55060, #50281 ) ) ;
#837=EDGE_LOOP ( 'NONE', ( #3899, #15136, #7179, #58174 ) ) ;
#842=ORIENTED_EDGE ( 'NONE', *, *, #45785, .F. ) ;
#854=CARTESIAN_POINT ( 'NONE',  ( 0.000000000000000000, 0.000000000000000000, 79.00402776293826435 ) ) ;
#864=MECHANICAL_DESIGN_GEOMETRIC_PRESENTATION_REPRESENTATION('',(#31253),#48145);
#866=STYLED_ITEM ( 'NONE', ( #49101 ), #66381 ) ;
#867=CARTESIAN_POINT ( 'NONE',  ( 36.00000000000002842, 5.000000000000000000, -32.00402776293825724 ) ) ;
#868=CARTESIAN_POINT ( 'NONE',  ( 16.00000000000001776, 42.00000000000000000, 29.68999999999999417 ) ) ;
#871=EDGE_CURVE ( 'NONE', #17912, #22405, #53502, .T. ) ;
#883=CARTESIAN_POINT ( 'NONE',  ( 24.29181562774721215, 24.88364009055414883, 27.31771990072506640 ) ) ;
#885=LINE ( 'NONE', #28364, #23641 ) ;
#891=UNCERTAINTY_MEASURE_WITH_UNIT (LENGTH_MEASURE( 1.000000000000000082E-05 ), #17075, 'distance_accuracy_value', 'NONE');
#892=DIRECTION ( 'NONE',  ( 1.000000000000000000, -0.000000000000000000, 0.000000000000000000 ) ) ;
#902=CYLINDRICAL_SURFACE ( 'NONE', #35389, 1.000000000000000888 ) ;
#904=( BOUNDED_CURVE ( )  B_SPLINE_CURVE ( 3, ( #64172, #16030, #47011, #64538 ),
 .UNSPECIFIED., .F., .F. ) 
 B_SPLINE_CURVE_WITH_KNOTS ( ( 4, 4 ),
 ( 0.000000000000000000, 1.570796326794899223 ),
 .UNSPECIFIED. ) 
 CURVE ( )  GEOMETRIC_REPRESENTATION_ITEM ( )  RATIONAL_B_SPLINE_CURVE ( ( 1.000000000000000000, 0.8047378541243643824, 0.8047378541243643824, 1.000000000000000000 ) ) 
 REPRESENTATION_ITEM ( '' )  );
#910=EDGE_LOOP ( 'NONE', ( #58286, #13364, #33728, #51994 ) ) ;
#917=AXIS2_PLACEMENT_3D ( 'NONE', #37172, #21275, #37530 ) ;
#923=CARTESIAN_POINT ( 'NONE',  ( 32.00000000000002132, 15.00000000000000000, 79.00402776293823592 ) ) ;
#929=CARTESIAN_POINT ( 'NONE',  ( 12.00000000000001776, 14.00000000000000000, 29.68999999999999417 ) ) ;
#941=UNCERTAINTY_MEASURE_WITH_UNIT (LENGTH_MEASURE( 1.000000000000000082E-05 ), #61585, 'distance_accuracy_value', 'NONE');
#946=EDGE_LOOP ( 'NONE', ( #19427, #8776, #15362 ) ) ;
#954=FILL_AREA_STYLE ('',( #63683 ) ) ;
#959=ADVANCED_FACE ( 'NONE', ( #41450 ), #57247, .F. ) ;
#967=CARTESIAN_POINT ( 'NONE',  ( 31.00000000000000355, 50.00000000000000000, -60.00000000000000711 ) ) ;
#969=( GEOMETRIC_REPRESENTATION_CONTEXT ( 3 ) GLOBAL_UNCERTAINTY_ASSIGNED_CONTEXT ( ( #46175 ) ) GLOBAL_UNIT_ASSIGNED_CONTEXT ( ( #23556, #2764, #12655 ) ) REPRESENTATION_CONTEXT ( 'NONE', 'WORKASPACE' ) );
#977=UNCERTAINTY_MEASURE_WITH_UNIT (LENGTH_MEASURE( 1.000000000000000082E-05 ), #63393, 'distance_accuracy_value', 'NONE');
#980=SURFACE_STYLE_FILL_AREA ( #27768 ) ;
#993=CARTESIAN_POINT ( 'NONE',  ( 74.89452121010485541, 0.000000000000000000, -66.39042820928574429 ) ) ;
#996=CARTESIAN_POINT ( 'NONE',  ( 31.00000000000000000, 42.00000000000000000, -79.00402776293826435 ) ) ;
#998=COLOUR_RGB ( '', 0.40784314, 0.44705882, 0.49803922) ;
#1004=CARTESIAN_POINT ( 'NONE',  ( 22.00000000000000711, 50.00000000000000000, -46.00000000000000000 ) ) ;
#1006=ORIENTED_EDGE ( 'NONE', *, *, #6104, .T. ) ;
#1019=ORIENTED_EDGE ( 'NONE', *, *, #17957, .F. ) ;
#1023=AXIS2_PLACEMENT_3D ( 'NONE', #41776, #45999, #51959 ) ;
#1025=CARTESIAN_POINT ( 'NONE',  ( 6.330869393641158638, 43.00000000000000000, 28.38386403503541899 ) ) ;
#1027=ADVANCED_FACE ( 'NONE', ( #10803 ), #9781, .T. ) ;
#1030=AXIS2_PLACEMENT_3D ( 'NONE', #28182, #1061, #1427 ) ;
#1043=CARTESIAN_POINT ( 'NONE',  ( 179.4361977533490347, 0.9999999999999991118, -103.7004518695263044 ) ) ;
#1044=VERTEX_POINT ( 'NONE', #36876 ) ;
#1052=AXIS2_PLACEMENT_3D ( 'NONE', #6461, #27897, #49403 ) ;
#1058=( NAMED_UNIT ( * ) PLANE_ANGLE_UNIT ( ) SI_UNIT ( $, .RADIAN. ) );
#1061=DIRECTION ( 'NONE',  ( -0.000000000000000000, -1.000000000000000000, -0.000000000000000000 ) ) ;
#1080=ORIENTED_EDGE ( 'NONE', *, *, #9314, .F. ) ;
#1082=AXIS2_PLACEMENT_3D ( 'NONE', #60399, #892, #22438 ) ;
#1087=CARTESIAN_POINT ( 'NONE',  ( 27.00000000000001776, 42.00000000000000000, 34.49999999999999289 ) ) ;
#1088=CARTESIAN_POINT ( 'NONE',  ( 16.00000000000001776, 42.00000000000000000, 29.68999999999999417 ) ) ;
#1091=FILL_AREA_STYLE ('',( #65180 ) ) ;
#1096=DIRECTION ( 'NONE',  ( 1.000000000000000000, 0.000000000000000000, 0.000000000000000000 ) ) ;
#1101=ORIENTED_EDGE ( 'NONE', *, *, #12298, .T. ) ;
#1107=FILL_AREA_STYLE ('',( #61306 ) ) ;
#1111=ADVANCED_FACE ( 'NONE', ( #48830 ), #43796, .F. ) ;
#1112=FACE_OUTER_BOUND ( 'NONE', #40591, .T. ) ;
#1117=CARTESIAN_POINT ( 'NONE',  ( 82.09357085539578236, 5.000000000000000000, 37.00402776293825724 ) ) ;
#1126=CIRCLE ( 'NONE', #57335, 12.50000000000001066 ) ;
#1129=ORIENTED_EDGE ( 'NONE', *, *, #69485, .F. ) ;
#1153=SURFACE_STYLE_FILL_AREA ( #7207 ) ;
#1156=VECTOR ( 'NONE', #44633, 1000.000000000000000 ) ;
#1157=EDGE_LOOP ( 'NONE', ( #14111, #36056 ) ) ;
#1158=CARTESIAN_POINT ( 'NONE',  ( 8.000000000000035527, 5.000000000000000000, -77.00402776293825013 ) ) ;
#1161=COLOUR_RGB ( '', 0.66274510, 0.83137255, 0.94901961) ;
#1162=CARTESIAN_POINT ( 'NONE',  ( -1.387778780781445676E-14, 17.78868675966041835, 1.540743955509788682E-30 ) ) ;
#1166=( GEOMETRIC_REPRESENTATION_CONTEXT ( 3 ) GLOBAL_UNCERTAINTY_ASSIGNED_CONTEXT ( ( #48224 ) ) GLOBAL_UNIT_ASSIGNED_CONTEXT ( ( #19992, #41496, #14751 ) ) REPRESENTATION_CONTEXT ( 'NONE', 'WORKASPACE' ) );
#1175=DIRECTION ( 'NONE',  ( 1.300977106640434891E-16, -0.000000000000000000, 1.000000000000000000 ) ) ;
#1184=DIRECTION ( 'NONE',  ( -0.000000000000000000, 0.000000000000000000, 1.000000000000000000 ) ) ;
#1187=DIRECTION ( 'NONE',  ( -1.000000000000000000, 0.000000000000000000, 0.000000000000000000 ) ) ;
#1191=ADVANCED_FACE ( 'NONE', ( #19171 ), #67357, .T. ) ;
#1197=FILL_AREA_STYLE ('',( #27959 ) ) ;
#1198=VERTEX_POINT ( 'NONE', #42101 ) ;
#1200=SURFACE_STYLE_USAGE ( .BOTH. , #54373 ) ;
#1201=EDGE_CURVE ( 'NONE', #34141, #63720, #44903, .T. ) ;
#1203=EDGE_CURVE ( 'NONE', #56838, #56593, #54978, .T. ) ;
#1209=ORIENTED_EDGE ( 'NONE', *, *, #62339, .F. ) ;
#1214=ORIENTED_EDGE ( 'NONE', *, *, #14225, .F. ) ;
#1216=( NAMED_UNIT ( * ) PLANE_ANGLE_UNIT ( ) SI_UNIT ( $, .RADIAN. ) );
#1219=DIRECTION ( 'NONE',  ( -0.000000000000000000, -1.000000000000000000, -0.000000000000000000 ) ) ;
#1221=COLOUR_RGB ( '', 0.72549020, 0.75294118, 0.79215686) ;
#1229=COLOUR_RGB ( '', 0.66274510, 0.83137255, 0.94901961) ;
#1238=ORIENTED_EDGE ( 'NONE', *, *, #36509, .F. ) ;
#1245=EDGE_CURVE ( 'NONE', #9552, #29900, #12302, .T. ) ;
#1248=AXIS2_PLACEMENT_3D ( 'NONE', #67127, #50957, #2716 ) ;
#1259=CARTESIAN_POINT ( 'NONE',  ( 57.00000000000000000, 14.00000000000000000, 79.00402776293826435 ) ) ;
#1261=CIRCLE ( 'NONE', #100, 4.999999999999997335 ) ;
#1265=MECHANICAL_DESIGN_GEOMETRIC_PRESENTATION_REPRESENTATION('',(#37346),#6794);
#1266=( NAMED_UNIT ( * ) SI_UNIT ( $, .STERADIAN. ) SOLID_ANGLE_UNIT ( ) );
#1268=CARTESIAN_POINT ( 'NONE',  ( 57.00000000000000000, 14.00000000000000000, -79.00402776293826435 ) ) ;
#1278=VERTEX_POINT ( 'NONE', #20585 ) ;
#1286=VERTEX_POINT ( 'NONE', #41726 ) ;
#1293=AXIS2_PLACEMENT_3D ( 'NONE', #38188, #59591, #65571 ) ;
#1306=VERTEX_POINT ( 'NONE', #14990 ) ;
#1307=DIRECTION ( 'NONE',  ( 0.000000000000000000, 0.6691306063588592368, 0.7431448254773934670 ) ) ;
#1309=( LENGTH_UNIT ( ) NAMED_UNIT ( * ) SI_UNIT ( .MILLI., .METRE. ) );
#1311=CARTESIAN_POINT ( 'NONE',  ( 33.00000000000000000, 13.00000000000000178, -80.00402776293826435 ) ) ;
#1325=DIRECTION ( 'NONE',  ( -1.300977106640434891E-16, 0.000000000000000000, -1.000000000000000000 ) ) ;
#1333=DIRECTION ( 'NONE',  ( -1.000000000000000000, 0.000000000000000000, -0.000000000000000000 ) ) ;
#1336=ORIENTED_EDGE ( 'NONE', *, *, #9744, .F. ) ;
#1339=SURFACE_SIDE_STYLE ('',( #32034 ) ) ;
#1359=SURFACE_SIDE_STYLE ('',( #45067 ) ) ;
#1363=SURFACE_SIDE_STYLE ('',( #6684 ) ) ;
#1367=CARTESIAN_POINT ( 'NONE',  ( 22.99999999999995026, 5.000000000000000000, 77.00402776293825013 ) ) ;
#1373=CYLINDRICAL_SURFACE ( 'NONE', #20731, 4.999999999999997335 ) ;
#1374=VERTEX_POINT ( 'NONE', #64865 ) ;
#1378=EDGE_LOOP ( 'NONE', ( #57692, #3735, #67885, #29980 ) ) ;
#1381=ORIENTED_EDGE ( 'NONE', *, *, #57111, .F. ) ;
#1385=ADVANCED_FACE ( 'NONE', ( #43805 ), #11752, .T. ) ;
#1386=SURFACE_STYLE_USAGE ( .BOTH. , #39807 ) ;
#1391=CARTESIAN_POINT ( 'NONE',  ( 179.4361977533490347, 5.000000000000000000, -103.7004518695263044 ) ) ;
#1412=ORIENTED_EDGE ( 'NONE', *, *, #31186, .T. ) ;
#1416=VERTEX_POINT ( 'NONE', #11404 ) ;
#1420=EDGE_LOOP ( 'NONE', ( #65933, #39551, #7020, #26468 ) ) ;
#1421=AXIS2_PLACEMENT_3D ( 'NONE', #7959, #45967, #55799 ) ;
#1427=DIRECTION ( 'NONE',  ( 0.000000000000000000, 0.000000000000000000, -1.000000000000000000 ) ) ;
#1431=( NAMED_UNIT ( * ) SI_UNIT ( $, .STERADIAN. ) SOLID_ANGLE_UNIT ( ) );
#1432=DIRECTION ( 'NONE',  ( -1.000000000000000000, 0.000000000000000000, 0.000000000000000000 ) ) ;
#1442=VERTEX_POINT ( 'NONE', #1488 ) ;
#1444=ORIENTED_EDGE ( 'NONE', *, *, #61752, .T. ) ;
#1446=SURFACE_STYLE_USAGE ( .BOTH. , #740 ) ;
#1447=EDGE_CURVE ( 'NONE', #42847, #7443, #5760, .T. ) ;
#1460=DIRECTION ( 'NONE',  ( 0.000000000000000000, 0.000000000000000000, -1.000000000000000000 ) ) ;
#1461=ADVANCED_FACE ( 'NONE', ( #29307 ), #50107, .T. ) ;
#1468=EDGE_LOOP ( 'NONE', ( #7591, #12251 ) ) ;
#1473=( LENGTH_UNIT ( ) NAMED_UNIT ( * ) SI_UNIT ( .MILLI., .METRE. ) );
#1485=COLOUR_RGB ( '', 0.40784314, 0.44705882, 0.49803922) ;
#1486=ORIENTED_EDGE ( 'NONE', *, *, #61250, .F. ) ;
#1488=CARTESIAN_POINT ( 'NONE',  ( 36.00000000000002842, 0.000000000000000000, -32.00402776293825724 ) ) ;
#1496=CARTESIAN_POINT ( 'NONE',  ( 35.99999999999999289, 5.000000000000000000, 32.00402776293825724 ) ) ;
#1505=MECHANICAL_DESIGN_GEOMETRIC_PRESENTATION_REPRESENTATION('',(#55485),#10565);
#1509=PLANE ( 'NONE',  #68354 ) ;
#1510=SURFACE_STYLE_FILL_AREA ( #66989 ) ;
#1515=( LENGTH_UNIT ( ) NAMED_UNIT ( * ) SI_UNIT ( .MILLI., .METRE. ) );
#1517=AXIS2_PLACEMENT_3D ( 'NONE', #21312, #42154, #46736 ) ;
#1521=LINE ( 'NONE', #7548, #63948 ) ;
#1523=UNCERTAINTY_MEASURE_WITH_UNIT (LENGTH_MEASURE( 1.000000000000000082E-05 ), #37418, 'distance_accuracy_value', 'NONE');
#1529=CARTESIAN_POINT ( 'NONE',  ( 35.99999999999999289, 0.000000000000000000, -29.00402776293825724 ) ) ;
#1537=FILL_AREA_STYLE ('',( #50151 ) ) ;
#1543=AXIS2_PLACEMENT_3D ( 'NONE', #26249, #49714, #27534 ) ;
#1546=FILL_AREA_STYLE_COLOUR ( '', #12747 ) ;
#1550=( NAMED_UNIT ( * ) SI_UNIT ( $, .STERADIAN. ) SOLID_ANGLE_UNIT ( ) );
#1551=CIRCLE ( 'NONE', #19577, 111.0000000000000142 ) ;
#1564=CIRCLE ( 'NONE', #40982, 5.000000000000004441 ) ;
#1567=VERTEX_POINT ( 'NONE', #30335 ) ;
#1570=( LENGTH_UNIT ( ) NAMED_UNIT ( * ) SI_UNIT ( .MILLI., .METRE. ) );
#1574=VECTOR ( 'NONE', #46104, 1000.000000000000000 ) ;
#1583=DIRECTION ( 'NONE',  ( 0.000000000000000000, -1.000000000000000000, 0.000000000000000000 ) ) ;
#1587=EDGE_CURVE ( 'NONE', #66764, #12604, #46944, .T. ) ;
#1616=( GEOMETRIC_REPRESENTATION_CONTEXT ( 3 ) GLOBAL_UNCERTAINTY_ASSIGNED_CONTEXT ( ( #47498 ) ) GLOBAL_UNIT_ASSIGNED_CONTEXT ( ( #59921, #33874, #38861 ) ) REPRESENTATION_CONTEXT ( 'NONE', 'WORKASPACE' ) );
#1617=VECTOR ( 'NONE', #37214, 1000.000000000000000 ) ;
#1620=SURFACE_STYLE_FILL_AREA ( #39684 ) ;
#1622=EDGE_CURVE ( 'NONE', #27240, #5819, #10310, .T. ) ;
#1625=AXIS2_PLACEMENT_3D ( 'NONE', #5260, #1583, #17827 ) ;
#1626=EDGE_CURVE ( 'NONE', #10996, #37203, #42701, .T. ) ;
#1629=( GEOMETRIC_REPRESENTATION_CONTEXT ( 3 ) GLOBAL_UNCERTAINTY_ASSIGNED_CONTEXT ( ( #55915 ) ) GLOBAL_UNIT_ASSIGNED_CONTEXT ( ( #24364, #66237, #23005 ) ) REPRESENTATION_CONTEXT ( 'NONE', 'WORKASPACE' ) );
#1644=ORIENTED_EDGE ( 'NONE', *, *, #8589, .T. ) ;
#1649=ORIENTED_EDGE ( 'NONE', *, *, #32637, .T. ) ;
#1653=DIRECTION ( 'NONE',  ( -1.000000000000000000, 0.000000000000000000, 0.000000000000000000 ) ) ;
#1656=AXIS2_PLACEMENT_3D ( 'NONE', #868, #6233, #22410 ) ;
#1664=EDGE_LOOP ( 'NONE', ( #14425, #17146, #44162, #32760 ) ) ;
#1667=CYLINDRICAL_SURFACE ( 'NONE', #31576, 1.000000000000000888 ) ;
#1684=AXIS2_PLACEMENT_3D ( 'NONE', #54632, #6442, #1096 ) ;
#1693=EDGE_CURVE ( 'NONE', #63720, #28531, #45617, .T. ) ;
#1694=SURFACE_SIDE_STYLE ('',( #54512 ) ) ;
#1698=EDGE_CURVE ( 'NONE', #34648, #11331, #27618, .T. ) ;
#1704=SURFACE_SIDE_STYLE ('',( #19304 ) ) ;
#1710=ORIENTED_EDGE ( 'NONE', *, *, #3780, .F. ) ;
#1731=VERTEX_POINT ( 'NONE', #33480 ) ;
#1757=DIRECTION ( 'NONE',  ( -0.000000000000000000, -1.000000000000000000, 0.000000000000000000 ) ) ;
#1761=ORIENTED_EDGE ( 'NONE', *, *, #46779, .T. ) ;
#1762=UNCERTAINTY_MEASURE_WITH_UNIT (LENGTH_MEASURE( 1.000000000000000082E-05 ), #2360, 'distance_accuracy_value', 'NONE');
#1763=AXIS2_PLACEMENT_3D ( 'NONE', #60378, #40701, #63172 ) ;
#1771=ORIENTED_EDGE ( 'NONE', *, *, #28441, .T. ) ;
#1772=PRESENTATION_STYLE_ASSIGNMENT (( #8156 ) ) ;
#1786=CARTESIAN_POINT ( 'NONE',  ( 26.00000000000001776, -3.148064030671221758, -29.68999999999999417 ) ) ;
#1792=CYLINDRICAL_SURFACE ( 'NONE', #51211, 5.000000000000011546 ) ;
#1793=CARTESIAN_POINT ( 'NONE',  ( 57.00000000000000000, 14.00000000000000000, 60.00402776293827145 ) ) ;
#1794=ORIENTED_EDGE ( 'NONE', *, *, #4602, .F. ) ;
#1795=DIRECTION ( 'NONE',  ( -2.478176394252586564E-16, 0.000000000000000000, -1.000000000000000000 ) ) ;
#1798=DIRECTION ( 'NONE',  ( 0.000000000000000000, 0.000000000000000000, 1.000000000000000000 ) ) ;
#1802=AXIS2_PLACEMENT_3D ( 'NONE', #26945, #38281, #12170 ) ;
#1812=( NAMED_UNIT ( * ) PLANE_ANGLE_UNIT ( ) SI_UNIT ( $, .RADIAN. ) );
#1816=UNCERTAINTY_MEASURE_WITH_UNIT (LENGTH_MEASURE( 1.000000000000000082E-05 ), #38811, 'distance_accuracy_value', 'NONE');
#1824=ORIENTED_EDGE ( 'NONE', *, *, #60940, .F. ) ;
#1830=LINE ( 'NONE', #54984, #13241 ) ;
#1836=CARTESIAN_POINT ( 'NONE',  ( 10.00000000000001954, 42.00000000000000000, 28.38386403503541899 ) ) ;
#1846=CARTESIAN_POINT ( 'NONE',  ( 57.00000000000000000, 5.000000000000000000, 77.00402776293825013 ) ) ;
#1850=ORIENTED_EDGE ( 'NONE', *, *, #31656, .T. ) ;
#1853=MECHANICAL_DESIGN_GEOMETRIC_PRESENTATION_REPRESENTATION('',(#45784),#19877);
#1865=ORIENTED_EDGE ( 'NONE', *, *, #14226, .T. ) ;
#1890=ORIENTED_EDGE ( 'NONE', *, *, #42040, .T. ) ;
#1892=DIRECTION ( 'NONE',  ( 0.000000000000000000, 0.000000000000000000, -1.000000000000000000 ) ) ;
#1893=PRESENTATION_STYLE_ASSIGNMENT (( #50170 ) ) ;
#1901=CARTESIAN_POINT ( 'NONE',  ( 1.000000000000000000, 43.00000000000000000, -74.38749456993816978 ) ) ;
#1906=FACE_OUTER_BOUND ( 'NONE', #44768, .T. ) ;
#1920=ORIENTED_EDGE ( 'NONE', *, *, #55164, .T. ) ;
#1942=SURFACE_STYLE_USAGE ( .BOTH. , #50220 ) ;
#1950=ORIENTED_EDGE ( 'NONE', *, *, #18817, .T. ) ;
#1953=DIRECTION ( 'NONE',  ( -1.000000000000000000, 0.000000000000000000, -0.000000000000000000 ) ) ;
#1957=SURFACE_STYLE_FILL_AREA ( #50236 ) ;
#1958=FILL_AREA_STYLE_COLOUR ( '', #16169 ) ;
#1967=COLOUR_RGB ( '', 0.72549020, 0.75294118, 0.79215686) ;
#1969=ORIENTED_EDGE ( 'NONE', *, *, #13332, .T. ) ;
#1974=ORIENTED_EDGE ( 'NONE', *, *, #20335, .T. ) ;
#1977=SURFACE_STYLE_USAGE ( .BOTH. , #11922 ) ;
#1984=ORIENTED_EDGE ( 'NONE', *, *, #37757, .F. ) ;
#1987=CYLINDRICAL_SURFACE ( 'NONE', #47041, 1.000000000000000888 ) ;
#1992=ORIENTED_EDGE ( 'NONE', *, *, #46091, .T. ) ;
#1996=DIRECTION ( 'NONE',  ( 1.000000000000000000, -0.000000000000000000, -1.300977106640434891E-16 ) ) ;
#1997=ORIENTED_EDGE ( 'NONE', *, *, #11606, .T. ) ;
#1999=ORIENTED_EDGE ( 'NONE', *, *, #67741, .T. ) ;
#2011=CARTESIAN_POINT ( 'NONE',  ( 33.00000000000000000, 15.00000000000000000, -79.00402776293826435 ) ) ;
#2014=DIRECTION ( 'NONE',  ( -0.000000000000000000, -1.000000000000000000, 0.000000000000000000 ) ) ;
#2025=LINE ( 'NONE', #39780, #3909 ) ;
#2030=CARTESIAN_POINT ( 'NONE',  ( 22.99999999999998224, 5.000000000000000000, 72.00402776293825013 ) ) ;
#2033=SURFACE_SIDE_STYLE ('',( #51696 ) ) ;
#2050=( NAMED_UNIT ( * ) PLANE_ANGLE_UNIT ( ) SI_UNIT ( $, .RADIAN. ) );
#2059=EDGE_CURVE ( 'NONE', #65559, #65056, #25221, .T. ) ;
#2060=SURFACE_SIDE_STYLE ('',( #3114 ) ) ;
#2073=VECTOR ( 'NONE', #55391, 1000.000000000000000 ) ;
#2076=FILL_AREA_STYLE_COLOUR ( '', #30282 ) ;
#2092=DIRECTION ( 'NONE',  ( -0.000000000000000000, -0.000000000000000000, -1.000000000000000000 ) ) ;
#2095=FILL_AREA_STYLE_COLOUR ( '', #56441 ) ;
#2096=STYLED_ITEM ( 'NONE', ( #50046 ), #15066 ) ;
#2099=MECHANICAL_DESIGN_GEOMETRIC_PRESENTATION_REPRESENTATION('',(#61642),#29054);
#2102=VECTOR ( 'NONE', #54339, 1000.000000000000000 ) ;
#2104=( NAMED_UNIT ( * ) PLANE_ANGLE_UNIT ( ) SI_UNIT ( $, .RADIAN. ) );
#2113=VECTOR ( 'NONE', #3338, 1000.000000000000000 ) ;
#2114=AXIS2_PLACEMENT_3D ( 'NONE', #67440, #45345, #41100 ) ;
#2119=( GEOMETRIC_REPRESENTATION_CONTEXT ( 3 ) GLOBAL_UNCERTAINTY_ASSIGNED_CONTEXT ( ( #18680 ) ) GLOBAL_UNIT_ASSIGNED_CONTEXT ( ( #52584, #42061, #3275 ) ) REPRESENTATION_CONTEXT ( 'NONE', 'WORKASPACE' ) );
#2131=( GEOMETRIC_REPRESENTATION_CONTEXT ( 3 ) GLOBAL_UNCERTAINTY_ASSIGNED_CONTEXT ( ( #275 ) ) GLOBAL_UNIT_ASSIGNED_CONTEXT ( ( #13075, #2104, #12726 ) ) REPRESENTATION_CONTEXT ( 'NONE', 'WORKASPACE' ) );
#2132=DIRECTION ( 'NONE',  ( 0.000000000000000000, 1.000000000000000000, -0.000000000000000000 ) ) ;
#2143=FILL_AREA_STYLE_COLOUR ( '', #18399 ) ;
#2144=EDGE_CURVE ( 'NONE', #3091, #11136, #51224, .T. ) ;
#2154=( NAMED_UNIT ( * ) SI_UNIT ( $, .STERADIAN. ) SOLID_ANGLE_UNIT ( ) );
#2156=DIRECTION ( 'NONE',  ( 0.000000000000000000, 1.000000000000000000, 0.000000000000000000 ) ) ;
#2157=CARTESIAN_POINT ( 'NONE',  ( 22.99999999999996447, 5.000000000000000000, -29.00402776293825369 ) ) ;
#2167=EDGE_LOOP ( 'NONE', ( #50739, #59302, #68092, #56929, #49728 ) ) ;
#2181=CIRCLE ( 'NONE', #42785, 1.000000000000000888 ) ;
#2193=EDGE_CURVE ( 'NONE', #11604, #10038, #2970, .T. ) ;
#2202=DIRECTION ( 'NONE',  ( 0.000000000000000000, 0.000000000000000000, -1.000000000000000000 ) ) ;
#2225=( GEOMETRIC_REPRESENTATION_CONTEXT ( 3 ) GLOBAL_UNCERTAINTY_ASSIGNED_CONTEXT ( ( #32772 ) ) GLOBAL_UNIT_ASSIGNED_CONTEXT ( ( #62827, #14308, #46728 ) ) REPRESENTATION_CONTEXT ( 'NONE', 'WORKASPACE' ) );
#2243=( NAMED_UNIT ( * ) SI_UNIT ( $, .STERADIAN. ) SOLID_ANGLE_UNIT ( ) );
#2245=ADVANCED_FACE ( 'NONE', ( #19182 ), #21886, .T. ) ;
#2249=ORIENTED_EDGE ( 'NONE', *, *, #12851, .T. ) ;
#2250=SURFACE_STYLE_FILL_AREA ( #39300 ) ;
#2261=AXIS2_PLACEMENT_3D ( 'NONE', #967, #65774, #49258 ) ;
#2262=CARTESIAN_POINT ( 'NONE',  ( 4.000000000000030198, 43.00000000000000000, 79.00402776293826435 ) ) ;
#2270=( GEOMETRIC_REPRESENTATION_CONTEXT ( 3 ) GLOBAL_UNCERTAINTY_ASSIGNED_CONTEXT ( ( #49071 ) ) GLOBAL_UNIT_ASSIGNED_CONTEXT ( ( #27531, #28567, #28206 ) ) REPRESENTATION_CONTEXT ( 'NONE', 'WORKASPACE' ) );
#2273=AXIS2_PLACEMENT_3D ( 'NONE', #57866, #19511, #68076 ) ;
#2286=UNCERTAINTY_MEASURE_WITH_UNIT (LENGTH_MEASURE( 1.000000000000000082E-05 ), #47305, 'distance_accuracy_value', 'NONE');
#2299=EDGE_CURVE ( 'NONE', #59244, #60780, #66826, .T. ) ;
#2313=VERTEX_POINT ( 'NONE', #44818 ) ;
#2328=EDGE_CURVE ( 'NONE', #65761, #408, #2513, .T. ) ;
#2333=( NAMED_UNIT ( * ) PLANE_ANGLE_UNIT ( ) SI_UNIT ( $, .RADIAN. ) );
#2335=( LENGTH_UNIT ( ) NAMED_UNIT ( * ) SI_UNIT ( .MILLI., .METRE. ) );
#2341=DIRECTION ( 'NONE',  ( 0.000000000000000000, -1.000000000000000000, 0.000000000000000000 ) ) ;
#2350=CARTESIAN_POINT ( 'NONE',  ( 1.000000000000000000, 14.00000000000000533, 35.50000000000000000 ) ) ;
#2360=( LENGTH_UNIT ( ) NAMED_UNIT ( * ) SI_UNIT ( .MILLI., .METRE. ) );
#2364=FACE_OUTER_BOUND ( 'NONE', #32171, .T. ) ;
#2368=EDGE_CURVE ( 'NONE', #31733, #14584, #43166, .T. ) ;
#2379=( GEOMETRIC_REPRESENTATION_CONTEXT ( 3 ) GLOBAL_UNCERTAINTY_ASSIGNED_CONTEXT ( ( #31444 ) ) GLOBAL_UNIT_ASSIGNED_CONTEXT ( ( #21067, #31965, #46829 ) ) REPRESENTATION_CONTEXT ( 'NONE', 'WORKASPACE' ) );
#2382=SURFACE_SIDE_STYLE ('',( #68217 ) ) ;
#2385=DIRECTION ( 'NONE',  ( -1.000000000000000000, 0.000000000000000000, 1.300977106640434644E-16 ) ) ;
#2393=VECTOR ( 'NONE', #37943, 1000.000000000000000 ) ;
#2395=DIRECTION ( 'NONE',  ( 0.000000000000000000, 0.000000000000000000, -1.000000000000000000 ) ) ;
#2396=AXIS2_PLACEMENT_3D ( 'NONE', #42704, #10, #26469 ) ;
#2402=EDGE_CURVE ( 'NONE', #40347, #32368, #52129, .T. ) ;
#2410=VERTEX_POINT ( 'NONE', #61301 ) ;
#2420=DIRECTION ( 'NONE',  ( -0.000000000000000000, -1.000000000000000000, -0.000000000000000000 ) ) ;
#2422=VECTOR ( 'NONE', #46931, 1000.000000000000114 ) ;
#2423=DIRECTION ( 'NONE',  ( 0.000000000000000000, 0.7431448254773944662, 0.6691306063588580155 ) ) ;
#2432=UNCERTAINTY_MEASURE_WITH_UNIT (LENGTH_MEASURE( 1.000000000000000082E-05 ), #24097, 'distance_accuracy_value', 'NONE');
#2435=DIRECTION ( 'NONE',  ( -0.000000000000000000, 1.000000000000000000, -0.000000000000000000 ) ) ;
#2440=ORIENTED_EDGE ( 'NONE', *, *, #68940, .T. ) ;
#2447=SURFACE_STYLE_FILL_AREA ( #55267 ) ;
#2448=UNCERTAINTY_MEASURE_WITH_UNIT (LENGTH_MEASURE( 1.000000000000000082E-05 ), #57735, 'distance_accuracy_value', 'NONE');
#2456=LINE ( 'NONE', #41830, #62734 ) ;
#2466=ORIENTED_EDGE ( 'NONE', *, *, #766, .T. ) ;
#2467=VECTOR ( 'NONE', #35994, 1000.000000000000000 ) ;
#2483=COLOUR_RGB ( '', 0.31764706, 0.68627451, 0.89019608) ;
#2492=UNCERTAINTY_MEASURE_WITH_UNIT (LENGTH_MEASURE( 1.000000000000000082E-05 ), #53386, 'distance_accuracy_value', 'NONE');
#2497=EDGE_CURVE ( 'NONE', #11976, #1198, #57068, .T. ) ;
#2498=DIRECTION ( 'NONE',  ( 0.000000000000000000, 0.000000000000000000, 1.000000000000000000 ) ) ;
#2513=LINE ( 'NONE', #39894, #49849 ) ;
#2542=LINE ( 'NONE', #60978, #42670 ) ;
#2552=CARTESIAN_POINT ( 'NONE',  ( 31.00000000000000711, 50.00000000000000000, -60.00000000000000711 ) ) ;
#2565=DIRECTION ( 'NONE',  ( 0.000000000000000000, -1.000000000000000000, 0.000000000000000000 ) ) ;
#2567=( NAMED_UNIT ( * ) PLANE_ANGLE_UNIT ( ) SI_UNIT ( $, .RADIAN. ) );
#2571=EDGE_CURVE ( 'NONE', #9516, #33963, #1551, .T. ) ;
#2572=EDGE_CURVE ( 'NONE', #7443, #68025, #40966, .T. ) ;
#2573=SURFACE_SIDE_STYLE ('',( #15220 ) ) ;
#2577=AXIS2_PLACEMENT_3D ( 'NONE', #17403, #28228, #56996 ) ;
#2578=DIRECTION ( 'NONE',  ( 1.000000000000000000, 0.000000000000000000, -1.300977106640434891E-16 ) ) ;
#2589=EDGE_CURVE ( 'NONE', #61460, #12604, #29681, .T. ) ;
#2600=AXIS2_PLACEMENT_3D ( 'NONE', #47237, #8863, #62651 ) ;
#2611=AXIS2_PLACEMENT_3D ( 'NONE', #1391, #49302, #32762 ) ;
#2613=ADVANCED_FACE ( 'NONE', ( #6368, #59845 ), #64075, .T. ) ;
#2616=AXIS2_PLACEMENT_3D ( 'NONE', #51317, #31219, #67850 ) ;
#2618=SURFACE_STYLE_FILL_AREA ( #19527 ) ;
#2626=ORIENTED_EDGE ( 'NONE', *, *, #3354, .T. ) ;
#2631=( GEOMETRIC_REPRESENTATION_CONTEXT ( 3 ) GLOBAL_UNCERTAINTY_ASSIGNED_CONTEXT ( ( #31951 ) ) GLOBAL_UNIT_ASSIGNED_CONTEXT ( ( #5223, #43608, #49546 ) ) REPRESENTATION_CONTEXT ( 'NONE', 'WORKASPACE' ) );
#2637=DIRECTION ( 'NONE',  ( -0.000000000000000000, -1.000000000000000000, -0.000000000000000000 ) ) ;
#2642=PRESENTATION_STYLE_ASSIGNMENT (( #40020 ) ) ;
#2657=LINE ( 'NONE', #45310, #16914 ) ;
#2658=( LENGTH_UNIT ( ) NAMED_UNIT ( * ) SI_UNIT ( .MILLI., .METRE. ) );
#2665=( GEOMETRIC_REPRESENTATION_CONTEXT ( 3 ) GLOBAL_UNCERTAINTY_ASSIGNED_CONTEXT ( ( #20848 ) ) GLOBAL_UNIT_ASSIGNED_CONTEXT ( ( #64198, #49430, #55014 ) ) REPRESENTATION_CONTEXT ( 'NONE', 'WORKASPACE' ) );
#2667=DIRECTION ( 'NONE',  ( 0.000000000000000000, 0.000000000000000000, 1.000000000000000000 ) ) ;
#2675=FILL_AREA_STYLE ('',( #55489 ) ) ;
#2685=SURFACE_STYLE_USAGE ( .BOTH. , #24508 ) ;
#2688=CARTESIAN_POINT ( 'NONE',  ( 2.999999999999997335, 0.000000000000000000, 72.00402776293822171 ) ) ;
#2695=ORIENTED_EDGE ( 'NONE', *, *, #39851, .T. ) ;
#2707=SURFACE_STYLE_USAGE ( .BOTH. , #45362 ) ;
#2711=( NAMED_UNIT ( * ) PLANE_ANGLE_UNIT ( ) SI_UNIT ( $, .RADIAN. ) );
#2712=( LENGTH_UNIT ( ) NAMED_UNIT ( * ) SI_UNIT ( .MILLI., .METRE. ) );
#2714=DIRECTION ( 'NONE',  ( -0.000000000000000000, 1.000000000000000000, -0.000000000000000000 ) ) ;
#2716=DIRECTION ( 'NONE',  ( -1.000000000000000000, 0.000000000000000000, 0.000000000000000000 ) ) ;
#2740=FILL_AREA_STYLE ('',( #19654 ) ) ;
#2744=FILL_AREA_STYLE ('',( #55199 ) ) ;
#2760=EDGE_CURVE ( 'NONE', #4579, #2313, #53252, .T. ) ;
#2764=( NAMED_UNIT ( * ) PLANE_ANGLE_UNIT ( ) SI_UNIT ( $, .RADIAN. ) );
#2767=CARTESIAN_POINT ( 'NONE',  ( 57.00000000000000000, 5.000000000000000000, -60.00402776293827145 ) ) ;
#2769=ORIENTED_EDGE ( 'NONE', *, *, #5693, .F. ) ;
#2772=MECHANICAL_DESIGN_GEOMETRIC_PRESENTATION_REPRESENTATION('',(#5066),#19632);
#2785=CIRCLE ( 'NONE', #14085, 1.000000000000000888 ) ;
#2789=FACE_OUTER_BOUND ( 'NONE', #52188, .T. ) ;
#2791=FACE_OUTER_BOUND ( 'NONE', #4912, .T. ) ;
#2801=ORIENTED_EDGE ( 'NONE', *, *, #54854, .T. ) ;
#2805=CARTESIAN_POINT ( 'NONE',  ( 57.00000000000000000, 14.00000000000000000, 79.00402776293826435 ) ) ;
#2814=ORIENTED_EDGE ( 'NONE', *, *, #32988, .T. ) ;
#2819=ORIENTED_EDGE ( 'NONE', *, *, #2572, .F. ) ;
#2820=ADVANCED_FACE ( 'NONE', ( #18674 ), #17653, .T. ) ;
#2821=CARTESIAN_POINT ( 'NONE',  ( 32.00000000000000000, 15.00000000000000000, -79.00402776293826435 ) ) ;
#2825=STYLED_ITEM ( 'NONE', ( #2642 ), #8523 ) ;
#2838=CARTESIAN_POINT ( 'NONE',  ( 36.00000000000002842, 0.000000000000000000, 32.00402776293825724 ) ) ;
#2839=ADVANCED_FACE ( 'NONE', ( #2791 ), #24281, .T. ) ;
#2872=SURFACE_SIDE_STYLE ('',( #38864 ) ) ;
#2875=AXIS2_PLACEMENT_3D ( 'NONE', #27722, #39041, #38705 ) ;
#2881=( NAMED_UNIT ( * ) SI_UNIT ( $, .STERADIAN. ) SOLID_ANGLE_UNIT ( ) );
#2883=FACE_OUTER_BOUND ( 'NONE', #45645, .T. ) ;
#2884=ORIENTED_EDGE ( 'NONE', *, *, #9795, .T. ) ;
#2890=( NAMED_UNIT ( * ) PLANE_ANGLE_UNIT ( ) SI_UNIT ( $, .RADIAN. ) );
#2902=EDGE_CURVE ( 'NONE', #51817, #35442, #52771, .T. ) ;
#2906=LINE ( 'NONE', #68038, #65066 ) ;
#2915=PRESENTATION_STYLE_ASSIGNMENT (( #12821 ) ) ;
#2921=( NAMED_UNIT ( * ) SI_UNIT ( $, .STERADIAN. ) SOLID_ANGLE_UNIT ( ) );
#2929=CARTESIAN_POINT ( 'NONE',  ( 57.00000000000000000, 16.00000000000000000, 47.50402776293824303 ) ) ;
#2932=( GEOMETRIC_REPRESENTATION_CONTEXT ( 3 ) GLOBAL_UNCERTAINTY_ASSIGNED_CONTEXT ( ( #67918 ) ) GLOBAL_UNIT_ASSIGNED_CONTEXT ( ( #11817, #56828, #56108 ) ) REPRESENTATION_CONTEXT ( 'NONE', 'WORKASPACE' ) );
#2934=VERTEX_POINT ( 'NONE', #35552 ) ;
#2935=CARTESIAN_POINT ( 'NONE',  ( 82.09357085539578236, 0.000000000000000000, 37.00402776293825724 ) ) ;
#2941=VERTEX_POINT ( 'NONE', #43623 ) ;
#2942=( LENGTH_UNIT ( ) NAMED_UNIT ( * ) SI_UNIT ( .MILLI., .METRE. ) );
#2946=SURFACE_SIDE_STYLE ('',( #57147 ) ) ;
#2963=ORIENTED_EDGE ( 'NONE', *, *, #15183, .T. ) ;
#2970=LINE ( 'NONE', #13217, #67983 ) ;
#2974=EDGE_CURVE ( 'NONE', #9284, #61460, #32667, .T. ) ;
#2986=ORIENTED_EDGE ( 'NONE', *, *, #11354, .F. ) ;
#2988=CARTESIAN_POINT ( 'NONE',  ( 2.999999999999990230, 5.000000000000000000, 37.00402776293829277 ) ) ;
#2996=SURFACE_SIDE_STYLE ('',( #19915 ) ) ;
#3001=( NAMED_UNIT ( * ) SI_UNIT ( $, .STERADIAN. ) SOLID_ANGLE_UNIT ( ) );
#3003=STYLED_ITEM ( 'NONE', ( #56201 ), #58599 ) ;
#3011=FILL_AREA_STYLE ('',( #57222 ) ) ;
#3013=AXIS2_PLACEMENT_3D ( 'NONE', #53654, #48429, #21647 ) ;
#3014=( NAMED_UNIT ( * ) PLANE_ANGLE_UNIT ( ) SI_UNIT ( $, .RADIAN. ) );
#3035=FILL_AREA_STYLE_COLOUR ( '', #17701 ) ;
#3038=ORIENTED_EDGE ( 'NONE', *, *, #2760, .T. ) ;
#3044=DIRECTION ( 'NONE',  ( -1.000000000000000000, 0.000000000000000000, -3.469446951953611033E-15 ) ) ;
#3045=ORIENTED_EDGE ( 'NONE', *, *, #30476, .F. ) ;
#3047=STYLED_ITEM ( 'NONE', ( #13235 ), #67261 ) ;
#3051=ORIENTED_EDGE ( 'NONE', *, *, #49380, .T. ) ;
#3053=EDGE_LOOP ( 'NONE', ( #20213, #28789, #746 ) ) ;
#3063=SURFACE_STYLE_FILL_AREA ( #35831 ) ;
#3067=DIRECTION ( 'NONE',  ( 0.000000000000000000, 1.000000000000000000, 0.000000000000000000 ) ) ;
#3073=DIRECTION ( 'NONE',  ( -1.000000000000000000, 0.000000000000000000, 2.478176394252586564E-16 ) ) ;
#3075=FILL_AREA_STYLE ('',( #30539 ) ) ;
#3076=STYLED_ITEM ( 'NONE', ( #44559 ), #41344 ) ;
#3080=DIRECTION ( 'NONE',  ( 0.000000000000000000, 0.000000000000000000, 1.000000000000000000 ) ) ;
#3081=CARTESIAN_POINT ( 'NONE',  ( 3.000000000000000000, 5.000000000000000000, -72.00402776293822171 ) ) ;
#3082=UNCERTAINTY_MEASURE_WITH_UNIT (LENGTH_MEASURE( 1.000000000000000082E-05 ), #5851, 'distance_accuracy_value', 'NONE');
#3090=SURFACE_STYLE_FILL_AREA ( #28202 ) ;
#3091=VERTEX_POINT ( 'NONE', #6610 ) ;
#3092=ORIENTED_EDGE ( 'NONE', *, *, #23206, .T. ) ;
#3094=DIRECTION ( 'NONE',  ( 1.982541115402069054E-16, 0.000000000000000000, -1.000000000000000000 ) ) ;
#3099=AXIS2_PLACEMENT_3D ( 'NONE', #13577, #56856, #51933 ) ;
#3105=ORIENTED_EDGE ( 'NONE', *, *, #44467, .T. ) ;
#3106=DIRECTION ( 'NONE',  ( 0.000000000000000000, -1.000000000000000000, 0.000000000000000000 ) ) ;
#3109=ADVANCED_FACE ( 'NONE', ( #66057 ), #50590, .F. ) ;
#3114=SURFACE_STYLE_FILL_AREA ( #67196 ) ;
#3123=CARTESIAN_POINT ( 'NONE',  ( 4.000000000000030198, 43.00000000000000000, 90.00000000000000000 ) ) ;
#3127=EDGE_CURVE ( 'NONE', #66584, #54496, #46755, .T. ) ;
#3131=CARTESIAN_POINT ( 'NONE',  ( 57.00000000000000000, 16.00000000000000000, 65.00402776293825013 ) ) ;
#3143=VERTEX_POINT ( 'NONE', #25236 ) ;
#3145=DIRECTION ( 'NONE',  ( -1.000000000000000000, 0.000000000000000000, 0.000000000000000000 ) ) ;
#3146=MECHANICAL_DESIGN_GEOMETRIC_PRESENTATION_REPRESENTATION('',(#68382),#67263);
#3151=DIRECTION ( 'NONE',  ( 0.000000000000000000, 0.000000000000000000, -1.000000000000000000 ) ) ;
#3154=LINE ( 'NONE', #61260, #60005 ) ;
#3164=STYLED_ITEM ( 'NONE', ( #69479 ), #14808 ) ;
#3165=( NAMED_UNIT ( * ) SI_UNIT ( $, .STERADIAN. ) SOLID_ANGLE_UNIT ( ) );
#3175=ORIENTED_EDGE ( 'NONE', *, *, #15745, .F. ) ;
#3197=ADVANCED_FACE ( 'NONE', ( #24879 ), #47442, .T. ) ;
#3206=UNCERTAINTY_MEASURE_WITH_UNIT (LENGTH_MEASURE( 1.000000000000000082E-05 ), #54167, 'distance_accuracy_value', 'NONE');
#3211=CARTESIAN_POINT ( 'NONE',  ( 57.00000000000000000, 0.000000000000000000, -60.00402776293825724 ) ) ;
#3215=EDGE_LOOP ( 'NONE', ( #4979, #59371, #9381, #40862 ) ) ;
#3218=( NAMED_UNIT ( * ) PLANE_ANGLE_UNIT ( ) SI_UNIT ( $, .RADIAN. ) );
#3222=VECTOR ( 'NONE', #65771, 1000.000000000000227 ) ;
#3223=CYLINDRICAL_SURFACE ( 'NONE', #18903, 5.000000000000000888 ) ;
#3228=( NAMED_UNIT ( * ) SI_UNIT ( $, .STERADIAN. ) SOLID_ANGLE_UNIT ( ) );
#3242=CARTESIAN_POINT ( 'NONE',  ( 1.000000000000000000, 42.00000000000000000, -79.00402776293826435 ) ) ;
#3244=DIRECTION ( 'NONE',  ( -0.000000000000000000, -1.000000000000000000, -0.000000000000000000 ) ) ;
#3246=( NAMED_UNIT ( * ) SI_UNIT ( $, .STERADIAN. ) SOLID_ANGLE_UNIT ( ) );
#3258=AXIS2_PLACEMENT_3D ( 'NONE', #54631, #6441, #44485 ) ;
#3263=CIRCLE ( 'NONE', #38149, 2.500000000000002220 ) ;
#3270=CIRCLE ( 'NONE', #41569, 1.000000000000000000 ) ;
#3275=( NAMED_UNIT ( * ) SI_UNIT ( $, .STERADIAN. ) SOLID_ANGLE_UNIT ( ) );
#3283=DIRECTION ( 'NONE',  ( 0.000000000000000000, -0.000000000000000000, -1.000000000000000000 ) ) ;
#3289=ORIENTED_EDGE ( 'NONE', *, *, #10953, .F. ) ;
#3307=EDGE_CURVE ( 'NONE', #50928, #62177, #7939, .T. ) ;
#3315=ORIENTED_EDGE ( 'NONE', *, *, #18960, .F. ) ;
#3320=FILL_AREA_STYLE_COLOUR ( '', #14044 ) ;
#3336=ORIENTED_EDGE ( 'NONE', *, *, #56202, .T. ) ;
#3338=DIRECTION ( 'NONE',  ( -0.000000000000000000, -0.000000000000000000, 1.000000000000000000 ) ) ;
#3340=VECTOR ( 'NONE', #19065, 1000.000000000000000 ) ;
#3349=VECTOR ( 'NONE', #43656, 1000.000000000000000 ) ;
#3354=EDGE_CURVE ( 'NONE', #44052, #8864, #62559, .T. ) ;
#3355=CARTESIAN_POINT ( 'NONE',  ( 27.99999999999999645, 5.000000000000000000, 24.00402776293821816 ) ) ;
#3356=SURFACE_STYLE_USAGE ( .BOTH. , #63870 ) ;
#3368=EDGE_CURVE ( 'NONE', #5288, #29168, #37425, .T. ) ;
#3370=DIRECTION ( 'NONE',  ( 0.000000000000000000, -0.000000000000000000, -1.000000000000000000 ) ) ;
#3384=PRESENTATION_STYLE_ASSIGNMENT (( #51629 ) ) ;
#3392=LINE ( 'NONE', #56912, #19921 ) ;
#3395=DIRECTION ( 'NONE',  ( 0.000000000000000000, 1.000000000000000000, 0.000000000000000000 ) ) ;
#3399=LINE ( 'NONE', #41124, #38648 ) ;
#3405=CARTESIAN_POINT ( 'NONE',  ( 33.00000000000000000, 13.00000000000000178, -79.00402776293826435 ) ) ;
#3406=CARTESIAN_POINT ( 'NONE',  ( 1.000000000000000000, 14.00000000000000000, 80.00402776293826435 ) ) ;
#3412=( NAMED_UNIT ( * ) PLANE_ANGLE_UNIT ( ) SI_UNIT ( $, .RADIAN. ) );
#3431=( NAMED_UNIT ( * ) PLANE_ANGLE_UNIT ( ) SI_UNIT ( $, .RADIAN. ) );
#3433=SURFACE_STYLE_FILL_AREA ( #46448 ) ;
#3442=SURFACE_SIDE_STYLE ('',( #30202 ) ) ;
#3443=COLOUR_RGB ( '', 0.66274510, 0.83137255, 0.94901961) ;
#3445=PRESENTATION_STYLE_ASSIGNMENT (( #23558 ) ) ;
#3449=FILL_AREA_STYLE ('',( #51700 ) ) ;
#3454=TOROIDAL_SURFACE ( 'NONE', #40641, 2.000000000000000000, 1.000000000000000000 ) ;
#3456=DIRECTION ( 'NONE',  ( -2.578301549612644668E-15, -0.6691306063588581265, 0.7431448254773944662 ) ) ;
#3457=COLOUR_RGB ( '', 0.72549020, 0.75294118, 0.79215686) ;
#3468=ORIENTED_EDGE ( 'NONE', *, *, #24450, .F. ) ;
#3471=CYLINDRICAL_SURFACE ( 'NONE', #35134, 5.000000000000000888 ) ;
#3473=EDGE_LOOP ( 'NONE', ( #49929, #11652, #43315, #4349 ) ) ;
#3494=ADVANCED_FACE ( 'NONE', ( #24443 ), #36375, .F. ) ;
#3499=EDGE_LOOP ( 'NONE', ( #68926, #51810, #23620, #4841 ) ) ;
#3502=( NAMED_UNIT ( * ) PLANE_ANGLE_UNIT ( ) SI_UNIT ( $, .RADIAN. ) );
#3512=VECTOR ( 'NONE', #42944, 1000.000000000000000 ) ;
#3524=( BOUNDED_CURVE ( )  B_SPLINE_CURVE ( 3, ( #52022, #36575, #9455, #64282 ),
 .UNSPECIFIED., .F., .F. ) 
 B_SPLINE_CURVE_WITH_KNOTS ( ( 4, 4 ),
 ( 1.570796326794896558, 3.141592653589792228 ),
 .UNSPECIFIED. ) 
 CURVE ( )  GEOMETRIC_REPRESENTATION_ITEM ( )  RATIONAL_B_SPLINE_CURVE ( ( 1.000000000000000000, 0.8047378541243652705, 0.8047378541243652705, 1.000000000000000000 ) ) 
 REPRESENTATION_ITEM ( '' )  );
#3542=AXIS2_PLACEMENT_3D ( 'NONE', #43351, #59111, #25457 ) ;
#3546=AXIS2_PLACEMENT_3D ( 'NONE', #31891, #31541, #53022 ) ;
#3551=EDGE_LOOP ( 'NONE', ( #49293, #8502, #48210, #3336, #16414 ) ) ;
#3554=COLOUR_RGB ( '', 0.66274510, 0.83137255, 0.94901961) ;
#3555=ORIENTED_EDGE ( 'NONE', *, *, #62642, .F. ) ;
#3558=DIRECTION ( 'NONE',  ( -0.000000000000000000, 0.9984713486292863260, 0.05527174654752588928 ) ) ;
#3560=( GEOMETRIC_REPRESENTATION_CONTEXT ( 3 ) GLOBAL_UNCERTAINTY_ASSIGNED_CONTEXT ( ( #24246 ) ) GLOBAL_UNIT_ASSIGNED_CONTEXT ( ( #17404, #6451, #12418 ) ) REPRESENTATION_CONTEXT ( 'NONE', 'WORKASPACE' ) );
#3566=ORIENTED_EDGE ( 'NONE', *, *, #41616, .T. ) ;
#3574=CARTESIAN_POINT ( 'NONE',  ( 29.00000000000002842, 42.00000000000000000, 89.00000000000000000 ) ) ;
#3581=DIRECTION ( 'NONE',  ( 0.000000000000000000, 0.000000000000000000, 1.000000000000000000 ) ) ;
#3584=CARTESIAN_POINT ( 'NONE',  ( 8.000000000000035527, 5.000000000000000000, 77.00402776293825013 ) ) ;
#3589=( NAMED_UNIT ( * ) PLANE_ANGLE_UNIT ( ) SI_UNIT ( $, .RADIAN. ) );
#3596=AXIS2_PLACEMENT_3D ( 'NONE', #44335, #65733, #17577 ) ;
#3605=COLOUR_RGB ( '', 0.72549020, 0.75294118, 0.79215686) ;
#3619=EDGE_CURVE ( 'NONE', #8149, #11591, #43045, .T. ) ;
#3625=CARTESIAN_POINT ( 'NONE',  ( 107.0858988931383777, 5.000000000000000000, -16.89933289725613363 ) ) ;
#3632=COLOUR_RGB ( '', 0.66274510, 0.83137255, 0.94901961) ;
#3636=SURFACE_SIDE_STYLE ('',( #47696 ) ) ;
#3640=DIRECTION ( 'NONE',  ( -1.000000000000000000, -0.000000000000000000, -0.000000000000000000 ) ) ;
#3657=CARTESIAN_POINT ( 'NONE',  ( 29.00000000000000000, 35.42594141563417054, -80.00402776293826435 ) ) ;
#3659=AXIS2_PLACEMENT_3D ( 'NONE', #14109, #8136, #18350 ) ;
#3665=SURFACE_STYLE_USAGE ( .BOTH. , #24444 ) ;
#3667=UNCERTAINTY_MEASURE_WITH_UNIT (LENGTH_MEASURE( 1.000000000000000082E-05 ), #15354, 'distance_accuracy_value', 'NONE');
#3670=( NAMED_UNIT ( * ) PLANE_ANGLE_UNIT ( ) SI_UNIT ( $, .RADIAN. ) );
#3672=AXIS2_PLACEMENT_3D ( 'NONE', #56621, #65793, #13348 ) ;
#3674=VERTEX_POINT ( 'NONE', #3131 ) ;
#3677=CARTESIAN_POINT ( 'NONE',  ( 10.00000000000002309, 43.00000000000000000, 90.00000000000000000 ) ) ;
#3705=PRESENTATION_STYLE_ASSIGNMENT (( #62478 ) ) ;
#3706=DIRECTION ( 'NONE',  ( 0.000000000000000000, 1.000000000000000000, 0.000000000000000000 ) ) ;
#3713=CARTESIAN_POINT ( 'NONE',  ( 10.00000000000001954, 50.00000000000000000, 46.00000000000000000 ) ) ;
#3717=CARTESIAN_POINT ( 'NONE',  ( -4.156108327861140431E-16, 42.24279663153610187, -45.14569480374296973 ) ) ;
#3720=SURFACE_STYLE_FILL_AREA ( #4075 ) ;
#3726=FACE_OUTER_BOUND ( 'NONE', #44249, .T. ) ;
#3730=FILL_AREA_STYLE_COLOUR ( '', #404 ) ;
#3735=ORIENTED_EDGE ( 'NONE', *, *, #9108, .F. ) ;
#3738=SURFACE_SIDE_STYLE ('',( #32243 ) ) ;
#3756=EDGE_LOOP ( 'NONE', ( #64534, #50996, #14334, #58273 ) ) ;
#3757=LINE ( 'NONE', #49494, #4611 ) ;
#3773=DIRECTION ( 'NONE',  ( -1.000000000000000000, 0.000000000000000000, 0.000000000000000000 ) ) ;
#3780=EDGE_CURVE ( 'NONE', #34648, #65503, #31291, .T. ) ;
#3784=AXIS2_PLACEMENT_3D ( 'NONE', #17975, #50681, #61229 ) ;
#3790=FILL_AREA_STYLE_COLOUR ( '', #21470 ) ;
#3793=DIRECTION ( 'NONE',  ( -1.239088197126290817E-16, 0.000000000000000000, -1.000000000000000000 ) ) ;
#3803=STYLED_ITEM ( 'NONE', ( #63555 ), #61877 ) ;
#3807=ORIENTED_EDGE ( 'NONE', *, *, #15018, .T. ) ;
#3813=FILL_AREA_STYLE ('',( #42915 ) ) ;
#3821=( GEOMETRIC_REPRESENTATION_CONTEXT ( 3 ) GLOBAL_UNCERTAINTY_ASSIGNED_CONTEXT ( ( #30674 ) ) GLOBAL_UNIT_ASSIGNED_CONTEXT ( ( #49968, #24571, #7389 ) ) REPRESENTATION_CONTEXT ( 'NONE', 'WORKASPACE' ) );
#3829=SURFACE_SIDE_STYLE ('',( #62252 ) ) ;
#3834=ORIENTED_EDGE ( 'NONE', *, *, #60975, .F. ) ;
#3837=FILL_AREA_STYLE_COLOUR ( '', #47601 ) ;
#3838=EDGE_CURVE ( 'NONE', #60366, #23764, #24991, .T. ) ;
#3849=VECTOR ( 'NONE', #55287, 1000.000000000000000 ) ;
#3850=CARTESIAN_POINT ( 'NONE',  ( 0.000000000000000000, 0.9999999999999991118, -80.00402776293826435 ) ) ;
#3856=COLOUR_RGB ( '', 0.31764706, 0.68627451, 0.89019608) ;
#3872=CARTESIAN_POINT ( 'NONE',  ( 22.91412244410874166, 24.72131563869667303, 27.25834036759371770 ) ) ;
#3880=STYLED_ITEM ( 'NONE', ( #53849 ), #37537 ) ;
#3885=FILL_AREA_STYLE ('',( #56689 ) ) ;
#3886=VECTOR ( 'NONE', #58677, 1000.000000000000227 ) ;
#3889=FACE_BOUND ( 'NONE', #22831, .T. ) ;
#3899=ORIENTED_EDGE ( 'NONE', *, *, #9744, .T. ) ;
#3904=CIRCLE ( 'NONE', #58962, 1.000000000000000888 ) ;
#3906=DIRECTION ( 'NONE',  ( 1.000000000000000000, 0.000000000000000000, -0.000000000000000000 ) ) ;
#3909=VECTOR ( 'NONE', #55916, 1000.000000000000000 ) ;
#3915=SURFACE_STYLE_USAGE ( .BOTH. , #57051 ) ;
#3929=SURFACE_STYLE_FILL_AREA ( #15240 ) ;
#3933=CARTESIAN_POINT ( 'NONE',  ( 92.41620014002536720, 0.000000000000000000, -24.00402776293825369 ) ) ;
#3936=STYLED_ITEM ( 'NONE', ( #51869 ), #32479 ) ;
#3941=UNCERTAINTY_MEASURE_WITH_UNIT (LENGTH_MEASURE( 1.000000000000000082E-05 ), #17192, 'distance_accuracy_value', 'NONE');
#3950=ORIENTED_EDGE ( 'NONE', *, *, #55677, .T. ) ;
#3953=SURFACE_SIDE_STYLE ('',( #46597 ) ) ;
#3954=ORIENTED_EDGE ( 'NONE', *, *, #17731, .F. ) ;
#3963=FILL_AREA_STYLE ('',( #53232 ) ) ;
#3997=VECTOR ( 'NONE', #62801, 1000.000000000000000 ) ;
#4000=SURFACE_STYLE_USAGE ( .BOTH. , #3636 ) ;
#4016=UNCERTAINTY_MEASURE_WITH_UNIT (LENGTH_MEASURE( 1.000000000000000082E-05 ), #42839, 'distance_accuracy_value', 'NONE');
#4022=DIRECTION ( 'NONE',  ( 1.000000000000000000, 0.000000000000000000, 0.000000000000000000 ) ) ;
#4031=SURFACE_STYLE_FILL_AREA ( #35020 ) ;
#4034=DIRECTION ( 'NONE',  ( 0.000000000000000000, 1.000000000000000000, 0.000000000000000000 ) ) ;
#4039=ADVANCED_FACE ( 'NONE', ( #7355 ), #1987, .T. ) ;
#4041=SURFACE_STYLE_USAGE ( .BOTH. , #36808 ) ;
#4066=SURFACE_STYLE_FILL_AREA ( #14656 ) ;
#4075=FILL_AREA_STYLE ('',( #4789 ) ) ;
#4078=CARTESIAN_POINT ( 'NONE',  ( 8.000000000000000000, 5.000000000000000000, -72.00402776293825013 ) ) ;
#4080=ORIENTED_EDGE ( 'NONE', *, *, #13990, .T. ) ;
#4082=SURFACE_STYLE_FILL_AREA ( #52330 ) ;
#4083=FACE_OUTER_BOUND ( 'NONE', #35255, .T. ) ;
#4085=ORIENTED_EDGE ( 'NONE', *, *, #44036, .T. ) ;
#4087=( GEOMETRIC_REPRESENTATION_CONTEXT ( 3 ) GLOBAL_UNCERTAINTY_ASSIGNED_CONTEXT ( ( #59349 ) ) GLOBAL_UNIT_ASSIGNED_CONTEXT ( ( #22062, #50872, #19179 ) ) REPRESENTATION_CONTEXT ( 'NONE', 'WORKASPACE' ) );
#4099=FILL_AREA_STYLE ('',( #41108 ) ) ;
#4115=CARTESIAN_POINT ( 'NONE',  ( 36.00000000000002842, 5.000000000000000000, -29.00402776293825724 ) ) ;
#4123=EDGE_LOOP ( 'NONE', ( #21502, #31337, #42919 ) ) ;
#4126=( LENGTH_UNIT ( ) NAMED_UNIT ( * ) SI_UNIT ( .MILLI., .METRE. ) );
#4136=VERTEX_POINT ( 'NONE', #25929 ) ;
#4148=SURFACE_STYLE_USAGE ( .BOTH. , #40452 ) ;
#4164=CARTESIAN_POINT ( 'NONE',  ( 57.00000000000000000, 16.00000000000000000, 60.00402776293825724 ) ) ;
#4167=DIRECTION ( 'NONE',  ( 0.000000000000000000, 1.000000000000000000, 0.000000000000000000 ) ) ;
#4172=FACE_OUTER_BOUND ( 'NONE', #55774, .T. ) ;
#4175=VERTEX_POINT ( 'NONE', #62182 ) ;
#4186=ORIENTED_EDGE ( 'NONE', *, *, #52517, .T. ) ;
#4191=AXIS2_PLACEMENT_3D ( 'NONE', #38985, #22767, #7283 ) ;
#4193=STYLED_ITEM ( 'NONE', ( #29483 ), #4039 ) ;
#4197=VERTEX_POINT ( 'NONE', #27300 ) ;
#4200=CARTESIAN_POINT ( 'NONE',  ( 31.00000000000002132, 50.00000000000000000, 59.99999999999999289 ) ) ;
#4203=PRESENTATION_STYLE_ASSIGNMENT (( #31658 ) ) ;
#4205=LINE ( 'NONE', #19726, #63082 ) ;
#4209=COLOUR_RGB ( '', 0.72549020, 0.75294118, 0.79215686) ;
#4211=CARTESIAN_POINT ( 'NONE',  ( 22.42372113159793656, 26.68536559262205543, 27.43315461247279430 ) ) ;
#4215=SURFACE_STYLE_FILL_AREA ( #69321 ) ;
#4223=CARTESIAN_POINT ( 'NONE',  ( 107.0858988931383493, 5.000000000000000000, 16.89933289725615850 ) ) ;
#4229=CARTESIAN_POINT ( 'NONE',  ( 57.00000000000000000, 5.000000000000000000, 60.00402776293827145 ) ) ;
#4230=VERTEX_POINT ( 'NONE', #32258 ) ;
#4238=CARTESIAN_POINT ( 'NONE',  ( 57.00000000000000000, 0.000000000000000000, -60.00402776293827145 ) ) ;
#4239=ORIENTED_EDGE ( 'NONE', *, *, #14930, .F. ) ;
#4255=CARTESIAN_POINT ( 'NONE',  ( 57.00000000000000000, 5.000000000000000000, -77.00402776293825013 ) ) ;
#4262=DIRECTION ( 'NONE',  ( 0.000000000000000000, 0.000000000000000000, -1.000000000000000000 ) ) ;
#4266=DIRECTION ( 'NONE',  ( -0.000000000000000000, -1.000000000000000000, -0.000000000000000000 ) ) ;
#4269=CARTESIAN_POINT ( 'NONE',  ( 57.00000000000000000, 13.00000000000000178, -80.00402776293826435 ) ) ;
#4270=EDGE_CURVE ( 'NONE', #34116, #41524, #33311, .T. ) ;
#4276=CARTESIAN_POINT ( 'NONE',  ( 2.000000000000008438, 26.00000000000000355, -27.50000000000000355 ) ) ;
#4288=FILL_AREA_STYLE_COLOUR ( '', #47402 ) ;
#4291=EDGE_LOOP ( 'NONE', ( #39789, #264, #3038, #66591, #50857, #1984, #5177, #32336, #1865, #66498, #24742, #5439, #46378, #37136, #47519, #45097, #28688, #25996, #60039, #19614, #58211, #31462 ) ) ;
#4292=DIRECTION ( 'NONE',  ( 0.000000000000000000, 0.000000000000000000, 1.000000000000000000 ) ) ;
#4296=SURFACE_SIDE_STYLE ('',( #63073 ) ) ;
#4318=CARTESIAN_POINT ( 'NONE',  ( 74.89452121010485541, 1.000000000000000000, 66.39042820928573008 ) ) ;
#4328=CARTESIAN_POINT ( 'NONE',  ( 1.000000000000000888, 43.00000000000000000, -45.61250543006183733 ) ) ;
#4333=SURFACE_STYLE_FILL_AREA ( #35699 ) ;
#4335=EDGE_CURVE ( 'NONE', #31338, #57372, #69542, .T. ) ;
#4342=CARTESIAN_POINT ( 'NONE',  ( 11.00000000000001776, 42.00000000000000000, -29.68999999999999417 ) ) ;
#4348=SURFACE_SIDE_STYLE ('',( #35714 ) ) ;
#4349=ORIENTED_EDGE ( 'NONE', *, *, #38509, .T. ) ;
#4363=MECHANICAL_DESIGN_GEOMETRIC_PRESENTATION_REPRESENTATION('',(#62775),#24561);
#4371=ORIENTED_EDGE ( 'NONE', *, *, #19305, .F. ) ;
#4379=EDGE_CURVE ( 'NONE', #17287, #55122, #66109, .T. ) ;
#4380=STYLED_ITEM ( 'NONE', ( #68834 ), #33355 ) ;
#4387=STYLED_ITEM ( 'NONE', ( #65443 ), #51434 ) ;
#4396=STYLED_ITEM ( 'NONE', ( #18781 ), #14878 ) ;
#4398=VERTEX_POINT ( 'NONE', #12169 ) ;
#4412=FILL_AREA_STYLE ('',( #133 ) ) ;
#4419=AXIS2_PLACEMENT_3D ( 'NONE', #19359, #1757, #17987 ) ;
#4429=VECTOR ( 'NONE', #32500, 1000.000000000000000 ) ;
#4436=( NAMED_UNIT ( * ) PLANE_ANGLE_UNIT ( ) SI_UNIT ( $, .RADIAN. ) );
#4442=VECTOR ( 'NONE', #19026, 1000.000000000000000 ) ;
#4452=DIRECTION ( 'NONE',  ( 1.300977106640434891E-16, 0.000000000000000000, 1.000000000000000000 ) ) ;
#4453=COLOUR_RGB ( '', 0.72549020, 0.75294118, 0.79215686) ;
#4454=PLANE ( 'NONE',  #67086 ) ;
#4455=ORIENTED_EDGE ( 'NONE', *, *, #570, .F. ) ;
#4464=CYLINDRICAL_SURFACE ( 'NONE', #25165, 5.000000000000000888 ) ;
#4468=CARTESIAN_POINT ( 'NONE',  ( 75.83633811589984930, 0.9999999999999991118, -66.72655454856717938 ) ) ;
#4477=ORIENTED_EDGE ( 'NONE', *, *, #15533, .T. ) ;
#4480=CARTESIAN_POINT ( 'NONE',  ( 23.50000000000001776, 42.00000000000000000, -27.18999999999999417 ) ) ;
#4481=SURFACE_SIDE_STYLE ('',( #25269 ) ) ;
#4484=COLOUR_RGB ( '', 0.72549020, 0.75294118, 0.79215686) ;
#4488=PRESENTATION_STYLE_ASSIGNMENT (( #63935 ) ) ;
#4489=FILL_AREA_STYLE_COLOUR ( '', #61609 ) ;
#4493=AXIS2_PLACEMENT_3D ( 'NONE', #39264, #12481, #60664 ) ;
#4500=ADVANCED_FACE ( 'NONE', ( #46688 ), #29758, .T. ) ;
#4515=SURFACE_STYLE_USAGE ( .BOTH. , #47503 ) ;
#4530=DIRECTION ( 'NONE',  ( 0.000000000000000000, 0.000000000000000000, 1.000000000000000000 ) ) ;
#4536=ORIENTED_EDGE ( 'NONE', *, *, #8589, .F. ) ;
#4556=AXIS2_PLACEMENT_3D ( 'NONE', #1087, #17380, #43773 ) ;
#4559=EDGE_LOOP ( 'NONE', ( #7169, #67659 ) ) ;
#4569=FILL_AREA_STYLE ('',( #9546 ) ) ;
#4576=CARTESIAN_POINT ( 'NONE',  ( 22.65098652982589300, 24.94475854255456326, 27.33790873936361621 ) ) ;
#4577=LINE ( 'NONE', #58756, #67087 ) ;
#4579=VERTEX_POINT ( 'NONE', #27216 ) ;
#4586=STYLED_ITEM ( 'NONE', ( #34916 ), #45142 ) ;
#4601=UNCERTAINTY_MEASURE_WITH_UNIT (LENGTH_MEASURE( 1.000000000000000082E-05 ), #7400, 'distance_accuracy_value', 'NONE');
#4602=EDGE_CURVE ( 'NONE', #4230, #4175, #58287, .T. ) ;
#4605=ORIENTED_EDGE ( 'NONE', *, *, #8626, .T. ) ;
#4607=LINE ( 'NONE', #20085, #23120 ) ;
#4611=VECTOR ( 'NONE', #21345, 1000.000000000000000 ) ;
#4616=STYLED_ITEM ( 'NONE', ( #42405 ), #17272 ) ;
#4623=SURFACE_STYLE_FILL_AREA ( #36700 ) ;
#4627=DIRECTION ( 'NONE',  ( -0.000000000000000000, -1.000000000000000000, -0.000000000000000000 ) ) ;
#4630=FILL_AREA_STYLE ('',( #20475 ) ) ;
#4635=AXIS2_PLACEMENT_3D ( 'NONE', #6887, #28313, #49819 ) ;
#4649=ORIENTED_EDGE ( 'NONE', *, *, #68979, .T. ) ;
#4657=MECHANICAL_DESIGN_GEOMETRIC_PRESENTATION_REPRESENTATION('',(#21483),#37297);
#4659=DIRECTION ( 'NONE',  ( -0.000000000000000000, -0.000000000000000000, 1.000000000000000000 ) ) ;
#4664=ORIENTED_EDGE ( 'NONE', *, *, #35447, .T. ) ;
#4671=PRESENTATION_STYLE_ASSIGNMENT (( #52550 ) ) ;
#4676=DIRECTION ( 'NONE',  ( -0.000000000000000000, -0.000000000000000000, -1.000000000000000000 ) ) ;
#4689=EDGE_CURVE ( 'NONE', #62990, #56887, #2542, .T. ) ;
#4693=( GEOMETRIC_REPRESENTATION_CONTEXT ( 3 ) GLOBAL_UNCERTAINTY_ASSIGNED_CONTEXT ( ( #6796 ) ) GLOBAL_UNIT_ASSIGNED_CONTEXT ( ( #39712, #51986, #25232 ) ) REPRESENTATION_CONTEXT ( 'NONE', 'WORKASPACE' ) );
#4725=UNCERTAINTY_MEASURE_WITH_UNIT (LENGTH_MEASURE( 1.000000000000000082E-05 ), #40644, 'distance_accuracy_value', 'NONE');
#4728=SURFACE_STYLE_FILL_AREA ( #57150 ) ;
#4733=VERTEX_POINT ( 'NONE', #7191 ) ;
#4737=VERTEX_POINT ( 'NONE', #1496 ) ;
#4738=FACE_OUTER_BOUND ( 'NONE', #14478, .T. ) ;
#4740=AXIS2_PLACEMENT_3D ( 'NONE', #27280, #60011, #11477 ) ;
#4748=DIRECTION ( 'NONE',  ( -1.000000000000000000, 0.000000000000000000, 1.300977106640434891E-16 ) ) ;
#4756=ORIENTED_EDGE ( 'NONE', *, *, #60335, .F. ) ;
#4758=EDGE_CURVE ( 'NONE', #11331, #69112, #59476, .T. ) ;
#4760=( LENGTH_UNIT ( ) NAMED_UNIT ( * ) SI_UNIT ( .MILLI., .METRE. ) );
#4763=COLOUR_RGB ( '', 0.09019608, 0.27058824, 0.51372549) ;
#4767=AXIS2_PLACEMENT_3D ( 'NONE', #29770, #6921, #40696 ) ;
#4771=VERTEX_POINT ( 'NONE', #57096 ) ;
#4773=AXIS2_PLACEMENT_3D ( 'NONE', #42708, #43737, #32430 ) ;
#4783=CIRCLE ( 'NONE', #62065, 4.000000000000003553 ) ;
#4784=LINE ( 'NONE', #36130, #8753 ) ;
#4789=FILL_AREA_STYLE_COLOUR ( '', #38302 ) ;
#4794=AXIS2_PLACEMENT_3D ( 'NONE', #65015, #17229, #38694 ) ;
#4795=SURFACE_STYLE_USAGE ( .BOTH. , #52998 ) ;
#4800=FILL_AREA_STYLE_COLOUR ( '', #67807 ) ;
#4803=DIRECTION ( 'NONE',  ( 1.084202172485504434E-16, 0.000000000000000000, 1.000000000000000000 ) ) ;
#4804=ORIENTED_EDGE ( 'NONE', *, *, #59726, .T. ) ;
#4809=FILL_AREA_STYLE_COLOUR ( '', #49 ) ;
#4810=ORIENTED_EDGE ( 'NONE', *, *, #570, .T. ) ;
#4816=EDGE_LOOP ( 'NONE', ( #31934, #47957, #32477, #51983 ) ) ;
#4823=DIRECTION ( 'NONE',  ( -1.239088197126290324E-16, 0.000000000000000000, -1.000000000000000000 ) ) ;
#4836=CIRCLE ( 'NONE', #43068, 2.000000000000001776 ) ;
#4841=ORIENTED_EDGE ( 'NONE', *, *, #23434, .F. ) ;
#4842=ORIENTED_EDGE ( 'NONE', *, *, #18285, .F. ) ;
#4847=VERTEX_POINT ( 'NONE', #56767 ) ;
#4864=EDGE_CURVE ( 'NONE', #4197, #24855, #45879, .T. ) ;
#4874=VECTOR ( 'NONE', #43861, 1000.000000000000227 ) ;
#4877=DIRECTION ( 'NONE',  ( -1.000000000000000000, 0.000000000000000000, 0.000000000000000000 ) ) ;
#4882=ORIENTED_EDGE ( 'NONE', *, *, #65607, .F. ) ;
#4897=ORIENTED_EDGE ( 'NONE', *, *, #16324, .T. ) ;
#4898=DIRECTION ( 'NONE',  ( 0.000000000000000000, 1.000000000000000000, 0.000000000000000000 ) ) ;
#4900=VECTOR ( 'NONE', #63575, 1000.000000000000000 ) ;
#4912=EDGE_LOOP ( 'NONE', ( #56644, #49211, #64768, #33306 ) ) ;
#4918=DIRECTION ( 'NONE',  ( -0.000000000000000000, -1.000000000000000000, -0.000000000000000000 ) ) ;
#4919=STYLED_ITEM ( 'NONE', ( #34151 ), #2839 ) ;
#4926=SURFACE_STYLE_FILL_AREA ( #4569 ) ;
#4931=ADVANCED_FACE ( 'NONE', ( #20868 ), #26121, .T. ) ;
#4933=CARTESIAN_POINT ( 'NONE',  ( 23.31805810294994075, 27.43935250242352453, 27.19033932930832620 ) ) ;
#4934=( NAMED_UNIT ( * ) PLANE_ANGLE_UNIT ( ) SI_UNIT ( $, .RADIAN. ) );
#4936=ORIENTED_EDGE ( 'NONE', *, *, #16019, .T. ) ;
#4937=( NAMED_UNIT ( * ) SI_UNIT ( $, .STERADIAN. ) SOLID_ANGLE_UNIT ( ) );
#4941=LINE ( 'NONE', #32352, #66086 ) ;
#4959=DIRECTION ( 'NONE',  ( 0.000000000000000000, 0.000000000000000000, -1.000000000000000000 ) ) ;
#4967=( NAMED_UNIT ( * ) PLANE_ANGLE_UNIT ( ) SI_UNIT ( $, .RADIAN. ) );
#4968=EDGE_LOOP ( 'NONE', ( #33773, #61380, #28120, #16946, #13028, #49468 ) ) ;
#4979=ORIENTED_EDGE ( 'NONE', *, *, #2144, .F. ) ;
#4983=DIRECTION ( 'NONE',  ( 0.000000000000000000, 0.000000000000000000, -1.000000000000000000 ) ) ;
#5005=ORIENTED_EDGE ( 'NONE', *, *, #61776, .F. ) ;
#5006=DIRECTION ( 'NONE',  ( 0.000000000000000000, -1.000000000000000000, 0.000000000000000000 ) ) ;
#5009=VECTOR ( 'NONE', #22877, 1000.000000000000000 ) ;
#5013=DIRECTION ( 'NONE',  ( 1.300977106640434891E-16, -0.000000000000000000, 1.000000000000000000 ) ) ;
#5018=( LENGTH_UNIT ( ) NAMED_UNIT ( * ) SI_UNIT ( .MILLI., .METRE. ) );
#5020=FILL_AREA_STYLE ('',( #15607 ) ) ;
#5022=DIRECTION ( 'NONE',  ( 0.000000000000000000, 0.000000000000000000, -1.000000000000000000 ) ) ;
#5058=DIRECTION ( 'NONE',  ( 0.6402681315062906942, 0.000000000000000000, 0.7681514953298230752 ) ) ;
#5066=STYLED_ITEM ( 'NONE', ( #48138 ), #7960 ) ;
#5067=ORIENTED_EDGE ( 'NONE', *, *, #52466, .T. ) ;
#5077=PRESENTATION_STYLE_ASSIGNMENT (( #10383 ) ) ;
#5078=SURFACE_STYLE_FILL_AREA ( #43118 ) ;
#5087=SURFACE_STYLE_FILL_AREA ( #11049 ) ;
#5094=CIRCLE ( 'NONE', #54507, 5.000000000000004441 ) ;
#5106=SURFACE_STYLE_USAGE ( .BOTH. , #26875 ) ;
#5114=ORIENTED_EDGE ( 'NONE', *, *, #9314, .T. ) ;
#5124=UNCERTAINTY_MEASURE_WITH_UNIT (LENGTH_MEASURE( 1.000000000000000082E-05 ), #49961, 'distance_accuracy_value', 'NONE');
#5129=DIRECTION ( 'NONE',  ( 0.000000000000000000, 0.000000000000000000, 1.000000000000000000 ) ) ;
#5132=DIRECTION ( 'NONE',  ( 0.000000000000000000, -1.000000000000000000, 0.000000000000000000 ) ) ;
#5135=AXIS2_PLACEMENT_3D ( 'NONE', #32791, #6391, #27137 ) ;
#5139=ADVANCED_FACE ( 'NONE', ( #57629 ), #36570, .T. ) ;
#5149=ORIENTED_EDGE ( 'NONE', *, *, #13907, .T. ) ;
#5156=( GEOMETRIC_REPRESENTATION_CONTEXT ( 3 ) GLOBAL_UNCERTAINTY_ASSIGNED_CONTEXT ( ( #62289 ) ) GLOBAL_UNIT_ASSIGNED_CONTEXT ( ( #44266, #12183, #34000 ) ) REPRESENTATION_CONTEXT ( 'NONE', 'WORKASPACE' ) );
#5171=CARTESIAN_POINT ( 'NONE',  ( 23.50000000000001776, 14.00000000000000000, 29.68999999999999417 ) ) ;
#5177=ORIENTED_EDGE ( 'NONE', *, *, #1622, .T. ) ;
#5187=EDGE_CURVE ( 'NONE', #11384, #21950, #32267, .T. ) ;
#5193=ORIENTED_EDGE ( 'NONE', *, *, #19621, .T. ) ;
#5199=CARTESIAN_POINT ( 'NONE',  ( 16.00000000000001776, 14.00000000000000000, -33.68999999999999773 ) ) ;
#5202=FACE_OUTER_BOUND ( 'NONE', #27007, .T. ) ;
#5205=UNCERTAINTY_MEASURE_WITH_UNIT (LENGTH_MEASURE( 1.000000000000000082E-05 ), #10100, 'distance_accuracy_value', 'NONE');
#5209=( LENGTH_UNIT ( ) NAMED_UNIT ( * ) SI_UNIT ( .MILLI., .METRE. ) );
#5212=CARTESIAN_POINT ( 'NONE',  ( 23.50000000000001776, -3.148064030671221758, -27.18999999999999417 ) ) ;
#5220=( NAMED_UNIT ( * ) SI_UNIT ( $, .STERADIAN. ) SOLID_ANGLE_UNIT ( ) );
#5221=SURFACE_SIDE_STYLE ('',( #26333 ) ) ;
#5223=( LENGTH_UNIT ( ) NAMED_UNIT ( * ) SI_UNIT ( .MILLI., .METRE. ) );
#5226=ORIENTED_EDGE ( 'NONE', *, *, #66932, .F. ) ;
#5228=AXIS2_PLACEMENT_3D ( 'NONE', #40664, #62075, #24438 ) ;
#5234=PRESENTATION_STYLE_ASSIGNMENT (( #26678 ) ) ;
#5241=DIRECTION ( 'NONE',  ( 1.000000000000000000, -0.000000000000000000, -0.000000000000000000 ) ) ;
#5244=UNCERTAINTY_MEASURE_WITH_UNIT (LENGTH_MEASURE( 1.000000000000000082E-05 ), #56322, 'distance_accuracy_value', 'NONE');
#5245=DIRECTION ( 'NONE',  ( -1.000000000000000000, 0.000000000000000000, 0.000000000000000000 ) ) ;
#5258=DIRECTION ( 'NONE',  ( 0.000000000000000000, 0.000000000000000000, -1.000000000000000000 ) ) ;
#5259=( NAMED_UNIT ( * ) PLANE_ANGLE_UNIT ( ) SI_UNIT ( $, .RADIAN. ) );
#5260=CARTESIAN_POINT ( 'NONE',  ( 22.99999999999999645, 5.000000000000000000, -72.00402776293825013 ) ) ;
#5268=CARTESIAN_POINT ( 'NONE',  ( 27.99999999999998224, 5.000000000000000000, 72.00402776293822171 ) ) ;
#5272=STYLED_ITEM ( 'NONE', ( #41370 ), #50424 ) ;
#5288=VERTEX_POINT ( 'NONE', #16816 ) ;
#5294=( NAMED_UNIT ( * ) SI_UNIT ( $, .STERADIAN. ) SOLID_ANGLE_UNIT ( ) );
#5296=ORIENTED_EDGE ( 'NONE', *, *, #13243, .F. ) ;
#5298=UNCERTAINTY_MEASURE_WITH_UNIT (LENGTH_MEASURE( 1.000000000000000082E-05 ), #1309, 'distance_accuracy_value', 'NONE');
#5304=FILL_AREA_STYLE_COLOUR ( '', #12879 ) ;
#5305=ORIENTED_EDGE ( 'NONE', *, *, #41103, .T. ) ;
#5312=EDGE_CURVE ( 'NONE', #7443, #60790, #10485, .T. ) ;
#5318=ORIENTED_EDGE ( 'NONE', *, *, #14255, .T. ) ;
#5319=( NAMED_UNIT ( * ) PLANE_ANGLE_UNIT ( ) SI_UNIT ( $, .RADIAN. ) );
#5328=MECHANICAL_DESIGN_GEOMETRIC_PRESENTATION_REPRESENTATION('',(#51396),#787);
#5336=DIRECTION ( 'NONE',  ( 1.000000000000000000, -0.000000000000000000, -1.300977106640434891E-16 ) ) ;
#5356=SURFACE_SIDE_STYLE ('',( #52893 ) ) ;
#5365=( NAMED_UNIT ( * ) PLANE_ANGLE_UNIT ( ) SI_UNIT ( $, .RADIAN. ) );
#5371=EDGE_CURVE ( 'NONE', #42163, #1442, #69555, .T. ) ;
#5379=( NAMED_UNIT ( * ) SI_UNIT ( $, .STERADIAN. ) SOLID_ANGLE_UNIT ( ) );
#5381=CARTESIAN_POINT ( 'NONE',  ( 108.3664351561509278, 13.00000000000000178, 18.43563588791581154 ) ) ;
#5383=EDGE_CURVE ( 'NONE', #33963, #27344, #51150, .T. ) ;
#5386=DIRECTION ( 'NONE',  ( 0.000000000000000000, -1.000000000000000000, 0.000000000000000000 ) ) ;
#5407=( NAMED_UNIT ( * ) SI_UNIT ( $, .STERADIAN. ) SOLID_ANGLE_UNIT ( ) );
#5409=ORIENTED_EDGE ( 'NONE', *, *, #19114, .F. ) ;
#5411=( NAMED_UNIT ( * ) SI_UNIT ( $, .STERADIAN. ) SOLID_ANGLE_UNIT ( ) );
#5412=DIRECTION ( 'NONE',  ( 0.000000000000000000, 0.3420201433256629953, -0.9396926207859104263 ) ) ;
#5418=VERTEX_POINT ( 'NONE', #40339 ) ;
#5420=DIRECTION ( 'NONE',  ( 0.000000000000000000, -1.000000000000000000, 0.000000000000000000 ) ) ;
#5429=SURFACE_STYLE_FILL_AREA ( #64194 ) ;
#5435=SURFACE_STYLE_USAGE ( .BOTH. , #62548 ) ;
#5439=ORIENTED_EDGE ( 'NONE', *, *, #26963, .T. ) ;
#5440=( LENGTH_UNIT ( ) NAMED_UNIT ( * ) SI_UNIT ( .MILLI., .METRE. ) );
#5441=LINE ( 'NONE', #43513, #51910 ) ;
#5450=DIRECTION ( 'NONE',  ( 1.000000000000000000, 0.000000000000000000, 0.000000000000000000 ) ) ;
#5456=STYLED_ITEM ( 'NONE', ( #17516 ), #68551 ) ;
#5457=( LENGTH_UNIT ( ) NAMED_UNIT ( * ) SI_UNIT ( .MILLI., .METRE. ) );
#5458=PRESENTATION_STYLE_ASSIGNMENT (( #4795 ) ) ;
#5460=ORIENTED_EDGE ( 'NONE', *, *, #20519, .T. ) ;
#5461=FACE_BOUND ( 'NONE', #34692, .T. ) ;
#5471=FACE_OUTER_BOUND ( 'NONE', #61817, .T. ) ;
#5475=PLANE ( 'NONE',  #28830 ) ;
#5478=DIRECTION ( 'NONE',  ( 1.000000000000000000, -0.000000000000000000, -1.300977106640434891E-16 ) ) ;
#5480=ORIENTED_EDGE ( 'NONE', *, *, #59212, .T. ) ;
#5489=VERTEX_POINT ( 'NONE', #67755 ) ;
#5490=CARTESIAN_POINT ( 'NONE',  ( 10.00000000000000533, 43.00000000000000000, -45.61250543006183733 ) ) ;
#5494=AXIS2_PLACEMENT_3D ( 'NONE', #37092, #389, #21919 ) ;
#5495=( NAMED_UNIT ( * ) PLANE_ANGLE_UNIT ( ) SI_UNIT ( $, .RADIAN. ) );
#5496=COLOUR_RGB ( '', 0.72549020, 0.75294118, 0.79215686) ;
#5497=FILL_AREA_STYLE ('',( #10814 ) ) ;
#5503=ORIENTED_EDGE ( 'NONE', *, *, #7396, .T. ) ;
#5514=DIRECTION ( 'NONE',  ( 1.000000000000000000, 0.000000000000000000, -0.000000000000000000 ) ) ;
#5522=( LENGTH_UNIT ( ) NAMED_UNIT ( * ) SI_UNIT ( .MILLI., .METRE. ) );
#5534=VECTOR ( 'NONE', #9742, 1000.000000000000000 ) ;
#5537=CIRCLE ( 'NONE', #12270, 1.000000000000000888 ) ;
#5540=CIRCLE ( 'NONE', #31358, 4.999999999999997335 ) ;
#5541=SURFACE_STYLE_FILL_AREA ( #37635 ) ;
#5547=FILL_AREA_STYLE_COLOUR ( '', #56268 ) ;
#5558=CARTESIAN_POINT ( 'NONE',  ( 22.00000000000001776, 43.00000000000000000, 45.61250543006183022 ) ) ;
#5559=CYLINDRICAL_SURFACE ( 'NONE', #26221, 1.000000000000000888 ) ;
#5571=CIRCLE ( 'NONE', #40469, 5.000000000000004441 ) ;
#5577=SURFACE_STYLE_USAGE ( .BOTH. , #16539 ) ;
#5587=COLOUR_RGB ( '', 0.72549020, 0.75294118, 0.79215686) ;
#5595=STYLED_ITEM ( 'NONE', ( #10944 ), #34175 ) ;
#5612=COLOUR_RGB ( '', 0.66274510, 0.83137255, 0.94901961) ;
#5618=PRESENTATION_STYLE_ASSIGNMENT (( #16236 ) ) ;
#5629=ORIENTED_EDGE ( 'NONE', *, *, #14798, .T. ) ;
#5636=CARTESIAN_POINT ( 'NONE',  ( 1.000000000000000000, 42.00000000000000000, 80.00402776293826435 ) ) ;
#5642=AXIS2_PLACEMENT_3D ( 'NONE', #53668, #11455, #58605 ) ;
#5647=FILL_AREA_STYLE ('',( #5304 ) ) ;
#5661=MECHANICAL_DESIGN_GEOMETRIC_PRESENTATION_REPRESENTATION('',(#43887),#22514);
#5668=ORIENTED_EDGE ( 'NONE', *, *, #56144, .F. ) ;
#5673=CYLINDRICAL_SURFACE ( 'NONE', #45209, 1.000000000000000888 ) ;
#5676=ORIENTED_EDGE ( 'NONE', *, *, #53086, .F. ) ;
#5693=EDGE_CURVE ( 'NONE', #23198, #56887, #10766, .T. ) ;
#5701=ORIENTED_EDGE ( 'NONE', *, *, #69502, .T. ) ;
#5703=CARTESIAN_POINT ( 'NONE',  ( 92.41620014002536720, 5.000000000000000000, 24.00402776293825369 ) ) ;
#5710=MECHANICAL_DESIGN_GEOMETRIC_PRESENTATION_REPRESENTATION('',(#43931),#18085);
#5719=DIRECTION ( 'NONE',  ( -0.000000000000000000, -1.000000000000000000, 0.000000000000000000 ) ) ;
#5735=PRESENTATION_STYLE_ASSIGNMENT (( #37485 ) ) ;
#5737=AXIS2_PLACEMENT_3D ( 'NONE', #62244, #45432, #14071 ) ;
#5740=STYLED_ITEM ( 'NONE', ( #61707 ), #34932 ) ;
#5744=FILL_AREA_STYLE_COLOUR ( '', #39492 ) ;
#5749=FILL_AREA_STYLE_COLOUR ( '', #22741 ) ;
#5751=FILL_AREA_STYLE_COLOUR ( '', #41850 ) ;
#5760=LINE ( 'NONE', #23017, #53893 ) ;
#5761=ORIENTED_EDGE ( 'NONE', *, *, #50765, .T. ) ;
#5767=( NAMED_UNIT ( * ) PLANE_ANGLE_UNIT ( ) SI_UNIT ( $, .RADIAN. ) );
#5776=ADVANCED_FACE ( 'NONE', ( #59742 ), #44991, .F. ) ;
#5785=LINE ( 'NONE', #21636, #34349 ) ;
#5805=VECTOR ( 'NONE', #39229, 1000.000000000000000 ) ;
#5814=VECTOR ( 'NONE', #68184, 1000.000000000000000 ) ;
#5817=CIRCLE ( 'NONE', #12549, 4.999999999999997335 ) ;
#5818=DIRECTION ( 'NONE',  ( -1.000000000000000000, 0.000000000000000000, -0.000000000000000000 ) ) ;
#5819=VERTEX_POINT ( 'NONE', #51274 ) ;
#5820=( LENGTH_UNIT ( ) NAMED_UNIT ( * ) SI_UNIT ( .MILLI., .METRE. ) );
#5832=ORIENTED_EDGE ( 'NONE', *, *, #21264, .F. ) ;
#5850=( GEOMETRIC_REPRESENTATION_CONTEXT ( 3 ) GLOBAL_UNCERTAINTY_ASSIGNED_CONTEXT ( ( #51124 ) ) GLOBAL_UNIT_ASSIGNED_CONTEXT ( ( #47660, #58495, #53234 ) ) REPRESENTATION_CONTEXT ( 'NONE', 'WORKASPACE' ) );
#5851=( LENGTH_UNIT ( ) NAMED_UNIT ( * ) SI_UNIT ( .MILLI., .METRE. ) );
#5852=ADVANCED_FACE ( 'NONE', ( #29456 ), #36159, .T. ) ;
#5857=CARTESIAN_POINT ( 'NONE',  ( 27.99999999999999645, 5.000000000000000000, -24.00402776293821816 ) ) ;
#5860=FILL_AREA_STYLE ('',( #16808 ) ) ;
#5862=ADVANCED_FACE ( 'NONE', ( #5471 ), #36863, .F. ) ;
#5867=ORIENTED_EDGE ( 'NONE', *, *, #49039, .F. ) ;
#5879=CIRCLE ( 'NONE', #45249, 4.999999999999997335 ) ;
#5880=( GEOMETRIC_REPRESENTATION_CONTEXT ( 3 ) GLOBAL_UNCERTAINTY_ASSIGNED_CONTEXT ( ( #41859 ) ) GLOBAL_UNIT_ASSIGNED_CONTEXT ( ( #13610, #44303, #61111 ) ) REPRESENTATION_CONTEXT ( 'NONE', 'WORKASPACE' ) );
#5891=( NAMED_UNIT ( * ) SI_UNIT ( $, .STERADIAN. ) SOLID_ANGLE_UNIT ( ) );
#5901=CARTESIAN_POINT ( 'NONE',  ( 27.00000000000001776, 15.00000000000000000, -34.49999999999999289 ) ) ;
#5905=CIRCLE ( 'NONE', #4767, 1.000000000000000888 ) ;
#5911=EDGE_CURVE ( 'NONE', #21950, #23421, #25556, .T. ) ;
#5916=ORIENTED_EDGE ( 'NONE', *, *, #55276, .F. ) ;
#5924=MECHANICAL_DESIGN_GEOMETRIC_PRESENTATION_REPRESENTATION('',(#39663),#13830);
#5929=ORIENTED_EDGE ( 'NONE', *, *, #61667, .F. ) ;
#5940=FILL_AREA_STYLE_COLOUR ( '', #23869 ) ;
#5964=SURFACE_STYLE_FILL_AREA ( #36657 ) ;
#5970=COLOUR_RGB ( '', 0.40784314, 0.44705882, 0.49803922) ;
#5974=CARTESIAN_POINT ( 'NONE',  ( 23.50000000000041211, 24.55989583709592949, -27.18999999999997286 ) ) ;
#5986=AXIS2_PLACEMENT_3D ( 'NONE', #53935, #10697, #48721 ) ;
#5992=AXIS2_PLACEMENT_3D ( 'NONE', #46941, #18763, #3581 ) ;
#5993=ORIENTED_EDGE ( 'NONE', *, *, #12746, .T. ) ;
#6000=ORIENTED_EDGE ( 'NONE', *, *, #62333, .T. ) ;
#6005=VECTOR ( 'NONE', #58297, 1000.000000000000000 ) ;
#6008=PRESENTATION_STYLE_ASSIGNMENT (( #23831 ) ) ;
#6012=AXIS2_PLACEMENT_3D ( 'NONE', #43625, #37321, #16541 ) ;
#6017=AXIS2_PLACEMENT_3D ( 'NONE', #4078, #24851, #46366 ) ;
#6023=( NAMED_UNIT ( * ) SI_UNIT ( $, .STERADIAN. ) SOLID_ANGLE_UNIT ( ) );
#6026=ORIENTED_EDGE ( 'NONE', *, *, #54064, .T. ) ;
#6034=ORIENTED_EDGE ( 'NONE', *, *, #46279, .F. ) ;
#6037=UNCERTAINTY_MEASURE_WITH_UNIT (LENGTH_MEASURE( 1.000000000000000082E-05 ), #21068, 'distance_accuracy_value', 'NONE');
#6038=SURFACE_SIDE_STYLE ('',( #65475 ) ) ;
#6040=( LENGTH_UNIT ( ) NAMED_UNIT ( * ) SI_UNIT ( .MILLI., .METRE. ) );
#6049=UNCERTAINTY_MEASURE_WITH_UNIT (LENGTH_MEASURE( 1.000000000000000082E-05 ), #38544, 'distance_accuracy_value', 'NONE');
#6068=CARTESIAN_POINT ( 'NONE',  ( 31.00000000000002132, 42.00000000000000000, 75.00000000000000000 ) ) ;
#6070=AXIS2_PLACEMENT_3D ( 'NONE', #34908, #46199, #2498 ) ;
#6077=MECHANICAL_DESIGN_GEOMETRIC_PRESENTATION_REPRESENTATION('',(#15109),#2665);
#6079=PRESENTATION_STYLE_ASSIGNMENT (( #11007 ) ) ;
#6094=CARTESIAN_POINT ( 'NONE',  ( 1.000000000000000888, 43.00000000000000000, 74.38749456993816978 ) ) ;
#6095=DIRECTION ( 'NONE',  ( 0.000000000000000000, 0.000000000000000000, 1.000000000000000000 ) ) ;
#6096=PLANE ( 'NONE',  #6070 ) ;
#6104=EDGE_CURVE ( 'NONE', #46312, #54047, #51815, .T. ) ;
#6115=UNCERTAINTY_MEASURE_WITH_UNIT (LENGTH_MEASURE( 1.000000000000000082E-05 ), #58706, 'distance_accuracy_value', 'NONE');
#6116=CARTESIAN_POINT ( 'NONE',  ( 57.00000000000000000, 5.000000000000000000, -55.00402776293825724 ) ) ;
#6123=FACE_OUTER_BOUND ( 'NONE', #15272, .T. ) ;
#6125=FILL_AREA_STYLE ('',( #38872 ) ) ;
#6131=LINE ( 'NONE', #17740, #17365 ) ;
#6142=CARTESIAN_POINT ( 'NONE',  ( 31.14385416795345307, 42.99999999999999289, -45.61250543006184444 ) ) ;
#6145=SURFACE_SIDE_STYLE ('',( #32886 ) ) ;
#6164=FACE_OUTER_BOUND ( 'NONE', #27520, .T. ) ;
#6170=SPHERICAL_SURFACE ( 'NONE', #52688, 1.000000000000000000 ) ;
#6183=CARTESIAN_POINT ( 'NONE',  ( 93.00000000000000000, 0.000000000000000000, 0.000000000000000000 ) ) ;
#6190=FACE_OUTER_BOUND ( 'NONE', #32555, .T. ) ;
#6193=ORIENTED_EDGE ( 'NONE', *, *, #5187, .F. ) ;
#6195=EDGE_CURVE ( 'NONE', #4847, #51461, #43131, .T. ) ;
#6198=FILL_AREA_STYLE_COLOUR ( '', #45704 ) ;
#6223=DIRECTION ( 'NONE',  ( -1.000000000000000000, 0.000000000000000000, -0.000000000000000000 ) ) ;
#6227=DIRECTION ( 'NONE',  ( -0.000000000000000000, 0.000000000000000000, -1.000000000000000000 ) ) ;
#6233=DIRECTION ( 'NONE',  ( 0.000000000000000000, 1.000000000000000000, 0.000000000000000000 ) ) ;
#6243=CARTESIAN_POINT ( 'NONE',  ( 32.00000000000000000, 42.00000000000000000, -74.38749456993816978 ) ) ;
#6251=SURFACE_STYLE_USAGE ( .BOTH. , #48171 ) ;
#6254=DIRECTION ( 'NONE',  ( 0.000000000000000000, -1.000000000000000000, 0.000000000000000000 ) ) ;
#6256=( NAMED_UNIT ( * ) PLANE_ANGLE_UNIT ( ) SI_UNIT ( $, .RADIAN. ) );
#6275=EDGE_LOOP ( 'NONE', ( #15555, #18332, #59764, #20222 ) ) ;
#6279=EDGE_CURVE ( 'NONE', #16530, #17308, #47976, .T. ) ;
#6281=STYLED_ITEM ( 'NONE', ( #66064 ), #732 ) ;
#6294=ORIENTED_EDGE ( 'NONE', *, *, #47050, .F. ) ;
#6308=EDGE_LOOP ( 'NONE', ( #61242, #8580, #31099, #47846 ) ) ;
#6314=SURFACE_STYLE_FILL_AREA ( #954 ) ;
#6324=( NAMED_UNIT ( * ) SI_UNIT ( $, .STERADIAN. ) SOLID_ANGLE_UNIT ( ) );
#6326=CARTESIAN_POINT ( 'NONE',  ( 23.50000000000001776, 24.55989583710066171, 27.18999999999999062 ) ) ;
#6342=EDGE_CURVE ( 'NONE', #51568, #29587, #31818, .T. ) ;
#6346=DIRECTION ( 'NONE',  ( -1.000000000000000000, 0.000000000000000000, 0.000000000000000000 ) ) ;
#6367=ORIENTED_EDGE ( 'NONE', *, *, #56153, .F. ) ;
#6368=FACE_OUTER_BOUND ( 'NONE', #66542, .T. ) ;
#6374=VERTEX_POINT ( 'NONE', #34495 ) ;
#6379=DIRECTION ( 'NONE',  ( 1.300977106640434891E-16, 0.000000000000000000, 1.000000000000000000 ) ) ;
#6391=DIRECTION ( 'NONE',  ( 0.000000000000000000, -0.000000000000000000, 1.000000000000000000 ) ) ;
#6394=CIRCLE ( 'NONE', #61410, 5.999999999999998224 ) ;
#6418=VECTOR ( 'NONE', #63904, 1000.000000000000000 ) ;
#6419=COLOUR_RGB ( '', 0.66274510, 0.83137255, 0.94901961) ;
#6427=CARTESIAN_POINT ( 'NONE',  ( 33.00000000000000000, 14.00000000000000000, -79.00402776293826435 ) ) ;
#6441=DIRECTION ( 'NONE',  ( -0.000000000000000000, -1.000000000000000000, -0.000000000000000000 ) ) ;
#6442=DIRECTION ( 'NONE',  ( 0.000000000000000000, 1.000000000000000000, 0.000000000000000000 ) ) ;
#6444=CARTESIAN_POINT ( 'NONE',  ( 1.000000000000000000, 1.000000000000000000, -79.00402776293826435 ) ) ;
#6449=FACE_OUTER_BOUND ( 'NONE', #7847, .T. ) ;
#6451=( NAMED_UNIT ( * ) PLANE_ANGLE_UNIT ( ) SI_UNIT ( $, .RADIAN. ) );
#6453=( LENGTH_UNIT ( ) NAMED_UNIT ( * ) SI_UNIT ( .MILLI., .METRE. ) );
#6461=CARTESIAN_POINT ( 'NONE',  ( 93.00000000000000000, 14.00000000000000000, 0.000000000000000000 ) ) ;
#6475=CYLINDRICAL_SURFACE ( 'NONE', #18993, 4.999999999999997335 ) ;
#6484=ORIENTED_EDGE ( 'NONE', *, *, #68808, .F. ) ;
#6487=UNCERTAINTY_MEASURE_WITH_UNIT (LENGTH_MEASURE( 1.000000000000000082E-05 ), #51686, 'distance_accuracy_value', 'NONE');
#6492=CARTESIAN_POINT ( 'NONE',  ( 11.00000000000001954, 17.23130743308432855, -3.198396408832238080E-15 ) ) ;
#6499=CARTESIAN_POINT ( 'NONE',  ( 31.00000000000001066, 42.00000000000000000, -4.033029030585349936E-15 ) ) ;
#6502=DIRECTION ( 'NONE',  ( -0.000000000000000000, -0.000000000000000000, -1.000000000000000000 ) ) ;
#6503=CIRCLE ( 'NONE', #53669, 5.000000000000004441 ) ;
#6506=ORIENTED_EDGE ( 'NONE', *, *, #8191, .F. ) ;
#6507=DIRECTION ( 'NONE',  ( -0.000000000000000000, -1.000000000000000000, -0.000000000000000000 ) ) ;
#6511=( GEOMETRIC_REPRESENTATION_CONTEXT ( 3 ) GLOBAL_UNCERTAINTY_ASSIGNED_CONTEXT ( ( #65034 ) ) GLOBAL_UNIT_ASSIGNED_CONTEXT ( ( #58517, #37474, #10347 ) ) REPRESENTATION_CONTEXT ( 'NONE', 'WORKASPACE' ) );
#6519=SURFACE_SIDE_STYLE ('',( #65285 ) ) ;
#6521=FACE_OUTER_BOUND ( 'NONE', #30175, .T. ) ;
#6530=UNCERTAINTY_MEASURE_WITH_UNIT (LENGTH_MEASURE( 1.000000000000000082E-05 ), #156, 'distance_accuracy_value', 'NONE');
#6533=CARTESIAN_POINT ( 'NONE',  ( 57.00000000000000000, 13.00000000000000178, 60.00402776293827145 ) ) ;
#6552=( NAMED_UNIT ( * ) SI_UNIT ( $, .STERADIAN. ) SOLID_ANGLE_UNIT ( ) );
#6556=FILL_AREA_STYLE_COLOUR ( '', #21196 ) ;
#6570=FILL_AREA_STYLE ('',( #54756 ) ) ;
#6574=CARTESIAN_POINT ( 'NONE',  ( 10.00000000000001776, 43.00000000000000000, -28.00000000000000000 ) ) ;
#6578=FACE_OUTER_BOUND ( 'NONE', #58655, .T. ) ;
#6581=EDGE_CURVE ( 'NONE', #62171, #45281, #35248, .T. ) ;
#6587=VERTEX_POINT ( 'NONE', #31986 ) ;
#6588=CIRCLE ( 'NONE', #26815, 1.000000000000000888 ) ;
#6593=CARTESIAN_POINT ( 'NONE',  ( 2.999999999999994671, 0.000000000000000000, -24.00402776293822527 ) ) ;
#6598=ORIENTED_EDGE ( 'NONE', *, *, #39046, .F. ) ;
#6603=ORIENTED_EDGE ( 'NONE', *, *, #56069, .F. ) ;
#6610=CARTESIAN_POINT ( 'NONE',  ( 31.00000000000002132, 43.00000000000000000, 79.00402776293826435 ) ) ;
#6614=ORIENTED_EDGE ( 'NONE', *, *, #38592, .T. ) ;
#6617=DIRECTION ( 'NONE',  ( -1.300977106640434891E-16, 0.000000000000000000, -1.000000000000000000 ) ) ;
#6624=FILL_AREA_STYLE_COLOUR ( '', #58508 ) ;
#6639=( LENGTH_UNIT ( ) NAMED_UNIT ( * ) SI_UNIT ( .MILLI., .METRE. ) );
#6641=ORIENTED_EDGE ( 'NONE', *, *, #13907, .F. ) ;
#6643=DIRECTION ( 'NONE',  ( 3.717264591378879477E-17, 0.000000000000000000, -1.000000000000000000 ) ) ;
#6648=( LENGTH_UNIT ( ) NAMED_UNIT ( * ) SI_UNIT ( .MILLI., .METRE. ) );
#6655=EDGE_CURVE ( 'NONE', #66133, #66860, #38354, .T. ) ;
#6658=CARTESIAN_POINT ( 'NONE',  ( 30.99999999999998579, 5.000000000000000000, 72.00402776293822171 ) ) ;
#6662=EDGE_CURVE ( 'NONE', #29216, #25731, #58376, .T. ) ;
#6663=EDGE_CURVE ( 'NONE', #45281, #62171, #36407, .T. ) ;
#6671=LINE ( 'NONE', #39086, #8119 ) ;
#6672=UNCERTAINTY_MEASURE_WITH_UNIT (LENGTH_MEASURE( 1.000000000000000082E-05 ), #60024, 'distance_accuracy_value', 'NONE');
#6673=VECTOR ( 'NONE', #9576, 1000.000000000000000 ) ;
#6681=( NAMED_UNIT ( * ) SI_UNIT ( $, .STERADIAN. ) SOLID_ANGLE_UNIT ( ) );
#6683=DIRECTION ( 'NONE',  ( -0.000000000000000000, -1.000000000000000000, -0.000000000000000000 ) ) ;
#6684=SURFACE_STYLE_FILL_AREA ( #53513 ) ;
#6702=ORIENTED_EDGE ( 'NONE', *, *, #25110, .T. ) ;
#6705=PRESENTATION_STYLE_ASSIGNMENT (( #1386 ) ) ;
#6714=STYLED_ITEM ( 'NONE', ( #68356 ), #41731 ) ;
#6719=SURFACE_STYLE_USAGE ( .BOTH. , #6038 ) ;
#6722=ORIENTED_EDGE ( 'NONE', *, *, #33756, .T. ) ;
#6725=MECHANICAL_DESIGN_GEOMETRIC_PRESENTATION_REPRESENTATION('',(#23545),#26885);
#6730=PRESENTATION_STYLE_ASSIGNMENT (( #23273 ) ) ;
#6731=UNCERTAINTY_MEASURE_WITH_UNIT (LENGTH_MEASURE( 1.000000000000000082E-05 ), #25907, 'distance_accuracy_value', 'NONE');
#6732=STYLED_ITEM ( 'NONE', ( #17623 ), #16349 ) ;
#6751=DIRECTION ( 'NONE',  ( 1.000000000000000000, 0.000000000000000000, 0.000000000000000000 ) ) ;
#6757=SURFACE_SIDE_STYLE ('',( #17361 ) ) ;
#6767=MECHANICAL_DESIGN_GEOMETRIC_PRESENTATION_REPRESENTATION('',(#68557),#65165);
#6768=( GEOMETRIC_REPRESENTATION_CONTEXT ( 3 ) GLOBAL_UNCERTAINTY_ASSIGNED_CONTEXT ( ( #38373 ) ) GLOBAL_UNIT_ASSIGNED_CONTEXT ( ( #61862, #35505, #51680 ) ) REPRESENTATION_CONTEXT ( 'NONE', 'WORKASPACE' ) );
#6775=DIRECTION ( 'NONE',  ( 0.000000000000000000, 1.000000000000000000, 0.000000000000000000 ) ) ;
#6776=FACE_OUTER_BOUND ( 'NONE', #64276, .T. ) ;
#6778=DIRECTION ( 'NONE',  ( -0.000000000000000000, -1.000000000000000000, -0.000000000000000000 ) ) ;
#6780=CIRCLE ( 'NONE', #67435, 4.999999999999997335 ) ;
#6794=( GEOMETRIC_REPRESENTATION_CONTEXT ( 3 ) GLOBAL_UNCERTAINTY_ASSIGNED_CONTEXT ( ( #23611 ) ) GLOBAL_UNIT_ASSIGNED_CONTEXT ( ( #42378, #58501, #31751 ) ) REPRESENTATION_CONTEXT ( 'NONE', 'WORKASPACE' ) );
#6796=UNCERTAINTY_MEASURE_WITH_UNIT (LENGTH_MEASURE( 1.000000000000000082E-05 ), #39712, 'distance_accuracy_value', 'NONE');
#6799=CARTESIAN_POINT ( 'NONE',  ( 93.00000000000000000, 5.000000000000000000, 0.000000000000000000 ) ) ;
#6801=STYLED_ITEM ( 'NONE', ( #33522 ), #21316 ) ;
#6802=DIRECTION ( 'NONE',  ( 1.300977106640434891E-16, -0.000000000000000000, 1.000000000000000000 ) ) ;
#6805=SURFACE_SIDE_STYLE ('',( #27558 ) ) ;
#6820=EDGE_CURVE ( 'NONE', #54496, #39359, #44329, .T. ) ;
#6821=LINE ( 'NONE', #53040, #54178 ) ;
#6822=CARTESIAN_POINT ( 'NONE',  ( 32.00000000000000711, 42.24279663153597397, -45.14569480374318289 ) ) ;
#6826=SURFACE_STYLE_USAGE ( .BOTH. , #6145 ) ;
#6835=ORIENTED_EDGE ( 'NONE', *, *, #33679, .F. ) ;
#6837=CYLINDRICAL_SURFACE ( 'NONE', #48255, 16.99999999999998579 ) ;
#6841=SURFACE_STYLE_USAGE ( .BOTH. , #12809 ) ;
#6845=DIRECTION ( 'NONE',  ( 0.000000000000000000, -0.6691306063588592368, 0.7431448254773934670 ) ) ;
#6849=ORIENTED_EDGE ( 'NONE', *, *, #36972, .F. ) ;
#6868=CIRCLE ( 'NONE', #10306, 14.00000000000000533 ) ;
#6871=VECTOR ( 'NONE', #26421, 1000.000000000000000 ) ;
#6875=PRESENTATION_STYLE_ASSIGNMENT (( #39968 ) ) ;
#6887=CARTESIAN_POINT ( 'NONE',  ( 57.00000000000000000, 13.00000000000000178, 79.00402776293826435 ) ) ;
#6891=CIRCLE ( 'NONE', #60806, 16.99999999999998579 ) ;
#6900=DIRECTION ( 'NONE',  ( -0.000000000000000000, 1.000000000000000000, -0.000000000000000000 ) ) ;
#6907=( NAMED_UNIT ( * ) SI_UNIT ( $, .STERADIAN. ) SOLID_ANGLE_UNIT ( ) );
#6910=DIRECTION ( 'NONE',  ( 0.000000000000000000, 0.000000000000000000, -1.000000000000000000 ) ) ;
#6914=DIRECTION ( 'NONE',  ( -1.000000000000000000, -0.000000000000000000, 1.300977106640434891E-16 ) ) ;
#6921=DIRECTION ( 'NONE',  ( 0.000000000000000000, 1.000000000000000000, 0.000000000000000000 ) ) ;
#6928=LINE ( 'NONE', #34688, #67307 ) ;
#6948=SURFACE_SIDE_STYLE ('',( #1620 ) ) ;
#6958=ORIENTED_EDGE ( 'NONE', *, *, #28495, .T. ) ;
#6970=CARTESIAN_POINT ( 'NONE',  ( 98.00000000000000000, 16.00000000000000000, 0.000000000000000000 ) ) ;
#6982=VECTOR ( 'NONE', #14199, 1000.000000000000000 ) ;
#7003=CARTESIAN_POINT ( 'NONE',  ( 11.00000000000001776, -35.45414562583513884, -57.63767942241966580 ) ) ;
#7006=CARTESIAN_POINT ( 'NONE',  ( 28.00000000000002132, 34.36176364315826248, 80.00402776293826435 ) ) ;
#7009=ORIENTED_EDGE ( 'NONE', *, *, #30853, .T. ) ;
#7011=EDGE_LOOP ( 'NONE', ( #40780, #45304, #65041, #37862 ) ) ;
#7013=EDGE_CURVE ( 'NONE', #4733, #29677, #53027, .T. ) ;
#7015=ORIENTED_EDGE ( 'NONE', *, *, #28386, .T. ) ;
#7017=LINE ( 'NONE', #55895, #53200 ) ;
#7018=MECHANICAL_DESIGN_GEOMETRIC_PRESENTATION_REPRESENTATION('',(#19356),#18266);
#7020=ORIENTED_EDGE ( 'NONE', *, *, #49659, .F. ) ;
#7030=FILL_AREA_STYLE ('',( #14049 ) ) ;
#7039=( BOUNDED_CURVE ( )  B_SPLINE_CURVE ( 3, ( #37337, #54139, #69633, #16212 ),
 .UNSPECIFIED., .F., .F. ) 
 B_SPLINE_CURVE_WITH_KNOTS ( ( 4, 4 ),
 ( 4.712388980384690562, 5.445427266222309548 ),
 .UNSPECIFIED. ) 
 CURVE ( )  GEOMETRIC_REPRESENTATION_ITEM ( )  RATIONAL_B_SPLINE_CURVE ( ( 1.000000000000000000, 0.9557202843314677176, 0.9557202843314677176, 1.000000000000000000 ) ) 
 REPRESENTATION_ITEM ( '' )  );
#7041=FILL_AREA_STYLE ('',( #13344 ) ) ;
#7046=VECTOR ( 'NONE', #6227, 1000.000000000000000 ) ;
#7047=ORIENTED_EDGE ( 'NONE', *, *, #35012, .T. ) ;
#7052=( LENGTH_UNIT ( ) NAMED_UNIT ( * ) SI_UNIT ( .MILLI., .METRE. ) );
#7055=FILL_AREA_STYLE_COLOUR ( '', #9093 ) ;
#7072=ORIENTED_EDGE ( 'NONE', *, *, #68020, .T. ) ;
#7077=ORIENTED_EDGE ( 'NONE', *, *, #2589, .F. ) ;
#7085=EDGE_CURVE ( 'NONE', #57872, #61983, #9303, .T. ) ;
#7107=FACE_OUTER_BOUND ( 'NONE', #910, .T. ) ;
#7111=DIRECTION ( 'NONE',  ( -0.000000000000000000, -0.000000000000000000, 1.000000000000000000 ) ) ;
#7131=SURFACE_SIDE_STYLE ('',( #12742 ) ) ;
#7141=CARTESIAN_POINT ( 'NONE',  ( 21.00000000000001776, 15.00000000000000000, -29.68999999999999417 ) ) ;
#7144=STYLED_ITEM ( 'NONE', ( #33205 ), #62484 ) ;
#7169=ORIENTED_EDGE ( 'NONE', *, *, #9108, .T. ) ;
#7173=ORIENTED_EDGE ( 'NONE', *, *, #65103, .F. ) ;
#7177=ADVANCED_FACE ( 'NONE', ( #49483 ), #12159, .F. ) ;
#7179=ORIENTED_EDGE ( 'NONE', *, *, #14976, .T. ) ;
#7191=CARTESIAN_POINT ( 'NONE',  ( 11.00000000000001776, 42.00000000000000000, 28.38386403503541899 ) ) ;
#7194=LINE ( 'NONE', #1846, #54171 ) ;
#7207=FILL_AREA_STYLE ('',( #65941 ) ) ;
#7215=CARTESIAN_POINT ( 'NONE',  ( 10.00000000000001954, 50.00000000000000000, 46.00000000000000000 ) ) ;
#7217=DIRECTION ( 'NONE',  ( 0.000000000000000000, 0.000000000000000000, 1.000000000000000000 ) ) ;
#7222=CIRCLE ( 'NONE', #35292, 1.000000000000000888 ) ;
#7232=VECTOR ( 'NONE', #41424, 1000.000000000000000 ) ;
#7237=DIRECTION ( 'NONE',  ( 0.000000000000000000, -1.000000000000000000, 0.000000000000000000 ) ) ;
#7242=FILL_AREA_STYLE ('',( #33956 ) ) ;
#7243=CARTESIAN_POINT ( 'NONE',  ( 16.00000000000001776, 43.00000000000000000, 35.68999999999999062 ) ) ;
#7250=DIRECTION ( 'NONE',  ( -1.000000000000000000, 0.000000000000000000, 0.000000000000000000 ) ) ;
#7256=VERTEX_POINT ( 'NONE', #40314 ) ;
#7259=ADVANCED_FACE ( 'NONE', ( #56837 ), #24118, .F. ) ;
#7262=DIRECTION ( 'NONE',  ( 0.000000000000000000, 0.000000000000000000, -1.000000000000000000 ) ) ;
#7266=DIRECTION ( 'NONE',  ( 1.000000000000000000, 0.000000000000000000, -1.300977106640435137E-16 ) ) ;
#7268=( LENGTH_UNIT ( ) NAMED_UNIT ( * ) SI_UNIT ( .MILLI., .METRE. ) );
#7281=CARTESIAN_POINT ( 'NONE',  ( 0.08961491207242036627, 42.48853761352472702, 45.29557347147078872 ) ) ;
#7283=DIRECTION ( 'NONE',  ( 0.000000000000000000, 0.000000000000000000, -1.000000000000000000 ) ) ;
#7287=CARTESIAN_POINT ( 'NONE',  ( 4.000000000000002665, 38.70020753820971748, -89.00000000000000000 ) ) ;
#7304=( GEOMETRIC_REPRESENTATION_CONTEXT ( 3 ) GLOBAL_UNCERTAINTY_ASSIGNED_CONTEXT ( ( #20717 ) ) GLOBAL_UNIT_ASSIGNED_CONTEXT ( ( #1473, #60951, #34570 ) ) REPRESENTATION_CONTEXT ( 'NONE', 'WORKASPACE' ) );
#7305=STYLED_ITEM ( 'NONE', ( #15734 ), #5862 ) ;
#7308=( LENGTH_UNIT ( ) NAMED_UNIT ( * ) SI_UNIT ( .MILLI., .METRE. ) );
#7309=CARTESIAN_POINT ( 'NONE',  ( 16.00000000000001776, 15.00000000000000000, 29.68999999999999417 ) ) ;
#7317=PRESENTATION_STYLE_ASSIGNMENT (( #24169 ) ) ;
#7319=ORIENTED_EDGE ( 'NONE', *, *, #3780, .T. ) ;
#7324=FILL_AREA_STYLE_COLOUR ( '', #1485 ) ;
#7327=ORIENTED_EDGE ( 'NONE', *, *, #10519, .F. ) ;
#7329=ORIENTED_EDGE ( 'NONE', *, *, #68891, .T. ) ;
#7330=CARTESIAN_POINT ( 'NONE',  ( 31.00000000000000711, 15.00000000000000711, -36.50000000000000000 ) ) ;
#7344=B_SPLINE_CURVE_WITH_KNOTS ( 'NONE', 3,
 ( #6094, #17381, #22981, #23651, #45157, #23312, #28911, #49055 ),
 .UNSPECIFIED., .F., .F.,
 ( 4, 2, 2, 4 ),
 ( 1.301042606982605321E-18, 0.0004249208466734727776, 0.0008498416933469442542, 0.001699683386693887207 ),
 .UNSPECIFIED. ) ;
#7353=DIRECTION ( 'NONE',  ( 0.000000000000000000, 0.000000000000000000, 1.000000000000000000 ) ) ;
#7354=COLOUR_RGB ( '', 0.66274510, 0.83137255, 0.94901961) ;
#7355=FACE_OUTER_BOUND ( 'NONE', #49634, .T. ) ;
#7361=ADVANCED_FACE ( 'NONE', ( #36800 ), #16379, .T. ) ;
#7368=CYLINDRICAL_SURFACE ( 'NONE', #31160, 113.0000000000000284 ) ;
#7377=( BOUNDED_CURVE ( )  B_SPLINE_CURVE ( 3, ( #20532, #14933, #68374, #57832 ),
 .UNSPECIFIED., .F., .F. ) 
 B_SPLINE_CURVE_WITH_KNOTS ( ( 4, 4 ),
 ( 4.712388980384689674, 6.283185307179586232 ),
 .UNSPECIFIED. ) 
 CURVE ( )  GEOMETRIC_REPRESENTATION_ITEM ( )  RATIONAL_B_SPLINE_CURVE ( ( 1.000000000000000000, 0.8047378541243649375, 0.8047378541243649375, 1.000000000000000000 ) ) 
 REPRESENTATION_ITEM ( '' )  );
#7378=SURFACE_STYLE_FILL_AREA ( #2740 ) ;
#7388=EDGE_CURVE ( 'NONE', #67224, #23974, #26852, .T. ) ;
#7389=( NAMED_UNIT ( * ) SI_UNIT ( $, .STERADIAN. ) SOLID_ANGLE_UNIT ( ) );
#7395=EDGE_LOOP ( 'NONE', ( #1992, #5668, #21505, #62412 ) ) ;
#7396=EDGE_CURVE ( 'NONE', #65503, #62949, #6131, .T. ) ;
#7400=( LENGTH_UNIT ( ) NAMED_UNIT ( * ) SI_UNIT ( .MILLI., .METRE. ) );
#7413=LINE ( 'NONE', #23569, #50909 ) ;
#7415=DIRECTION ( 'NONE',  ( -0.000000000000000000, -1.000000000000000000, 0.000000000000000000 ) ) ;
#7429=SURFACE_STYLE_FILL_AREA ( #12678 ) ;
#7432=SURFACE_STYLE_USAGE ( .BOTH. , #28503 ) ;
#7439=UNCERTAINTY_MEASURE_WITH_UNIT (LENGTH_MEASURE( 1.000000000000000082E-05 ), #17248, 'distance_accuracy_value', 'NONE');
#7443=VERTEX_POINT ( 'NONE', #51138 ) ;
#7444=SURFACE_STYLE_USAGE ( .BOTH. , #23268 ) ;
#7453=CARTESIAN_POINT ( 'NONE',  ( 1.709458476932651091E-14, 43.00000000000000000, 35.50000000000000000 ) ) ;
#7469=EDGE_CURVE ( 'NONE', #34188, #24855, #61317, .T. ) ;
#7470=( NAMED_UNIT ( * ) PLANE_ANGLE_UNIT ( ) SI_UNIT ( $, .RADIAN. ) );
#7476=( LENGTH_UNIT ( ) NAMED_UNIT ( * ) SI_UNIT ( .MILLI., .METRE. ) );
#7502=PLANE ( 'NONE',  #41022 ) ;
#7508=ORIENTED_EDGE ( 'NONE', *, *, #56153, .T. ) ;
#7512=EDGE_LOOP ( 'NONE', ( #39055, #59637 ) ) ;
#7534=DIRECTION ( 'NONE',  ( -0.000000000000000000, -0.000000000000000000, -1.000000000000000000 ) ) ;
#7548=CARTESIAN_POINT ( 'NONE',  ( 10.00000000000000533, 50.00000000000000000, -46.00000000000000000 ) ) ;
#7554=AXIS2_PLACEMENT_3D ( 'NONE', #689, #37766, #4022 ) ;
#7565=CYLINDRICAL_SURFACE ( 'NONE', #19107, 4.999999999999997335 ) ;
#7571=DIRECTION ( 'NONE',  ( 0.000000000000000000, 1.000000000000000000, 0.000000000000000000 ) ) ;
#7582=DIRECTION ( 'NONE',  ( -1.000000000000000000, -0.000000000000000000, 1.300977106640434891E-16 ) ) ;
#7591=ORIENTED_EDGE ( 'NONE', *, *, #96, .F. ) ;
#7593=FILL_AREA_STYLE ('',( #13207 ) ) ;
#7606=ORIENTED_EDGE ( 'NONE', *, *, #45146, .T. ) ;
#7614=DIRECTION ( 'NONE',  ( -0.000000000000000000, 0.3420201433256629953, 0.9396926207859104263 ) ) ;
#7625=FILL_AREA_STYLE ('',( #13954 ) ) ;
#7626=AXIS2_PLACEMENT_3D ( 'NONE', #27562, #17061, #11400 ) ;
#7647=ORIENTED_EDGE ( 'NONE', *, *, #32560, .F. ) ;
#7650=ORIENTED_EDGE ( 'NONE', *, *, #65995, .F. ) ;
#7653=EDGE_LOOP ( 'NONE', ( #56692, #42268, #19459, #45343 ) ) ;
#7660=( GEOMETRIC_REPRESENTATION_CONTEXT ( 3 ) GLOBAL_UNCERTAINTY_ASSIGNED_CONTEXT ( ( #14262 ) ) GLOBAL_UNIT_ASSIGNED_CONTEXT ( ( #2712, #24203, #45711 ) ) REPRESENTATION_CONTEXT ( 'NONE', 'WORKASPACE' ) );
#7670=AXIS2_PLACEMENT_3D ( 'NONE', #30024, #50125, #44864 ) ;
#7672=ORIENTED_EDGE ( 'NONE', *, *, #10669, .F. ) ;
#7680=SURFACE_SIDE_STYLE ('',( #55169 ) ) ;
#7684=EDGE_CURVE ( 'NONE', #4847, #31418, #37621, .T. ) ;
#7699=FILL_AREA_STYLE ('',( #29509 ) ) ;
#7702=CARTESIAN_POINT ( 'NONE',  ( 23.50000000000001776, 42.00000000000000000, 29.68999999999999417 ) ) ;
#7709=FILL_AREA_STYLE ('',( #40113 ) ) ;
#7721=CYLINDRICAL_SURFACE ( 'NONE', #33690, 1.000000000000000888 ) ;
#7727=FILL_AREA_STYLE_COLOUR ( '', #11134 ) ;
#7728=COLOUR_RGB ( '', 0.31764706, 0.68627451, 0.89019608) ;
#7729=FILL_AREA_STYLE_COLOUR ( '', #15721 ) ;
#7731=ORIENTED_EDGE ( 'NONE', *, *, #37471, .F. ) ;
#7737=AXIS2_PLACEMENT_3D ( 'NONE', #24473, #51576, #30801 ) ;
#7745=CARTESIAN_POINT ( 'NONE',  ( 0.000000000000000000, 42.00000000000000000, 75.00000000000001421 ) ) ;
#7763=VERTEX_POINT ( 'NONE', #66078 ) ;
#7770=AXIS2_PLACEMENT_3D ( 'NONE', #11801, #54700, #44212 ) ;
#7772=COLOUR_RGB ( '', 0.66274510, 0.83137255, 0.94901961) ;
#7780=CARTESIAN_POINT ( 'NONE',  ( 32.00000000000000711, 42.00000000000000000, -35.50000000000000000 ) ) ;
#7785=SURFACE_STYLE_FILL_AREA ( #28537 ) ;
#7789=VECTOR ( 'NONE', #41582, 1000.000000000000000 ) ;
#7799=( LENGTH_UNIT ( ) NAMED_UNIT ( * ) SI_UNIT ( .MILLI., .METRE. ) );
#7807=FILL_AREA_STYLE ('',( #50389 ) ) ;
#7809=CIRCLE ( 'NONE', #61717, 3.499999999999999556 ) ;
#7811=ORIENTED_EDGE ( 'NONE', *, *, #32189, .F. ) ;
#7826=ORIENTED_EDGE ( 'NONE', *, *, #44143, .T. ) ;
#7829=COLOUR_RGB ( '', 0.09019608, 0.27058824, 0.51372549) ;
#7835=CARTESIAN_POINT ( 'NONE',  ( 23.50000000000001776, 43.00000000000000000, -29.68999999999999417 ) ) ;
#7847=EDGE_LOOP ( 'NONE', ( #69084, #66413, #13279 ) ) ;
#7850=TOROIDAL_SURFACE ( 'NONE', #26903, 18.99999999999998934, 1.000000000000000000 ) ;
#7855=FILL_AREA_STYLE ('',( #13134 ) ) ;
#7875=DIRECTION ( 'NONE',  ( -0.000000000000000000, -1.000000000000000000, -0.000000000000000000 ) ) ;
#7891=FILL_AREA_STYLE_COLOUR ( '', #54826 ) ;
#7894=( NAMED_UNIT ( * ) SI_UNIT ( $, .STERADIAN. ) SOLID_ANGLE_UNIT ( ) );
#7912=( NAMED_UNIT ( * ) SI_UNIT ( $, .STERADIAN. ) SOLID_ANGLE_UNIT ( ) );
#7913=( NAMED_UNIT ( * ) PLANE_ANGLE_UNIT ( ) SI_UNIT ( $, .RADIAN. ) );
#7927=LINE ( 'NONE', #35372, #9637 ) ;
#7932=EDGE_CURVE ( 'NONE', #50329, #69192, #30164, .T. ) ;
#7939=LINE ( 'NONE', #49827, #61356 ) ;
#7940=SURFACE_STYLE_USAGE ( .BOTH. , #56116 ) ;
#7952=DIRECTION ( 'NONE',  ( 0.000000000000000000, 0.000000000000000000, 1.000000000000000000 ) ) ;
#7955=EDGE_CURVE ( 'NONE', #57229, #9516, #54471, .T. ) ;
#7959=CARTESIAN_POINT ( 'NONE',  ( 25.00000000000001421, 42.00000000000000000, -34.49999999999999289 ) ) ;
#7960=ADVANCED_FACE ( 'NONE', ( #21349 ), #16121, .F. ) ;
#7963=ORIENTED_EDGE ( 'NONE', *, *, #67861, .F. ) ;
#7966=STYLED_ITEM ( 'NONE', ( #60398 ), #13842 ) ;
#7977=LINE ( 'NONE', #30809, #12085 ) ;
#7986=VECTOR ( 'NONE', #19623, 1000.000000000000000 ) ;
#7993=( NAMED_UNIT ( * ) PLANE_ANGLE_UNIT ( ) SI_UNIT ( $, .RADIAN. ) );
#7997=ORIENTED_EDGE ( 'NONE', *, *, #55595, .T. ) ;
#8001=PLANE ( 'NONE',  #57730 ) ;
#8027=FILL_AREA_STYLE_COLOUR ( '', #31749 ) ;
#8028=SURFACE_STYLE_USAGE ( .BOTH. , #40762 ) ;
#8029=EDGE_LOOP ( 'NONE', ( #4664, #41570, #25015, #39109 ) ) ;
#8031=CARTESIAN_POINT ( 'NONE',  ( 1.000000000000000000, 0.9999999999999991118, 79.00402776293826435 ) ) ;
#8032=EDGE_CURVE ( 'NONE', #69517, #65703, #47823, .T. ) ;
#8034=( NAMED_UNIT ( * ) SI_UNIT ( $, .STERADIAN. ) SOLID_ANGLE_UNIT ( ) );
#8042=CIRCLE ( 'NONE', #57505, 1.000000000000000888 ) ;
#8052=DIRECTION ( 'NONE',  ( -0.000000000000000000, -1.000000000000000000, -0.000000000000000000 ) ) ;
#8056=CIRCLE ( 'NONE', #10332, 12.50000000000000178 ) ;
#8059=VERTEX_POINT ( 'NONE', #61681 ) ;
#8072=CYLINDRICAL_SURFACE ( 'NONE', #16252, 16.00000000000000000 ) ;
#8076=UNCERTAINTY_MEASURE_WITH_UNIT (LENGTH_MEASURE( 1.000000000000000082E-05 ), #65736, 'distance_accuracy_value', 'NONE');
#8081=VERTEX_POINT ( 'NONE', #19127 ) ;
#8084=DIRECTION ( 'NONE',  ( 0.000000000000000000, 0.000000000000000000, -1.000000000000000000 ) ) ;
#8099=VERTEX_POINT ( 'NONE', #40630 ) ;
#8106=EDGE_LOOP ( 'NONE', ( #60871, #8304, #65910, #12780 ) ) ;
#8112=DIRECTION ( 'NONE',  ( -0.000000000000000000, -1.000000000000000000, 0.000000000000000000 ) ) ;
#8114=FACE_OUTER_BOUND ( 'NONE', #68280, .T. ) ;
#8119=VECTOR ( 'NONE', #39428, 1000.000000000000000 ) ;
#8122=ORIENTED_EDGE ( 'NONE', *, *, #34896, .F. ) ;
#8127=ADVANCED_FACE ( 'NONE', ( #30365 ), #46632, .F. ) ;
#8136=DIRECTION ( 'NONE',  ( -0.000000000000000000, -1.000000000000000000, -0.000000000000000000 ) ) ;
#8140=( LENGTH_UNIT ( ) NAMED_UNIT ( * ) SI_UNIT ( .MILLI., .METRE. ) );
#8141=UNCERTAINTY_MEASURE_WITH_UNIT (LENGTH_MEASURE( 1.000000000000000082E-05 ), #54065, 'distance_accuracy_value', 'NONE');
#8149=VERTEX_POINT ( 'NONE', #41328 ) ;
#8151=DIRECTION ( 'NONE',  ( 1.000000000000000000, 0.000000000000000000, -1.300977106640435384E-16 ) ) ;
#8156=SURFACE_STYLE_USAGE ( .BOTH. , #50037 ) ;
#8161=CARTESIAN_POINT ( 'NONE',  ( 10.00000000000002309, 43.00000000000000000, 90.00000000000000000 ) ) ;
#8162=CIRCLE ( 'NONE', #22715, 5.000000000000004441 ) ;
#8167=FACE_OUTER_BOUND ( 'NONE', #36640, .T. ) ;
#8172=STYLED_ITEM ( 'NONE', ( #69299 ), #46275 ) ;
#8179=FILL_AREA_STYLE_COLOUR ( '', #37280 ) ;
#8187=DIRECTION ( 'NONE',  ( -0.000000000000000000, -0.6691306063588591257, -0.7431448254773933559 ) ) ;
#8191=EDGE_CURVE ( 'NONE', #36332, #49909, #23876, .T. ) ;
#8212=EDGE_CURVE ( 'NONE', #582, #15864, #56758, .T. ) ;
#8219=ORIENTED_EDGE ( 'NONE', *, *, #49110, .F. ) ;
#8232=ORIENTED_EDGE ( 'NONE', *, *, #27291, .T. ) ;
#8246=DIRECTION ( 'NONE',  ( 0.000000000000000000, 0.000000000000000000, 1.000000000000000000 ) ) ;
#8259=CARTESIAN_POINT ( 'NONE',  ( 28.00000000000000000, 38.70020753820971748, -89.00000000000000000 ) ) ;
#8267=LINE ( 'NONE', #8611, #67190 ) ;
#8277=FILL_AREA_STYLE ('',( #36434 ) ) ;
#8282=CARTESIAN_POINT ( 'NONE',  ( 36.00000000000002842, 0.000000000000000000, 29.00402776293825724 ) ) ;
#8288=( GEOMETRIC_REPRESENTATION_CONTEXT ( 3 ) GLOBAL_UNCERTAINTY_ASSIGNED_CONTEXT ( ( #6672 ) ) GLOBAL_UNIT_ASSIGNED_CONTEXT ( ( #60024, #12166, #6907 ) ) REPRESENTATION_CONTEXT ( 'NONE', 'WORKASPACE' ) );
#8292=DIRECTION ( 'NONE',  ( 1.000000000000000000, 0.000000000000000000, 0.000000000000000000 ) ) ;
#8293=ORIENTED_EDGE ( 'NONE', *, *, #9003, .T. ) ;
#8304=ORIENTED_EDGE ( 'NONE', *, *, #46454, .F. ) ;
#8306=MECHANICAL_DESIGN_GEOMETRIC_PRESENTATION_REPRESENTATION('',(#25114),#50978);
#8307=CYLINDRICAL_SURFACE ( 'NONE', #23266, 0.9999999999999997780 ) ;
#8308=PRESENTATION_STYLE_ASSIGNMENT (( #57521 ) ) ;
#8328=LINE ( 'NONE', #23791, #65433 ) ;
#8339=FILL_AREA_STYLE ('',( #62124 ) ) ;
#8350=AXIS2_PLACEMENT_3D ( 'NONE', #3933, #36361, #4262 ) ;
#8352=CIRCLE ( 'NONE', #37573, 1.000000000000000888 ) ;
#8363=DIRECTION ( 'NONE',  ( 0.000000000000000000, 1.000000000000000000, 0.000000000000000000 ) ) ;
#8366=ORIENTED_EDGE ( 'NONE', *, *, #43143, .T. ) ;
#8372=EDGE_LOOP ( 'NONE', ( #38710, #60409, #9449, #65594 ) ) ;
#8381=FILL_AREA_STYLE_COLOUR ( '', #15985 ) ;
#8385=( NAMED_UNIT ( * ) PLANE_ANGLE_UNIT ( ) SI_UNIT ( $, .RADIAN. ) );
#8386=CARTESIAN_POINT ( 'NONE',  ( 24.58159228739605950, 26.69105118024819490, -27.43537399302963919 ) ) ;
#8389=ORIENTED_EDGE ( 'NONE', *, *, #19312, .F. ) ;
#8396=SURFACE_SIDE_STYLE ('',( #35113 ) ) ;
#8397=DIRECTION ( 'NONE',  ( -8.673617379884040402E-17, 0.000000000000000000, -1.000000000000000000 ) ) ;
#8417=FILL_AREA_STYLE_COLOUR ( '', #38127 ) ;
#8424=ORIENTED_EDGE ( 'NONE', *, *, #37926, .F. ) ;
#8425=DIRECTION ( 'NONE',  ( 0.000000000000000000, 0.000000000000000000, 1.000000000000000000 ) ) ;
#8442=ADVANCED_FACE ( 'NONE', ( #11856 ), #11847, .T. ) ;
#8456=STYLED_ITEM ( 'NONE', ( #68053 ), #8127 ) ;
#8464=ORIENTED_EDGE ( 'NONE', *, *, #2193, .T. ) ;
#8468=CARTESIAN_POINT ( 'NONE',  ( 7.999999999999992895, 5.000000000000000000, -24.00402776293826079 ) ) ;
#8472=VECTOR ( 'NONE', #26625, 1000.000000000000000 ) ;
#8487=ORIENTED_EDGE ( 'NONE', *, *, #33430, .T. ) ;
#8495=ORIENTED_EDGE ( 'NONE', *, *, #28312, .T. ) ;
#8497=AXIS2_PLACEMENT_3D ( 'NONE', #34828, #8112, #47172 ) ;
#8502=ORIENTED_EDGE ( 'NONE', *, *, #51407, .T. ) ;
#8510=SURFACE_STYLE_FILL_AREA ( #3885 ) ;
#8511=VERTEX_POINT ( 'NONE', #50884 ) ;
#8514=CARTESIAN_POINT ( 'NONE',  ( 22.99999999999995026, 5.000000000000000000, -32.00402776293824303 ) ) ;
#8521=PRESENTATION_STYLE_ASSIGNMENT (( #19031 ) ) ;
#8523=ADVANCED_FACE ( 'NONE', ( #13578 ), #33250, .T. ) ;
#8539=ADVANCED_FACE ( 'NONE', ( #68116 ), #19192, .F. ) ;
#8543=PRESENTATION_STYLE_ASSIGNMENT (( #39525 ) ) ;
#8544=ORIENTED_EDGE ( 'NONE', *, *, #29228, .T. ) ;
#8549=FILL_AREA_STYLE_COLOUR ( '', #25289 ) ;
#8551=( GEOMETRIC_REPRESENTATION_CONTEXT ( 3 ) GLOBAL_UNCERTAINTY_ASSIGNED_CONTEXT ( ( #19365 ) ) GLOBAL_UNIT_ASSIGNED_CONTEXT ( ( #36821, #20247, #9017 ) ) REPRESENTATION_CONTEXT ( 'NONE', 'WORKASPACE' ) );
#8552=ORIENTED_EDGE ( 'NONE', *, *, #50765, .F. ) ;
#8560=DIRECTION ( 'NONE',  ( -0.000000000000000000, 1.000000000000000000, -0.000000000000000000 ) ) ;
#8565=EDGE_LOOP ( 'NONE', ( #31997, #16219, #50175, #43650 ) ) ;
#8570=( LENGTH_UNIT ( ) NAMED_UNIT ( * ) SI_UNIT ( .MILLI., .METRE. ) );
#8572=DIRECTION ( 'NONE',  ( 0.000000000000000000, 0.000000000000000000, 1.000000000000000000 ) ) ;
#8578=FILL_AREA_STYLE_COLOUR ( '', #37104 ) ;
#8580=ORIENTED_EDGE ( 'NONE', *, *, #45856, .T. ) ;
#8589=EDGE_CURVE ( 'NONE', #65035, #11349, #41752, .T. ) ;
#8601=DIRECTION ( 'NONE',  ( 1.000000000000000000, 0.000000000000000000, 0.000000000000000000 ) ) ;
#8603=CARTESIAN_POINT ( 'NONE',  ( 2.999999999999996447, 5.000000000000000000, -37.00402776293829277 ) ) ;
#8607=TOROIDAL_SURFACE ( 'NONE', #26556, 2.000000000000000000, 1.000000000000000000 ) ;
#8608=VECTOR ( 'NONE', #33034, 1000.000000000000000 ) ;
#8611=CARTESIAN_POINT ( 'NONE',  ( 98.00000000000000000, 0.000000000000000000, -5.000000000000004441 ) ) ;
#8620=CIRCLE ( 'NONE', #13076, 5.000000000000004441 ) ;
#8624=ORIENTED_EDGE ( 'NONE', *, *, #27852, .F. ) ;
#8626=EDGE_CURVE ( 'NONE', #5418, #17013, #5785, .T. ) ;
#8634=CIRCLE ( 'NONE', #48007, 4.999999999999997335 ) ;
#8635=( NAMED_UNIT ( * ) PLANE_ANGLE_UNIT ( ) SI_UNIT ( $, .RADIAN. ) );
#8636=VERTEX_POINT ( 'NONE', #37880 ) ;
#8637=CYLINDRICAL_SURFACE ( 'NONE', #56814, 3.499999999999999556 ) ;
#8646=UNCERTAINTY_MEASURE_WITH_UNIT (LENGTH_MEASURE( 1.000000000000000082E-05 ), #26456, 'distance_accuracy_value', 'NONE');
#8651=CARTESIAN_POINT ( 'NONE',  ( 179.4361977533490631, 0.000000000000000000, -103.7004518695262192 ) ) ;
#8654=ORIENTED_EDGE ( 'NONE', *, *, #11928, .F. ) ;
#8655=CIRCLE ( 'NONE', #65943, 5.000000000000004441 ) ;
#8656=FILL_AREA_STYLE ('',( #63502 ) ) ;
#8671=PRESENTATION_STYLE_ASSIGNMENT (( #30796 ) ) ;
#8691=DIRECTION ( 'NONE',  ( 1.000000000000000000, -0.000000000000000000, 0.000000000000000000 ) ) ;
#8698=DIRECTION ( 'NONE',  ( -1.000000000000000000, 0.000000000000000000, 0.000000000000000000 ) ) ;
#8706=CARTESIAN_POINT ( 'NONE',  ( 23.00000000000000000, 5.000000000000000000, -24.00402776293825013 ) ) ;
#8708=ORIENTED_EDGE ( 'NONE', *, *, #29458, .T. ) ;
#8714=SURFACE_SIDE_STYLE ('',( #19606 ) ) ;
#8717=DIRECTION ( 'NONE',  ( 0.000000000000000000, 1.000000000000000000, 0.000000000000000000 ) ) ;
#8723=PRESENTATION_STYLE_ASSIGNMENT (( #14004 ) ) ;
#8724=FILL_AREA_STYLE ('',( #8027 ) ) ;
#8746=LINE ( 'NONE', #67138, #26643 ) ;
#8751=CARTESIAN_POINT ( 'NONE',  ( 6.000000000000017764, 26.00000000000000355, 20.49999999999999645 ) ) ;
#8753=VECTOR ( 'NONE', #5450, 1000.000000000000000 ) ;
#8754=ADVANCED_FACE ( 'NONE', ( #35231 ), #56691, .T. ) ;
#8757=ORIENTED_EDGE ( 'NONE', *, *, #7396, .F. ) ;
#8766=EDGE_CURVE ( 'NONE', #51395, #11136, #40051, .T. ) ;
#8771=FILL_AREA_STYLE ('',( #52401 ) ) ;
#8776=ORIENTED_EDGE ( 'NONE', *, *, #61250, .T. ) ;
#8779=FILL_AREA_STYLE ('',( #57305 ) ) ;
#8781=FACE_OUTER_BOUND ( 'NONE', #51788, .T. ) ;
#8784=CARTESIAN_POINT ( 'NONE',  ( 31.00000000000000000, 42.00000000000000000, -75.00000000000001421 ) ) ;
#8787=LINE ( 'NONE', #30215, #54261 ) ;
#8814=CARTESIAN_POINT ( 'NONE',  ( 28.00000000000002132, 34.36176364315826248, 80.00402776293826435 ) ) ;
#8841=DIRECTION ( 'NONE',  ( 0.000000000000000000, 0.000000000000000000, -1.000000000000000000 ) ) ;
#8848=PRESENTATION_STYLE_ASSIGNMENT (( #57030 ) ) ;
#8855=UNCERTAINTY_MEASURE_WITH_UNIT (LENGTH_MEASURE( 1.000000000000000082E-05 ), #29747, 'distance_accuracy_value', 'NONE');
#8861=MECHANICAL_DESIGN_GEOMETRIC_PRESENTATION_REPRESENTATION('',(#69505),#62761);
#8862=CARTESIAN_POINT ( 'NONE',  ( 98.00000000000000000, 0.000000000000000000, 5.000000000000004441 ) ) ;
#8863=DIRECTION ( 'NONE',  ( -0.000000000000000000, -1.000000000000000000, 0.000000000000000000 ) ) ;
#8864=VERTEX_POINT ( 'NONE', #56265 ) ;
#8876=DIRECTION ( 'NONE',  ( 1.000000000000000000, 0.000000000000000000, 0.000000000000000000 ) ) ;
#8880=PRESENTATION_STYLE_ASSIGNMENT (( #29982 ) ) ;
#8888=ORIENTED_EDGE ( 'NONE', *, *, #40004, .T. ) ;
#8909=CARTESIAN_POINT ( 'NONE',  ( 10.00000000000002132, 50.00000000000000000, 55.00000000000000711 ) ) ;
#8923=ADVANCED_FACE ( 'NONE', ( #18655 ), #16081, .T. ) ;
#8938=AXIS2_PLACEMENT_3D ( 'NONE', #52245, #15316, #14238 ) ;
#8942=AXIS2_PLACEMENT_3D ( 'NONE', #37125, #55, #58189 ) ;
#8944=CIRCLE ( 'NONE', #26873, 24.00000000000001421 ) ;
#8955=COLOUR_RGB ( '', 0.31764706, 0.68627451, 0.89019608) ;
#8956=SURFACE_STYLE_FILL_AREA ( #67012 ) ;
#8960=DIRECTION ( 'NONE',  ( 0.000000000000000000, 1.000000000000000000, 0.000000000000000000 ) ) ;
#8965=LINE ( 'NONE', #14241, #51609 ) ;
#8969=COLOUR_RGB ( '', 0.31764706, 0.68627451, 0.89019608) ;
#8974=AXIS2_PLACEMENT_3D ( 'NONE', #68644, #63356, #61957 ) ;
#9000=ORIENTED_EDGE ( 'NONE', *, *, #43442, .T. ) ;
#9003=EDGE_CURVE ( 'NONE', #35982, #21029, #49828, .T. ) ;
#9004=PRESENTATION_STYLE_ASSIGNMENT (( #4041 ) ) ;
#9005=LINE ( 'NONE', #68801, #42071 ) ;
#9013=ORIENTED_EDGE ( 'NONE', *, *, #17969, .F. ) ;
#9017=( NAMED_UNIT ( * ) SI_UNIT ( $, .STERADIAN. ) SOLID_ANGLE_UNIT ( ) );
#9026=SURFACE_SIDE_STYLE ('',( #9384 ) ) ;
#9036=FILL_AREA_STYLE ('',( #35065 ) ) ;
#9041=VECTOR ( 'NONE', #36511, 1000.000000000000000 ) ;
#9045=MECHANICAL_DESIGN_GEOMETRIC_PRESENTATION_REPRESENTATION('',(#57347),#15795);
#9049=AXIS2_PLACEMENT_3D ( 'NONE', #562, #44282, #23810 ) ;
#9054=SURFACE_STYLE_FILL_AREA ( #10446 ) ;
#9057=ADVANCED_FACE ( 'NONE', ( #55764 ), #45244, .F. ) ;
#9062=EDGE_CURVE ( 'NONE', #23486, #60366, #17467, .T. ) ;
#9064=EDGE_CURVE ( 'NONE', #47623, #62580, #66669, .T. ) ;
#9068=ADVANCED_FACE ( 'NONE', ( #38596 ), #66307, .F. ) ;
#9075=STYLED_ITEM ( 'NONE', ( #10621 ), #45224 ) ;
#9076=STYLED_ITEM ( 'NONE', ( #8848 ), #12013 ) ;
#9081=EDGE_CURVE ( 'NONE', #17236, #30128, #11653, .T. ) ;
#9084=AXIS2_PLACEMENT_3D ( 'NONE', #5381, #53271, #5058 ) ;
#9086=ORIENTED_EDGE ( 'NONE', *, *, #39046, .T. ) ;
#9093=COLOUR_RGB ( '', 0.08235294, 0.09019608, 0.10196078) ;
#9096=( GEOMETRIC_REPRESENTATION_CONTEXT ( 3 ) GLOBAL_UNCERTAINTY_ASSIGNED_CONTEXT ( ( #67245 ) ) GLOBAL_UNIT_ASSIGNED_CONTEXT ( ( #26996, #7993, #1266 ) ) REPRESENTATION_CONTEXT ( 'NONE', 'WORKASPACE' ) );
#9102=SURFACE_SIDE_STYLE ('',( #41135 ) ) ;
#9108=EDGE_CURVE ( 'NONE', #46872, #60023, #15051, .T. ) ;
#9112=EDGE_CURVE ( 'NONE', #60430, #48506, #20645, .T. ) ;
#9121=FACE_OUTER_BOUND ( 'NONE', #54914, .T. ) ;
#9139=CIRCLE ( 'NONE', #28171, 2.000000000000001776 ) ;
#9144=( GEOMETRIC_REPRESENTATION_CONTEXT ( 3 ) GLOBAL_UNCERTAINTY_ASSIGNED_CONTEXT ( ( #56657 ) ) GLOBAL_UNIT_ASSIGNED_CONTEXT ( ( #59207, #1812, #17726 ) ) REPRESENTATION_CONTEXT ( 'NONE', 'WORKASPACE' ) );
#9152=FACE_OUTER_BOUND ( 'NONE', #67030, .T. ) ;
#9160=DIRECTION ( 'NONE',  ( 1.000000000000000000, -0.000000000000000000, -0.000000000000000000 ) ) ;
#9163=MECHANICAL_DESIGN_GEOMETRIC_PRESENTATION_REPRESENTATION('',(#60781),#9212);
#9195=CARTESIAN_POINT ( 'NONE',  ( 23.41056558150575029, 24.55989583710066526, 27.18999999999999417 ) ) ;
#9199=EDGE_LOOP ( 'NONE', ( #21905, #37331, #49742, #16027 ) ) ;
#9205=SURFACE_STYLE_USAGE ( .BOTH. , #67588 ) ;
#9212=( GEOMETRIC_REPRESENTATION_CONTEXT ( 3 ) GLOBAL_UNCERTAINTY_ASSIGNED_CONTEXT ( ( #25720 ) ) GLOBAL_UNIT_ASSIGNED_CONTEXT ( ( #7268, #23778, #12876 ) ) REPRESENTATION_CONTEXT ( 'NONE', 'WORKASPACE' ) );
#9215=CIRCLE ( 'NONE', #66492, 1.000000000000000888 ) ;
#9217=VERTEX_POINT ( 'NONE', #31092 ) ;
#9229=COLOUR_RGB ( '', 0.08235294, 0.09019608, 0.10196078) ;
#9230=LINE ( 'NONE', #32058, #6871 ) ;
#9238=ORIENTED_EDGE ( 'NONE', *, *, #58093, .T. ) ;
#9242=ORIENTED_EDGE ( 'NONE', *, *, #36972, .T. ) ;
#9253=EDGE_CURVE ( 'NONE', #417, #20026, #8965, .T. ) ;
#9270=ORIENTED_EDGE ( 'NONE', *, *, #9407, .T. ) ;
#9273=SURFACE_STYLE_USAGE ( .BOTH. , #36003 ) ;
#9279=STYLED_ITEM ( 'NONE', ( #7317 ), #60805 ) ;
#9282=CIRCLE ( 'NONE', #3596, 4.999999999999997335 ) ;
#9284=VERTEX_POINT ( 'NONE', #46289 ) ;
#9288=FACE_OUTER_BOUND ( 'NONE', #19603, .T. ) ;
#9298=EDGE_LOOP ( 'NONE', ( #8122, #9950, #16360, #45151, #21143, #17735, #40212 ) ) ;
#9303=CIRCLE ( 'NONE', #57589, 5.000000000000000888 ) ;
#9307=EDGE_CURVE ( 'NONE', #35954, #20328, #67708, .T. ) ;
#9308=CARTESIAN_POINT ( 'NONE',  ( 23.50000000000001776, 42.00000000000000000, -29.68999999999999417 ) ) ;
#9314=EDGE_CURVE ( 'NONE', #56811, #52016, #22383, .T. ) ;
#9324=DIRECTION ( 'NONE',  ( 0.000000000000000000, -0.000000000000000000, 1.000000000000000000 ) ) ;
#9328=CIRCLE ( 'NONE', #39668, 12.50000000000001066 ) ;
#9331=ADVANCED_FACE ( 'NONE', ( #48033 ), #59200, .F. ) ;
#9366=STYLED_ITEM ( 'NONE', ( #11600 ), #26213 ) ;
#9368=ORIENTED_EDGE ( 'NONE', *, *, #2328, .F. ) ;
#9381=ORIENTED_EDGE ( 'NONE', *, *, #62291, .F. ) ;
#9383=STYLED_ITEM ( 'NONE', ( #19805 ), #46912 ) ;
#9384=SURFACE_STYLE_FILL_AREA ( #8339 ) ;
#9385=CARTESIAN_POINT ( 'NONE',  ( 29.00000000000002842, 42.00000000000000000, 3.902931319921305165E-16 ) ) ;
#9386=UNCERTAINTY_MEASURE_WITH_UNIT (LENGTH_MEASURE( 1.000000000000000082E-05 ), #69509, 'distance_accuracy_value', 'NONE');
#9388=CARTESIAN_POINT ( 'NONE',  ( 8.000000000000035527, 5.000000000000000000, -77.00402776293825013 ) ) ;
#9390=EDGE_CURVE ( 'NONE', #48634, #4737, #5540, .T. ) ;
#9392=AXIS2_PLACEMENT_3D ( 'NONE', #15637, #43450, #26500 ) ;
#9397=UNCERTAINTY_MEASURE_WITH_UNIT (LENGTH_MEASURE( 1.000000000000000082E-05 ), #40987, 'distance_accuracy_value', 'NONE');
#9399=CIRCLE ( 'NONE', #13898, 1.000000000000000888 ) ;
#9403=SURFACE_STYLE_USAGE ( .BOTH. , #24489 ) ;
#9406=CIRCLE ( 'NONE', #6017, 5.000000000000004441 ) ;
#9407=EDGE_CURVE ( 'NONE', #34574, #4197, #15684, .T. ) ;
#9415=CARTESIAN_POINT ( 'NONE',  ( 23.14573592869279750, 24.60297829105063983, -27.21022641015704835 ) ) ;
#9419=FILL_AREA_STYLE ('',( #57591 ) ) ;
#9430=ORIENTED_EDGE ( 'NONE', *, *, #64155, .F. ) ;
#9449=ORIENTED_EDGE ( 'NONE', *, *, #18282, .T. ) ;
#9454=ORIENTED_EDGE ( 'NONE', *, *, #62505, .T. ) ;
#9455=CARTESIAN_POINT ( 'NONE',  ( 3.414213562373125121, 42.99999999999999289, 90.00000000000001421 ) ) ;
#9458=( NAMED_UNIT ( * ) PLANE_ANGLE_UNIT ( ) SI_UNIT ( $, .RADIAN. ) );
#9470=( LENGTH_UNIT ( ) NAMED_UNIT ( * ) SI_UNIT ( .MILLI., .METRE. ) );
#9471=SURFACE_STYLE_USAGE ( .BOTH. , #40802 ) ;
#9473=ADVANCED_FACE ( 'NONE', ( #20907 ), #32147, .T. ) ;
#9486=DIRECTION ( 'NONE',  ( 0.000000000000000000, 0.9396926207859082059, 0.3420201433256693790 ) ) ;
#9492=STYLED_ITEM ( 'NONE', ( #23748 ), #38644 ) ;
#9493=FILL_AREA_STYLE_COLOUR ( '', #5587 ) ;
#9503=AXIS2_PLACEMENT_3D ( 'NONE', #40809, #34794, #45055 ) ;
#9506=CARTESIAN_POINT ( 'NONE',  ( 1.000000000000000000, 14.00000000000000000, -36.49999999999999289 ) ) ;
#9510=VECTOR ( 'NONE', #22905, 1000.000000000000000 ) ;
#9511=PRESENTATION_STYLE_ASSIGNMENT (( #44488 ) ) ;
#9516=VERTEX_POINT ( 'NONE', #44815 ) ;
#9518=FACE_OUTER_BOUND ( 'NONE', #61001, .T. ) ;
#9522=ORIENTED_EDGE ( 'NONE', *, *, #16085, .T. ) ;
#9539=MECHANICAL_DESIGN_GEOMETRIC_PRESENTATION_REPRESENTATION('',(#60063),#17372);
#9540=DIRECTION ( 'NONE',  ( -0.000000000000000000, -1.000000000000000000, -0.000000000000000000 ) ) ;
#9546=FILL_AREA_STYLE_COLOUR ( '', #27251 ) ;
#9552=VERTEX_POINT ( 'NONE', #49063 ) ;
#9567=PLANE ( 'NONE',  #64536 ) ;
#9568=DIRECTION ( 'NONE',  ( -2.168404344971007882E-16, 0.000000000000000000, -1.000000000000000000 ) ) ;
#9572=DIRECTION ( 'NONE',  ( 0.000000000000000000, -0.9396926207859082059, 0.3420201433256693790 ) ) ;
#9573=DIRECTION ( 'NONE',  ( -0.000000000000000000, -1.000000000000000000, -0.000000000000000000 ) ) ;
#9574=UNCERTAINTY_MEASURE_WITH_UNIT (LENGTH_MEASURE( 1.000000000000000082E-05 ), #20454, 'distance_accuracy_value', 'NONE');
#9576=DIRECTION ( 'NONE',  ( 1.000000000000000000, -0.000000000000000000, -1.300977106640434891E-16 ) ) ;
#9589=( GEOMETRIC_REPRESENTATION_CONTEXT ( 3 ) GLOBAL_UNCERTAINTY_ASSIGNED_CONTEXT ( ( #6731 ) ) GLOBAL_UNIT_ASSIGNED_CONTEXT ( ( #25907, #4436, #152 ) ) REPRESENTATION_CONTEXT ( 'NONE', 'WORKASPACE' ) );
#9591=UNCERTAINTY_MEASURE_WITH_UNIT (LENGTH_MEASURE( 1.000000000000000082E-05 ), #46047, 'distance_accuracy_value', 'NONE');
#9594=CARTESIAN_POINT ( 'NONE',  ( 109.0067032876572171, 0.9999999999999991118, 19.20378738324562917 ) ) ;
#9595=FILL_AREA_STYLE_COLOUR ( '', #56696 ) ;
#9604=CARTESIAN_POINT ( 'NONE',  ( 74.89452121010485541, 13.00000000000000178, -66.39042820928574429 ) ) ;
#9610=AXIS2_PLACEMENT_3D ( 'NONE', #14228, #20177, #30728 ) ;
#9623=VERTEX_POINT ( 'NONE', #20101 ) ;
#9625=CARTESIAN_POINT ( 'NONE',  ( 26.00000000000001776, 15.00000000000000000, -34.49999999999999289 ) ) ;
#9634=CARTESIAN_POINT ( 'NONE',  ( 0.000000000000000000, 14.00000000000000000, -80.00402776293826435 ) ) ;
#9637=VECTOR ( 'NONE', #18823, 1000.000000000000114 ) ;
#9651=( NAMED_UNIT ( * ) PLANE_ANGLE_UNIT ( ) SI_UNIT ( $, .RADIAN. ) );
#9660=DIRECTION ( 'NONE',  ( 0.000000000000000000, 0.000000000000000000, -1.000000000000000000 ) ) ;
#9661=EDGE_CURVE ( 'NONE', #51304, #67697, #25396, .T. ) ;
#9669=CARTESIAN_POINT ( 'NONE',  ( 2.000000000000009326, 50.00000000000000000, -54.99999999999998579 ) ) ;
#9673=( NAMED_UNIT ( * ) SI_UNIT ( $, .STERADIAN. ) SOLID_ANGLE_UNIT ( ) );
#9676=( NAMED_UNIT ( * ) PLANE_ANGLE_UNIT ( ) SI_UNIT ( $, .RADIAN. ) );
#9685=CIRCLE ( 'NONE', #56863, 1.000000000000000888 ) ;
#9686=CARTESIAN_POINT ( 'NONE',  ( 30.99999999999999289, 5.000000000000000000, 37.00402776293829277 ) ) ;
#9690=( NAMED_UNIT ( * ) PLANE_ANGLE_UNIT ( ) SI_UNIT ( $, .RADIAN. ) );
#9693=UNCERTAINTY_MEASURE_WITH_UNIT (LENGTH_MEASURE( 1.000000000000000082E-05 ), #15784, 'distance_accuracy_value', 'NONE');
#9694=CARTESIAN_POINT ( 'NONE',  ( 33.00000000000000711, 15.00000000000000000, -36.50000000000000000 ) ) ;
#9696=VECTOR ( 'NONE', #30846, 1000.000000000000000 ) ;
#9713=ORIENTED_EDGE ( 'NONE', *, *, #13027, .T. ) ;
#9721=AXIS2_PLACEMENT_3D ( 'NONE', #24647, #46165, #67589 ) ;
#9742=DIRECTION ( 'NONE',  ( -0.000000000000000000, -1.000000000000000000, -0.000000000000000000 ) ) ;
#9744=EDGE_CURVE ( 'NONE', #48456, #62990, #57774, .T. ) ;
#9757=VERTEX_POINT ( 'NONE', #4255 ) ;
#9758=ORIENTED_EDGE ( 'NONE', *, *, #23217, .T. ) ;
#9759=SURFACE_STYLE_USAGE ( .BOTH. , #63206 ) ;
#9760=EDGE_CURVE ( 'NONE', #13259, #65467, #20009, .T. ) ;
#9764=ORIENTED_EDGE ( 'NONE', *, *, #50203, .T. ) ;
#9765=ORIENTED_EDGE ( 'NONE', *, *, #10519, .T. ) ;
#9769=ORIENTED_EDGE ( 'NONE', *, *, #12980, .F. ) ;
#9781=CYLINDRICAL_SURFACE ( 'NONE', #34645, 1.000000000000000888 ) ;
#9788=ORIENTED_EDGE ( 'NONE', *, *, #5312, .T. ) ;
#9795=EDGE_CURVE ( 'NONE', #8081, #23178, #41976, .T. ) ;
#9800=ORIENTED_EDGE ( 'NONE', *, *, #24526, .T. ) ;
#9801=ORIENTED_EDGE ( 'NONE', *, *, #1245, .T. ) ;
#9803=DIRECTION ( 'NONE',  ( 1.000000000000000000, 0.000000000000000000, 0.000000000000000000 ) ) ;
#9810=CYLINDRICAL_SURFACE ( 'NONE', #10024, 1.000000000000000888 ) ;
#9815=SURFACE_STYLE_USAGE ( .BOTH. , #26974 ) ;
#9819=FACE_OUTER_BOUND ( 'NONE', #58061, .T. ) ;
#9820=CYLINDRICAL_SURFACE ( 'NONE', #21447, 3.499999999999999556 ) ;
#9832=CARTESIAN_POINT ( 'NONE',  ( 107.0858988931383493, 0.000000000000000000, 16.89933289725615850 ) ) ;
#9834=DIRECTION ( 'NONE',  ( 0.000000000000000000, 1.000000000000000000, -0.000000000000000000 ) ) ;
#9839=ADVANCED_FACE ( 'NONE', ( #15918 ), #43702, .T. ) ;
#9850=FILL_AREA_STYLE ('',( #10537 ) ) ;
#9855=VERTEX_POINT ( 'NONE', #42660 ) ;
#9857=( NAMED_UNIT ( * ) SI_UNIT ( $, .STERADIAN. ) SOLID_ANGLE_UNIT ( ) );
#9862=CARTESIAN_POINT ( 'NONE',  ( 3.000000000000002665, 34.36176364315826248, -80.00402776293826435 ) ) ;
#9891=DIRECTION ( 'NONE',  ( 0.000000000000000000, 0.000000000000000000, 1.000000000000000000 ) ) ;
#9894=FACE_OUTER_BOUND ( 'NONE', #60295, .T. ) ;
#9899=CARTESIAN_POINT ( 'NONE',  ( 0.000000000000000000, 14.00000000000000000, 36.50000000000000000 ) ) ;
#9917=CIRCLE ( 'NONE', #3099, 1.000000000000000888 ) ;
#9921=ORIENTED_EDGE ( 'NONE', *, *, #13332, .F. ) ;
#9926=CARTESIAN_POINT ( 'NONE',  ( 0.9999999999999991118, 50.00000000000000000, -60.00000000000000000 ) ) ;
#9928=SURFACE_SIDE_STYLE ('',( #4623 ) ) ;
#9932=DIRECTION ( 'NONE',  ( -0.000000000000000000, -1.000000000000000000, -0.000000000000000000 ) ) ;
#9934=( NAMED_UNIT ( * ) PLANE_ANGLE_UNIT ( ) SI_UNIT ( $, .RADIAN. ) );
#9937=ORIENTED_EDGE ( 'NONE', *, *, #38412, .T. ) ;
#9941=STYLED_ITEM ( 'NONE', ( #65426 ), #43504 ) ;
#9942=ORIENTED_EDGE ( 'NONE', *, *, #32512, .F. ) ;
#9944=EDGE_CURVE ( 'NONE', #66425, #59410, #49294, .T. ) ;
#9950=ORIENTED_EDGE ( 'NONE', *, *, #30726, .T. ) ;
#9951=PRESENTATION_STYLE_ASSIGNMENT (( #63409 ) ) ;
#9971=DIRECTION ( 'NONE',  ( 0.000000000000000000, 0.000000000000000000, 1.000000000000000000 ) ) ;
#9974=( LENGTH_UNIT ( ) NAMED_UNIT ( * ) SI_UNIT ( .MILLI., .METRE. ) );
#9981=LINE ( 'NONE', #49031, #31372 ) ;
#9987=EDGE_CURVE ( 'NONE', #51568, #39729, #6588, .T. ) ;
#9993=( NAMED_UNIT ( * ) PLANE_ANGLE_UNIT ( ) SI_UNIT ( $, .RADIAN. ) );
#9994=AXIS2_PLACEMENT_3D ( 'NONE', #34680, #44943, #33995 ) ;
#9995=( GEOMETRIC_REPRESENTATION_CONTEXT ( 3 ) GLOBAL_UNCERTAINTY_ASSIGNED_CONTEXT ( ( #9693 ) ) GLOBAL_UNIT_ASSIGNED_CONTEXT ( ( #15784, #52032, #42215 ) ) REPRESENTATION_CONTEXT ( 'NONE', 'WORKASPACE' ) );
#10005=PRESENTATION_STYLE_ASSIGNMENT (( #30050 ) ) ;
#10006=MECHANICAL_DESIGN_GEOMETRIC_PRESENTATION_REPRESENTATION('',(#67288),#12178);
#10010=( NAMED_UNIT ( * ) SI_UNIT ( $, .STERADIAN. ) SOLID_ANGLE_UNIT ( ) );
#10014=VERTEX_POINT ( 'NONE', #14081 ) ;
#10017=CARTESIAN_POINT ( 'NONE',  ( 31.00000000000000000, 42.00000000000000000, -79.00402776293826435 ) ) ;
#10020=CIRCLE ( 'NONE', #50480, 16.00000000000000711 ) ;
#10024=AXIS2_PLACEMENT_3D ( 'NONE', #36578, #67144, #30885 ) ;
#10028=DIRECTION ( 'NONE',  ( 0.000000000000000000, 0.000000000000000000, 1.000000000000000000 ) ) ;
#10036=PRESENTATION_STYLE_ASSIGNMENT (( #31112 ) ) ;
#10037=MECHANICAL_DESIGN_GEOMETRIC_PRESENTATION_REPRESENTATION('',(#40364),#41532);
#10038=VERTEX_POINT ( 'NONE', #18665 ) ;
#10041=AXIS2_PLACEMENT_3D ( 'NONE', #31482, #15360, #67751 ) ;
#10042=EDGE_CURVE ( 'NONE', #19928, #44275, #34672, .T. ) ;
#10053=VECTOR ( 'NONE', #13847, 1000.000000000000000 ) ;
#10068=ORIENTED_EDGE ( 'NONE', *, *, #62505, .F. ) ;
#10078=AXIS2_PLACEMENT_3D ( 'NONE', #58918, #4034, #41374 ) ;
#10079=CIRCLE ( 'NONE', #31393, 113.0000000000000284 ) ;
#10081=( LENGTH_UNIT ( ) NAMED_UNIT ( * ) SI_UNIT ( .MILLI., .METRE. ) );
#10082=MECHANICAL_DESIGN_GEOMETRIC_PRESENTATION_REPRESENTATION('',(#39326),#23567);
#10085=CARTESIAN_POINT ( 'NONE',  ( 82.09357085539566867, 0.000000000000000000, -32.00402776293823592 ) ) ;
#10088=STYLED_ITEM ( 'NONE', ( #67561 ), #20668 ) ;
#10092=FILL_AREA_STYLE ('',( #20282 ) ) ;
#10100=( LENGTH_UNIT ( ) NAMED_UNIT ( * ) SI_UNIT ( .MILLI., .METRE. ) );
#10103=DIRECTION ( 'NONE',  ( -3.717264591378879477E-17, 0.000000000000000000, 1.000000000000000000 ) ) ;
#10105=FACE_OUTER_BOUND ( 'NONE', #36903, .T. ) ;
#10110=ADVANCED_FACE ( 'NONE', ( #13365 ), #35544, .F. ) ;
#10111=MECHANICAL_DESIGN_GEOMETRIC_PRESENTATION_REPRESENTATION('',(#66224),#60586);
#10115=EDGE_LOOP ( 'NONE', ( #27710, #11208, #59055, #2986 ) ) ;
#10120=ORIENTED_EDGE ( 'NONE', *, *, #55610, .T. ) ;
#10123=MECHANICAL_DESIGN_GEOMETRIC_PRESENTATION_REPRESENTATION('',(#17947),#67397);
#10124=DIRECTION ( 'NONE',  ( 0.000000000000000000, 1.000000000000000000, -0.000000000000000000 ) ) ;
#10143=( GEOMETRIC_REPRESENTATION_CONTEXT ( 3 ) GLOBAL_UNCERTAINTY_ASSIGNED_CONTEXT ( ( #42080 ) ) GLOBAL_UNIT_ASSIGNED_CONTEXT ( ( #15470, #58343, #52058 ) ) REPRESENTATION_CONTEXT ( 'NONE', 'WORKASPACE' ) );
#10155=MECHANICAL_DESIGN_GEOMETRIC_PRESENTATION_REPRESENTATION('',(#65163),#34842);
#10160=DIRECTION ( 'NONE',  ( -0.000000000000000000, 1.000000000000000000, -0.000000000000000000 ) ) ;
#10165=SURFACE_STYLE_USAGE ( .BOTH. , #11531 ) ;
#10179=FILL_AREA_STYLE_COLOUR ( '', #13628 ) ;
#10188=ORIENTED_EDGE ( 'NONE', *, *, #2589, .T. ) ;
#10190=ADVANCED_FACE ( 'NONE', ( #52762 ), #31975, .F. ) ;
#10201=DIRECTION ( 'NONE',  ( -0.000000000000000000, -1.000000000000000000, -0.000000000000000000 ) ) ;
#10210=AXIS2_PLACEMENT_3D ( 'NONE', #33069, #69322, #44006 ) ;
#10217=( LENGTH_UNIT ( ) NAMED_UNIT ( * ) SI_UNIT ( .MILLI., .METRE. ) );
#10218=UNCERTAINTY_MEASURE_WITH_UNIT (LENGTH_MEASURE( 1.000000000000000082E-05 ), #37828, 'distance_accuracy_value', 'NONE');
#10222=FILL_AREA_STYLE ('',( #58398 ) ) ;
#10227=CARTESIAN_POINT ( 'NONE',  ( 23.14150002214069701, 27.39558012762189065, 27.21086609277890034 ) ) ;
#10251=CARTESIAN_POINT ( 'NONE',  ( 36.00000000000002842, 0.000000000000000000, -29.00402776293825724 ) ) ;
#10252=( GEOMETRIC_REPRESENTATION_CONTEXT ( 3 ) GLOBAL_UNCERTAINTY_ASSIGNED_CONTEXT ( ( #60199 ) ) GLOBAL_UNIT_ASSIGNED_CONTEXT ( ( #57140, #9690, #36785 ) ) REPRESENTATION_CONTEXT ( 'NONE', 'WORKASPACE' ) );
#10263=STYLED_ITEM ( 'NONE', ( #64262 ), #18116 ) ;
#10266=AXIS2_PLACEMENT_3D ( 'NONE', #22271, #49710, #33851 ) ;
#10276=DIRECTION ( 'NONE',  ( -0.000000000000000000, -1.000000000000000000, -0.000000000000000000 ) ) ;
#10281=DIRECTION ( 'NONE',  ( -0.000000000000000000, -1.000000000000000000, -0.000000000000000000 ) ) ;
#10285=ORIENTED_EDGE ( 'NONE', *, *, #52459, .F. ) ;
#10301=DIRECTION ( 'NONE',  ( 0.000000000000000000, 0.000000000000000000, -1.000000000000000000 ) ) ;
#10306=AXIS2_PLACEMENT_3D ( 'NONE', #37905, #42831, #64223 ) ;
#10307=LINE ( 'NONE', #37070, #36943 ) ;
#10310=LINE ( 'NONE', #31738, #65814 ) ;
#10332=AXIS2_PLACEMENT_3D ( 'NONE', #52416, #9834, #63630 ) ;
#10343=EDGE_CURVE ( 'NONE', #49504, #23750, #11077, .T. ) ;
#10344=ADVANCED_FACE ( 'NONE', ( #28396 ), #21778, .T. ) ;
#10347=( NAMED_UNIT ( * ) SI_UNIT ( $, .STERADIAN. ) SOLID_ANGLE_UNIT ( ) );
#10365=B_SPLINE_CURVE_WITH_KNOTS ( 'NONE', 3,
 ( #66991, #61664, #35326, #18784, #62720, #19110, #29329, #40262, #14549, #61341 ),
 .UNSPECIFIED., .F., .F.,
 ( 4, 2, 2, 2, 4 ),
 ( 0.002117352549236312977, 0.002645155315643570038, 0.003172958082050826665, 0.003700760848458083292, 0.004228563614865340353 ),
 .UNSPECIFIED. ) ;
#10366=SURFACE_STYLE_FILL_AREA ( #68761 ) ;
#10383=SURFACE_STYLE_USAGE ( .BOTH. , #41711 ) ;
#10386=EDGE_CURVE ( 'NONE', #11113, #22147, #68438, .T. ) ;
#10412=SURFACE_SIDE_STYLE ('',( #58583 ) ) ;
#10419=DIRECTION ( 'NONE',  ( -0.000000000000000000, -0.000000000000000000, 1.000000000000000000 ) ) ;
#10432=( GEOMETRIC_REPRESENTATION_CONTEXT ( 3 ) GLOBAL_UNCERTAINTY_ASSIGNED_CONTEXT ( ( #69162 ) ) GLOBAL_UNIT_ASSIGNED_CONTEXT ( ( #47899, #21093, #52100 ) ) REPRESENTATION_CONTEXT ( 'NONE', 'WORKASPACE' ) );
#10434=SURFACE_STYLE_USAGE ( .BOTH. , #492 ) ;
#10446=FILL_AREA_STYLE ('',( #36525 ) ) ;
#10451=SURFACE_STYLE_FILL_AREA ( #68852 ) ;
#10458=CARTESIAN_POINT ( 'NONE',  ( 10.00000000000001954, 43.00000000000000000, 45.61250543006183733 ) ) ;
#10462=( BOUNDED_CURVE ( )  B_SPLINE_CURVE ( 3, ( #40941, #20121, #67293, #35641 ),
 .UNSPECIFIED., .F., .F. ) 
 B_SPLINE_CURVE_WITH_KNOTS ( ( 4, 4 ),
 ( 1.570796326794896558, 3.141592653589793116 ),
 .UNSPECIFIED. ) 
 CURVE ( )  GEOMETRIC_REPRESENTATION_ITEM ( )  RATIONAL_B_SPLINE_CURVE ( ( 1.000000000000000000, 0.8047378541243649375, 0.8047378541243649375, 1.000000000000000000 ) ) 
 REPRESENTATION_ITEM ( '' )  );
#10476=SURFACE_SIDE_STYLE ('',( #63584 ) ) ;
#10480=DIRECTION ( 'NONE',  ( -0.000000000000000000, -1.000000000000000000, -0.000000000000000000 ) ) ;
#10485=LINE ( 'NONE', #17510, #8472 ) ;
#10491=LINE ( 'NONE', #53408, #12196 ) ;
#10494=STYLED_ITEM ( 'NONE', ( #21803 ), #36477 ) ;
#10515=( GEOMETRIC_REPRESENTATION_CONTEXT ( 3 ) GLOBAL_UNCERTAINTY_ASSIGNED_CONTEXT ( ( #13754 ) ) GLOBAL_UNIT_ASSIGNED_CONTEXT ( ( #5820, #54018, #69507 ) ) REPRESENTATION_CONTEXT ( 'NONE', 'WORKASPACE' ) );
#10519=EDGE_CURVE ( 'NONE', #15573, #20378, #20105, .T. ) ;
#10521=( NAMED_UNIT ( * ) PLANE_ANGLE_UNIT ( ) SI_UNIT ( $, .RADIAN. ) );
#10525=( GEOMETRIC_REPRESENTATION_CONTEXT ( 3 ) GLOBAL_UNCERTAINTY_ASSIGNED_CONTEXT ( ( #9386 ) ) GLOBAL_UNIT_ASSIGNED_CONTEXT ( ( #69509, #57578, #15395 ) ) REPRESENTATION_CONTEXT ( 'NONE', 'WORKASPACE' ) );
#10534=PLANE ( 'NONE',  #18554 ) ;
#10536=ORIENTED_EDGE ( 'NONE', *, *, #67587, .F. ) ;
#10537=FILL_AREA_STYLE_COLOUR ( '', #41441 ) ;
#10540=AXIS2_PLACEMENT_3D ( 'NONE', #65311, #37597, #53704 ) ;
#10563=CARTESIAN_POINT ( 'NONE',  ( 27.00000000000001776, 15.00000000000000000, -34.49999999999999289 ) ) ;
#10565=( GEOMETRIC_REPRESENTATION_CONTEXT ( 3 ) GLOBAL_UNCERTAINTY_ASSIGNED_CONTEXT ( ( #68616 ) ) GLOBAL_UNIT_ASSIGNED_CONTEXT ( ( #51543, #45948, #41030 ) ) REPRESENTATION_CONTEXT ( 'NONE', 'WORKASPACE' ) );
#10568=( LENGTH_UNIT ( ) NAMED_UNIT ( * ) SI_UNIT ( .MILLI., .METRE. ) );
#10569=EDGE_LOOP ( 'NONE', ( #57356, #13841, #15267, #15570 ) ) ;
#10575=ORIENTED_EDGE ( 'NONE', *, *, #55164, .F. ) ;
#10578=LINE ( 'NONE', #639, #14422 ) ;
#10591=DIRECTION ( 'NONE',  ( 0.000000000000000000, 1.000000000000000000, 0.000000000000000000 ) ) ;
#10595=DIRECTION ( 'NONE',  ( 0.6402681315062906942, 0.000000000000000000, -0.7681514953298230752 ) ) ;
#10604=LINE ( 'NONE', #5636, #11362 ) ;
#10605=ORIENTED_EDGE ( 'NONE', *, *, #13243, .T. ) ;
#10607=ORIENTED_EDGE ( 'NONE', *, *, #16237, .T. ) ;
#10615=VECTOR ( 'NONE', #57732, 1000.000000000000000 ) ;
#10617=SURFACE_STYLE_FILL_AREA ( #58802 ) ;
#10621=PRESENTATION_STYLE_ASSIGNMENT (( #26759 ) ) ;
#10626=( NAMED_UNIT ( * ) SI_UNIT ( $, .STERADIAN. ) SOLID_ANGLE_UNIT ( ) );
#10643=ORIENTED_EDGE ( 'NONE', *, *, #47065, .F. ) ;
#10654=( NAMED_UNIT ( * ) SI_UNIT ( $, .STERADIAN. ) SOLID_ANGLE_UNIT ( ) );
#10665=CARTESIAN_POINT ( 'NONE',  ( 7.000000000000017764, 17.78868675966041835, -4.077457891279206668E-16 ) ) ;
#10669=EDGE_CURVE ( 'NONE', #33379, #35954, #25163, .T. ) ;
#10671=AXIS2_PLACEMENT_3D ( 'NONE', #47431, #53015, #53364 ) ;
#10697=DIRECTION ( 'NONE',  ( 0.000000000000000000, -1.000000000000000000, 0.000000000000000000 ) ) ;
#10712=SURFACE_SIDE_STYLE ('',( #5078 ) ) ;
#10713=CIRCLE ( 'NONE', #69122, 2.000000000000001776 ) ;
#10715=FILL_AREA_STYLE ('',( #23008 ) ) ;
#10717=ORIENTED_EDGE ( 'NONE', *, *, #8032, .F. ) ;
#10744=DIRECTION ( 'NONE',  ( 0.000000000000000000, 0.000000000000000000, 1.000000000000000000 ) ) ;
#10745=ORIENTED_EDGE ( 'NONE', *, *, #52216, .F. ) ;
#10746=CYLINDRICAL_SURFACE ( 'NONE', #39688, 0.9999999999999998890 ) ;
#10760=UNCERTAINTY_MEASURE_WITH_UNIT (LENGTH_MEASURE( 1.000000000000000082E-05 ), #45869, 'distance_accuracy_value', 'NONE');
#10766=CIRCLE ( 'NONE', #50096, 1.000000000000000888 ) ;
#10774=DIRECTION ( 'NONE',  ( 0.000000000000000000, 1.000000000000000000, 0.000000000000000000 ) ) ;
#10790=FILL_AREA_STYLE ('',( #4809 ) ) ;
#10795=DIRECTION ( 'NONE',  ( 0.000000000000000000, 0.000000000000000000, 1.000000000000000000 ) ) ;
#10803=FACE_OUTER_BOUND ( 'NONE', #59369, .T. ) ;
#10814=FILL_AREA_STYLE_COLOUR ( '', #37579 ) ;
#10817=CARTESIAN_POINT ( 'NONE',  ( 22.00000000000000711, 43.00000000000000000, -45.61250543006183733 ) ) ;
#10837=( NAMED_UNIT ( * ) SI_UNIT ( $, .STERADIAN. ) SOLID_ANGLE_UNIT ( ) );
#10844=ADVANCED_FACE ( 'NONE', ( #4738 ), #22308, .T. ) ;
#10849=UNCERTAINTY_MEASURE_WITH_UNIT (LENGTH_MEASURE( 1.000000000000000082E-05 ), #35251, 'distance_accuracy_value', 'NONE');
#10859=( NAMED_UNIT ( * ) PLANE_ANGLE_UNIT ( ) SI_UNIT ( $, .RADIAN. ) );
#10866=LINE ( 'NONE', #22812, #62159 ) ;
#10875=DIRECTION ( 'NONE',  ( 0.000000000000000000, 0.000000000000000000, -1.000000000000000000 ) ) ;
#10896=( NAMED_UNIT ( * ) PLANE_ANGLE_UNIT ( ) SI_UNIT ( $, .RADIAN. ) );
#10898=SURFACE_STYLE_FILL_AREA ( #38013 ) ;
#10902=UNCERTAINTY_MEASURE_WITH_UNIT (LENGTH_MEASURE( 1.000000000000000082E-05 ), #66272, 'distance_accuracy_value', 'NONE');
#10907=EDGE_LOOP ( 'NONE', ( #46102, #24266, #4649 ) ) ;
#10909=AXIS2_PLACEMENT_3D ( 'NONE', #52118, #8151, #46515 ) ;
#10911=FACE_OUTER_BOUND ( 'NONE', #58437, .T. ) ;
#10914=SURFACE_STYLE_USAGE ( .BOTH. , #46878 ) ;
#10939=VERTEX_POINT ( 'NONE', #993 ) ;
#10944=PRESENTATION_STYLE_ASSIGNMENT (( #31343 ) ) ;
#10945=STYLED_ITEM ( 'NONE', ( #55545 ), #65596 ) ;
#10951=CARTESIAN_POINT ( 'NONE',  ( 31.00000000000000711, 42.00000000000000000, -36.50000000000000000 ) ) ;
#10953=EDGE_CURVE ( 'NONE', #26431, #8149, #7809, .T. ) ;
#10972=CIRCLE ( 'NONE', #19940, 1.000000000000000888 ) ;
#10978=ORIENTED_EDGE ( 'NONE', *, *, #42803, .F. ) ;
#10985=EDGE_CURVE ( 'NONE', #51461, #44668, #11284, .T. ) ;
#10989=ORIENTED_EDGE ( 'NONE', *, *, #30740, .T. ) ;
#10996=VERTEX_POINT ( 'NONE', #1367 ) ;
#10998=FACE_OUTER_BOUND ( 'NONE', #27896, .T. ) ;
#11007=SURFACE_STYLE_USAGE ( .BOTH. , #30814 ) ;
#11011=LINE ( 'NONE', #16337, #36650 ) ;
#11027=CARTESIAN_POINT ( 'NONE',  ( 28.00000000000002842, 0.000000000000000000, 89.00000000000000000 ) ) ;
#11033=UNCERTAINTY_MEASURE_WITH_UNIT (LENGTH_MEASURE( 1.000000000000000082E-05 ), #49299, 'distance_accuracy_value', 'NONE');
#11034=LINE ( 'NONE', #21963, #51094 ) ;
#11036=ORIENTED_EDGE ( 'NONE', *, *, #56069, .T. ) ;
#11044=VECTOR ( 'NONE', #63789, 1000.000000000000000 ) ;
#11048=MECHANICAL_DESIGN_GEOMETRIC_PRESENTATION_REPRESENTATION('',(#18921),#36959);
#11049=FILL_AREA_STYLE ('',( #58557 ) ) ;
#11055=FILL_AREA_STYLE ('',( #47361 ) ) ;
#11056=CARTESIAN_POINT ( 'NONE',  ( 22.00000000000000355, 42.47058823529412308, -74.11764705882353610 ) ) ;
#11058=VERTEX_POINT ( 'NONE', #49629 ) ;
#11077=CIRCLE ( 'NONE', #62789, 2.499999999999998668 ) ;
#11099=CARTESIAN_POINT ( 'NONE',  ( 1.709458476932651091E-14, -60.04052944165106709, -35.50000000000000000 ) ) ;
#11104=PRESENTATION_STYLE_ASSIGNMENT (( #55053 ) ) ;
#11111=DIRECTION ( 'NONE',  ( 0.000000000000000000, 0.3420201433256693790, 0.9396926207859082059 ) ) ;
#11113=VERTEX_POINT ( 'NONE', #52807 ) ;
#11123=VECTOR ( 'NONE', #57524, 1000.000000000000000 ) ;
#11134=COLOUR_RGB ( '', 0.72549020, 0.75294118, 0.79215686) ;
#11136=VERTEX_POINT ( 'NONE', #48235 ) ;
#11139=DIRECTION ( 'NONE',  ( 1.000000000000000000, 0.000000000000000000, -1.300977106640434891E-16 ) ) ;
#11142=SURFACE_STYLE_FILL_AREA ( #64952 ) ;
#11144=SURFACE_STYLE_FILL_AREA ( #5860 ) ;
#11148=CARTESIAN_POINT ( 'NONE',  ( 30.99999999999998579, 5.000000000000000000, 72.00402776293822171 ) ) ;
#11160=DIRECTION ( 'NONE',  ( 0.000000000000000000, 0.000000000000000000, 1.000000000000000000 ) ) ;
#11186=ADVANCED_FACE ( 'NONE', ( #9894 ), #64378, .F. ) ;
#11187=DIRECTION ( 'NONE',  ( 0.000000000000000000, 0.000000000000000000, 1.000000000000000000 ) ) ;
#11195=DIRECTION ( 'NONE',  ( 0.000000000000000000, 0.000000000000000000, -1.000000000000000000 ) ) ;
#11208=ORIENTED_EDGE ( 'NONE', *, *, #63233, .T. ) ;
#11209=( NAMED_UNIT ( * ) SI_UNIT ( $, .STERADIAN. ) SOLID_ANGLE_UNIT ( ) );
#11214=COLOUR_RGB ( '', 0.66274510, 0.83137255, 0.94901961) ;
#11221=DIRECTION ( 'NONE',  ( 0.000000000000000000, 1.000000000000000000, 0.000000000000000000 ) ) ;
#11229=EDGE_LOOP ( 'NONE', ( #10188, #20783, #67897, #41258 ) ) ;
#11233=FACE_OUTER_BOUND ( 'NONE', #14390, .T. ) ;
#11249=EDGE_LOOP ( 'NONE', ( #64684, #40739, #13548, #26623 ) ) ;
#11258=AXIS2_PLACEMENT_3D ( 'NONE', #42314, #37020, #4959 ) ;
#11266=CARTESIAN_POINT ( 'NONE',  ( 2.999999999999993339, 5.000000000000000000, 24.00402776293822882 ) ) ;
#11267=CARTESIAN_POINT ( 'NONE',  ( 74.89452121010485541, 1.000000000000000000, -66.39042820928574429 ) ) ;
#11271=DIRECTION ( 'NONE',  ( -1.000000000000000000, 0.000000000000000000, 0.000000000000000000 ) ) ;
#11284=LINE ( 'NONE', #33100, #24667 ) ;
#11289=( NAMED_UNIT ( * ) SI_UNIT ( $, .STERADIAN. ) SOLID_ANGLE_UNIT ( ) );
#11292=EDGE_CURVE ( 'NONE', #2410, #58564, #65418, .T. ) ;
#11296=ORIENTED_EDGE ( 'NONE', *, *, #2974, .F. ) ;
#11297=( NAMED_UNIT ( * ) SI_UNIT ( $, .STERADIAN. ) SOLID_ANGLE_UNIT ( ) );
#11301=DIRECTION ( 'NONE',  ( 1.000000000000000000, -6.162975822039156098E-33, -1.300977106640435384E-16 ) ) ;
#11328=ORIENTED_EDGE ( 'NONE', *, *, #33071, .T. ) ;
#11331=VERTEX_POINT ( 'NONE', #17266 ) ;
#11333=CARTESIAN_POINT ( 'NONE',  ( 28.00000000000002842, 42.00000000000000000, 3.902931319921305165E-16 ) ) ;
#11334=MECHANICAL_DESIGN_GEOMETRIC_PRESENTATION_REPRESENTATION('',(#45075),#10252);
#11338=AXIS2_PLACEMENT_3D ( 'NONE', #66380, #56165, #61434 ) ;
#11346=VECTOR ( 'NONE', #11139, 1000.000000000000000 ) ;
#11347=ADVANCED_FACE ( 'NONE', ( #38730 ), #64725, .F. ) ;
#11349=VERTEX_POINT ( 'NONE', #54001 ) ;
#11354=EDGE_CURVE ( 'NONE', #56002, #45281, #62204, .T. ) ;
#11357=EDGE_CURVE ( 'NONE', #3674, #4136, #62939, .T. ) ;
#11361=VERTEX_POINT ( 'NONE', #50969 ) ;
#11362=VECTOR ( 'NONE', #37734, 1000.000000000000000 ) ;
#11373=DIRECTION ( 'NONE',  ( 1.000000000000000000, -0.000000000000000000, 0.000000000000000000 ) ) ;
#11375=ORIENTED_EDGE ( 'NONE', *, *, #63113, .T. ) ;
#11378=CARTESIAN_POINT ( 'NONE',  ( 7.999999999999992895, 0.000000000000000000, -24.00402776293826079 ) ) ;
#11384=VERTEX_POINT ( 'NONE', #62543 ) ;
#11388=DIRECTION ( 'NONE',  ( -1.000000000000000000, 0.000000000000000000, 0.000000000000000000 ) ) ;
#11390=CARTESIAN_POINT ( 'NONE',  ( 57.00000000000000000, 5.000000000000000000, -60.00402776293825724 ) ) ;
#11394=FACE_OUTER_BOUND ( 'NONE', #33617, .T. ) ;
#11396=ORIENTED_EDGE ( 'NONE', *, *, #22695, .F. ) ;
#11400=DIRECTION ( 'NONE',  ( -1.000000000000000000, 0.000000000000000000, 0.000000000000000000 ) ) ;
#11402=ORIENTED_EDGE ( 'NONE', *, *, #50599, .T. ) ;
#11404=CARTESIAN_POINT ( 'NONE',  ( 3.000000000000030198, 42.00000000000000000, 89.00000000000000000 ) ) ;
#11413=FILL_AREA_STYLE ('',( #27218 ) ) ;
#11427=LINE ( 'NONE', #27589, #2102 ) ;
#11431=EDGE_CURVE ( 'NONE', #1416, #65761, #3524, .T. ) ;
#11443=SURFACE_SIDE_STYLE ('',( #49789 ) ) ;
#11455=DIRECTION ( 'NONE',  ( -1.000000000000000000, 0.000000000000000000, 0.000000000000000000 ) ) ;
#11475=( NAMED_UNIT ( * ) SI_UNIT ( $, .STERADIAN. ) SOLID_ANGLE_UNIT ( ) );
#11477=DIRECTION ( 'NONE',  ( 0.000000000000000000, 0.000000000000000000, -1.000000000000000000 ) ) ;
#11479=ORIENTED_EDGE ( 'NONE', *, *, #15533, .F. ) ;
#11484=UNCERTAINTY_MEASURE_WITH_UNIT (LENGTH_MEASURE( 1.000000000000000082E-05 ), #19867, 'distance_accuracy_value', 'NONE');
#11485=EDGE_LOOP ( 'NONE', ( #65846, #1381, #38070, #1761 ) ) ;
#11490=DIRECTION ( 'NONE',  ( -1.000000000000000000, 0.000000000000000000, 1.300977106640435137E-16 ) ) ;
#11494=ORIENTED_EDGE ( 'NONE', *, *, #64178, .F. ) ;
#11495=CARTESIAN_POINT ( 'NONE',  ( 28.58578643762692550, 42.99999999999999289, 79.58981420056515788 ) ) ;
#11499=MECHANICAL_DESIGN_GEOMETRIC_PRESENTATION_REPRESENTATION('',(#48667),#58703);
#11511=CARTESIAN_POINT ( 'NONE',  ( 32.00000000000001421, -60.04052944165106709, 35.50000000000000000 ) ) ;
#11520=CARTESIAN_POINT ( 'NONE',  ( 24.68215826162192528, 25.64799036762169848, 27.48644429636420128 ) ) ;
#11521=DIRECTION ( 'NONE',  ( 0.000000000000000000, -1.000000000000000000, 0.000000000000000000 ) ) ;
#11526=FACE_BOUND ( 'NONE', #61628, .T. ) ;
#11529=SURFACE_STYLE_FILL_AREA ( #569 ) ;
#11531=SURFACE_SIDE_STYLE ('',( #5541 ) ) ;
#11532=EDGE_LOOP ( 'NONE', ( #29259, #24865, #47352, #28864 ) ) ;
#11537=VECTOR ( 'NONE', #20329, 1000.000000000000000 ) ;
#11539=ORIENTED_EDGE ( 'NONE', *, *, #4758, .F. ) ;
#11545=COLOUR_RGB ( '', 0.72549020, 0.75294118, 0.79215686) ;
#11549=ORIENTED_EDGE ( 'NONE', *, *, #19305, .T. ) ;
#11551=SURFACE_SIDE_STYLE ('',( #34047 ) ) ;
#11553=( NAMED_UNIT ( * ) SI_UNIT ( $, .STERADIAN. ) SOLID_ANGLE_UNIT ( ) );
#11562=ORIENTED_EDGE ( 'NONE', *, *, #52420, .T. ) ;
#11570=( NAMED_UNIT ( * ) SI_UNIT ( $, .STERADIAN. ) SOLID_ANGLE_UNIT ( ) );
#11571=( LENGTH_UNIT ( ) NAMED_UNIT ( * ) SI_UNIT ( .MILLI., .METRE. ) );
#11576=FILL_AREA_STYLE_COLOUR ( '', #40839 ) ;
#11582=UNCERTAINTY_MEASURE_WITH_UNIT (LENGTH_MEASURE( 1.000000000000000082E-05 ), #4760, 'distance_accuracy_value', 'NONE');
#11591=VERTEX_POINT ( 'NONE', #35321 ) ;
#11598=PLANE ( 'NONE',  #10210 ) ;
#11600=PRESENTATION_STYLE_ASSIGNMENT (( #47923 ) ) ;
#11604=VERTEX_POINT ( 'NONE', #34962 ) ;
#11606=EDGE_CURVE ( 'NONE', #48365, #24376, #15938, .T. ) ;
#11607=FILL_AREA_STYLE_COLOUR ( '', #40271 ) ;
#11619=CIRCLE ( 'NONE', #48724, 5.000000000000004441 ) ;
#11623=DIRECTION ( 'NONE',  ( 1.300977106640429960E-16, 0.000000000000000000, 1.000000000000000000 ) ) ;
#11639=VECTOR ( 'NONE', #66060, 1000.000000000000000 ) ;
#11648=AXIS2_PLACEMENT_3D ( 'NONE', #51369, #13372, #2423 ) ;
#11652=ORIENTED_EDGE ( 'NONE', *, *, #60054, .F. ) ;
#11653=CIRCLE ( 'NONE', #36416, 1.000000000000000888 ) ;
#11661=DIRECTION ( 'NONE',  ( 0.000000000000000000, 0.000000000000000000, -1.000000000000000000 ) ) ;
#11671=EDGE_LOOP ( 'NONE', ( #67707, #47417, #27615, #32754 ) ) ;
#11680=( NAMED_UNIT ( * ) PLANE_ANGLE_UNIT ( ) SI_UNIT ( $, .RADIAN. ) );
#11697=( GEOMETRIC_REPRESENTATION_CONTEXT ( 3 ) GLOBAL_UNCERTAINTY_ASSIGNED_CONTEXT ( ( #41994 ) ) GLOBAL_UNIT_ASSIGNED_CONTEXT ( ( #51106, #23655, #57055 ) ) REPRESENTATION_CONTEXT ( 'NONE', 'WORKASPACE' ) );
#11705=LINE ( 'NONE', #48013, #59501 ) ;
#11711=( NAMED_UNIT ( * ) PLANE_ANGLE_UNIT ( ) SI_UNIT ( $, .RADIAN. ) );
#11714=ORIENTED_EDGE ( 'NONE', *, *, #36207, .T. ) ;
#11719=( NAMED_UNIT ( * ) PLANE_ANGLE_UNIT ( ) SI_UNIT ( $, .RADIAN. ) );
#11738=PRESENTATION_STYLE_ASSIGNMENT (( #12413 ) ) ;
#11744=PRESENTATION_STYLE_ASSIGNMENT (( #21972 ) ) ;
#11748=DIRECTION ( 'NONE',  ( -0.000000000000000000, 0.000000000000000000, 1.000000000000000000 ) ) ;
#11752=CYLINDRICAL_SURFACE ( 'NONE', #1052, 25.00000000000001421 ) ;
#11762=DIRECTION ( 'NONE',  ( -0.000000000000000000, -1.000000000000000000, -0.000000000000000000 ) ) ;
#11777=FACE_BOUND ( 'NONE', #38333, .T. ) ;
#11793=FACE_OUTER_BOUND ( 'NONE', #14556, .T. ) ;
#11798=STYLED_ITEM ( 'NONE', ( #22519 ), #27374 ) ;
#11801=CARTESIAN_POINT ( 'NONE',  ( 57.00000000000000000, 13.00000000000000178, -79.00402776293826435 ) ) ;
#11805=( NAMED_UNIT ( * ) PLANE_ANGLE_UNIT ( ) SI_UNIT ( $, .RADIAN. ) );
#11817=( LENGTH_UNIT ( ) NAMED_UNIT ( * ) SI_UNIT ( .MILLI., .METRE. ) );
#11818=DIRECTION ( 'NONE',  ( 0.000000000000000000, 1.000000000000000000, 0.000000000000000000 ) ) ;
#11824=MECHANICAL_DESIGN_GEOMETRIC_PRESENTATION_REPRESENTATION('',(#63507),#65818);
#11832=PRESENTATION_STYLE_ASSIGNMENT (( #27979 ) ) ;
#11833=ADVANCED_FACE ( 'NONE', ( #20876 ), #36747, .F. ) ;
#11837=DIRECTION ( 'NONE',  ( 1.000000000000000000, 0.000000000000000000, -1.300977106640442040E-16 ) ) ;
#11847=TOROIDAL_SURFACE ( 'NONE', #1656, 6.000000000000000000, 1.000000000000000000 ) ;
#11855=VECTOR ( 'NONE', #62189, 1000.000000000000000 ) ;
#11856=FACE_OUTER_BOUND ( 'NONE', #8565, .T. ) ;
#11863=MECHANICAL_DESIGN_GEOMETRIC_PRESENTATION_REPRESENTATION('',(#29830),#37790);
#11879=FACE_OUTER_BOUND ( 'NONE', #59064, .T. ) ;
#11880=AXIS2_PLACEMENT_3D ( 'NONE', #15832, #4898, #69285 ) ;
#11885=MECHANICAL_DESIGN_GEOMETRIC_PRESENTATION_REPRESENTATION('',(#574),#35500);
#11922=SURFACE_SIDE_STYLE ('',( #23181 ) ) ;
#11924=AXIS2_PLACEMENT_3D ( 'NONE', #24870, #19602, #66404 ) ;
#11927=FILL_AREA_STYLE_COLOUR ( '', #67780 ) ;
#11928=EDGE_CURVE ( 'NONE', #40021, #11113, #18373, .T. ) ;
#11930=FILL_AREA_STYLE ('',( #6624 ) ) ;
#11933=( NAMED_UNIT ( * ) SI_UNIT ( $, .STERADIAN. ) SOLID_ANGLE_UNIT ( ) );
#11938=VECTOR ( 'NONE', #27552, 1000.000000000000000 ) ;
#11941=LINE ( 'NONE', #43994, #56341 ) ;
#11945=FACE_OUTER_BOUND ( 'NONE', #49831, .T. ) ;
#11948=FILL_AREA_STYLE ('',( #16569 ) ) ;
#11956=CYLINDRICAL_SURFACE ( 'NONE', #30270, 110.0000000000000142 ) ;
#11961=MECHANICAL_DESIGN_GEOMETRIC_PRESENTATION_REPRESENTATION('',(#44592),#14227);
#11967=CARTESIAN_POINT ( 'NONE',  ( 29.00000000000000000, 42.00000000000000000, -80.00402776293826435 ) ) ;
#11972=( NAMED_UNIT ( * ) PLANE_ANGLE_UNIT ( ) SI_UNIT ( $, .RADIAN. ) );
#11973=CIRCLE ( 'NONE', #5228, 113.0000000000000142 ) ;
#11974=LINE ( 'NONE', #33431, #37512 ) ;
#11976=VERTEX_POINT ( 'NONE', #23290 ) ;
#11983=CARTESIAN_POINT ( 'NONE',  ( 8.000000000000024869, 5.000000000000000000, 32.00402776293825724 ) ) ;
#11996=( NAMED_UNIT ( * ) PLANE_ANGLE_UNIT ( ) SI_UNIT ( $, .RADIAN. ) );
#11998=( LENGTH_UNIT ( ) NAMED_UNIT ( * ) SI_UNIT ( .MILLI., .METRE. ) );
#12005=CARTESIAN_POINT ( 'NONE',  ( 16.00000000000001776, 43.00000000000000000, 29.68999999999999417 ) ) ;
#12007=EDGE_CURVE ( 'NONE', #52838, #22382, #48793, .T. ) ;
#12013=ADVANCED_FACE ( 'NONE', ( #62309 ), #34877, .T. ) ;
#12014=EDGE_LOOP ( 'NONE', ( #57021, #44437, #47376, #11539 ) ) ;
#12016=CARTESIAN_POINT ( 'NONE',  ( 92.41620014002536720, 0.000000000000000000, 29.00402776293826079 ) ) ;
#12033=FACE_OUTER_BOUND ( 'NONE', #30570, .T. ) ;
#12048=CARTESIAN_POINT ( 'NONE',  ( 57.00000000000000000, 0.9999999999999991118, -60.00402776293827145 ) ) ;
#12059=AXIS2_PLACEMENT_3D ( 'NONE', #50257, #43976, #59759 ) ;
#12066=( LENGTH_UNIT ( ) NAMED_UNIT ( * ) SI_UNIT ( .MILLI., .METRE. ) );
#12070=ORIENTED_EDGE ( 'NONE', *, *, #63915, .F. ) ;
#12072=SURFACE_SIDE_STYLE ('',( #28223 ) ) ;
#12078=DIRECTION ( 'NONE',  ( 1.000000000000000000, 0.000000000000000000, 0.000000000000000000 ) ) ;
#12079=CYLINDRICAL_SURFACE ( 'NONE', #39673, 5.000000000000004441 ) ;
#12084=DIRECTION ( 'NONE',  ( -0.000000000000000000, -0.6691306063588591257, 0.7431448254773933559 ) ) ;
#12085=VECTOR ( 'NONE', #29421, 1000.000000000000000 ) ;
#12086=ORIENTED_EDGE ( 'NONE', *, *, #4379, .T. ) ;
#12091=CARTESIAN_POINT ( 'NONE',  ( 93.00000000000000000, 0.000000000000000000, 0.000000000000000000 ) ) ;
#12093=ORIENTED_EDGE ( 'NONE', *, *, #17368, .F. ) ;
#12099=( NAMED_UNIT ( * ) PLANE_ANGLE_UNIT ( ) SI_UNIT ( $, .RADIAN. ) );
#12102=LINE ( 'NONE', #16479, #2393 ) ;
#12110=( LENGTH_UNIT ( ) NAMED_UNIT ( * ) SI_UNIT ( .MILLI., .METRE. ) );
#12120=ORIENTED_EDGE ( 'NONE', *, *, #10669, .T. ) ;
#12123=LINE ( 'NONE', #1162, #24920 ) ;
#12141=CARTESIAN_POINT ( 'NONE',  ( 0.000000000000000000, 14.00000000000000000, 80.00402776293826435 ) ) ;
#12144=FILL_AREA_STYLE ('',( #17126 ) ) ;
#12159=CYLINDRICAL_SURFACE ( 'NONE', #45276, 5.000000000000004441 ) ;
#12166=( NAMED_UNIT ( * ) PLANE_ANGLE_UNIT ( ) SI_UNIT ( $, .RADIAN. ) );
#12167=ORIENTED_EDGE ( 'NONE', *, *, #51801, .F. ) ;
#12168=DIRECTION ( 'NONE',  ( -1.000000000000000000, 0.000000000000000000, 0.000000000000000000 ) ) ;
#12169=CARTESIAN_POINT ( 'NONE',  ( 10.00000000000002309, 43.00000000000000000, 74.38749456993816978 ) ) ;
#12170=DIRECTION ( 'NONE',  ( 0.000000000000000000, 0.000000000000000000, 1.000000000000000000 ) ) ;
#12178=( GEOMETRIC_REPRESENTATION_CONTEXT ( 3 ) GLOBAL_UNCERTAINTY_ASSIGNED_CONTEXT ( ( #9574 ) ) GLOBAL_UNIT_ASSIGNED_CONTEXT ( ( #20454, #25379, #28985 ) ) REPRESENTATION_CONTEXT ( 'NONE', 'WORKASPACE' ) );
#12183=( NAMED_UNIT ( * ) PLANE_ANGLE_UNIT ( ) SI_UNIT ( $, .RADIAN. ) );
#12196=VECTOR ( 'NONE', #69563, 1000.000000000000000 ) ;
#12206=EDGE_CURVE ( 'NONE', #59091, #27365, #47216, .T. ) ;
#12212=DIRECTION ( 'NONE',  ( 0.000000000000000000, 0.000000000000000000, 1.000000000000000000 ) ) ;
#12214=ORIENTED_EDGE ( 'NONE', *, *, #29984, .F. ) ;
#12237=MECHANICAL_DESIGN_GEOMETRIC_PRESENTATION_REPRESENTATION('',(#33600),#61622);
#12246=VECTOR ( 'NONE', #45299, 1000.000000000000000 ) ;
#12251=ORIENTED_EDGE ( 'NONE', *, *, #11606, .F. ) ;
#12270=AXIS2_PLACEMENT_3D ( 'NONE', #63796, #11373, #53272 ) ;
#12275=MECHANICAL_DESIGN_GEOMETRIC_PRESENTATION_REPRESENTATION('',(#29142),#32513);
#12277=DIRECTION ( 'NONE',  ( 1.000000000000000000, 0.000000000000000000, 0.000000000000000000 ) ) ;
#12278=SURFACE_STYLE_FILL_AREA ( #59426 ) ;
#12280=SURFACE_STYLE_USAGE ( .BOTH. , #34448 ) ;
#12285=CARTESIAN_POINT ( 'NONE',  ( 28.00000000000002842, 38.70020753820971748, 90.00000000000000000 ) ) ;
#12291=ADVANCED_FACE ( 'NONE', ( #65058 ), #30426, .T. ) ;
#12292=( LENGTH_UNIT ( ) NAMED_UNIT ( * ) SI_UNIT ( .MILLI., .METRE. ) );
#12298=EDGE_CURVE ( 'NONE', #51304, #60615, #44016, .T. ) ;
#12302=CIRCLE ( 'NONE', #60604, 1.000000000000000888 ) ;
#12303=COLOUR_RGB ( '', 0.08235294, 0.09019608, 0.10196078) ;
#12309=CARTESIAN_POINT ( 'NONE',  ( 10.00000000000000533, 43.00000000000000000, -45.61250543006183733 ) ) ;
#12323=( NAMED_UNIT ( * ) PLANE_ANGLE_UNIT ( ) SI_UNIT ( $, .RADIAN. ) );
#12326=CIRCLE ( 'NONE', #35960, 3.499999999999999556 ) ;
#12334=SURFACE_STYLE_USAGE ( .BOTH. , #356 ) ;
#12352=COLOUR_RGB ( '', 0.40784314, 0.44705882, 0.49803922) ;
#12357=VERTEX_POINT ( 'NONE', #61179 ) ;
#12364=ORIENTED_EDGE ( 'NONE', *, *, #7932, .T. ) ;
#12373=( GEOMETRIC_REPRESENTATION_CONTEXT ( 3 ) GLOBAL_UNCERTAINTY_ASSIGNED_CONTEXT ( ( #1762 ) ) GLOBAL_UNIT_ASSIGNED_CONTEXT ( ( #2360, #35827, #66446 ) ) REPRESENTATION_CONTEXT ( 'NONE', 'WORKASPACE' ) );
#12383=AXIS2_PLACEMENT_3D ( 'NONE', #37967, #11521, #28725 ) ;
#12392=EDGE_CURVE ( 'NONE', #54537, #5489, #30534, .T. ) ;
#12393=DIRECTION ( 'NONE',  ( 1.000000000000000000, 0.000000000000000000, 0.000000000000000000 ) ) ;
#12394=SURFACE_STYLE_FILL_AREA ( #61287 ) ;
#12403=( NAMED_UNIT ( * ) PLANE_ANGLE_UNIT ( ) SI_UNIT ( $, .RADIAN. ) );
#12408=AXIS2_PLACEMENT_3D ( 'NONE', #8161, #14457, #68286 ) ;
#12412=UNCERTAINTY_MEASURE_WITH_UNIT (LENGTH_MEASURE( 1.000000000000000082E-05 ), #24972, 'distance_accuracy_value', 'NONE');
#12413=SURFACE_STYLE_USAGE ( .BOTH. , #50770 ) ;
#12416=CARTESIAN_POINT ( 'NONE',  ( 4.000000000000030198, 38.00000000000000711, 90.00000000000000000 ) ) ;
#12418=( NAMED_UNIT ( * ) SI_UNIT ( $, .STERADIAN. ) SOLID_ANGLE_UNIT ( ) );
#12423=ADVANCED_FACE ( 'NONE', ( #13684 ), #56256, .F. ) ;
#12427=ORIENTED_EDGE ( 'NONE', *, *, #43018, .F. ) ;
#12449=ORIENTED_EDGE ( 'NONE', *, *, #51084, .F. ) ;
#12451=FILL_AREA_STYLE ('',( #23037 ) ) ;
#12452=ADVANCED_FACE ( 'NONE', ( #50632 ), #12990, .F. ) ;
#12470=AXIS2_PLACEMENT_3D ( 'NONE', #39004, #6254, #60065 ) ;
#12471=CARTESIAN_POINT ( 'NONE',  ( 31.00000000000002132, 43.00000000000000000, 79.00402776293826435 ) ) ;
#12481=DIRECTION ( 'NONE',  ( 0.000000000000000000, -1.000000000000000000, 0.000000000000000000 ) ) ;
#12488=SURFACE_STYLE_USAGE ( .BOTH. , #18485 ) ;
#12501=DIRECTION ( 'NONE',  ( -0.000000000000000000, 1.000000000000000000, -0.000000000000000000 ) ) ;
#12509=EDGE_LOOP ( 'NONE', ( #17942, #57992, #154, #20953 ) ) ;
#12512=SURFACE_STYLE_FILL_AREA ( #60701 ) ;
#12519=DIRECTION ( 'NONE',  ( 0.000000000000000000, 0.000000000000000000, 1.000000000000000000 ) ) ;
#12541=STYLED_ITEM ( 'NONE', ( #67578 ), #18531 ) ;
#12549=AXIS2_PLACEMENT_3D ( 'NONE', #25495, #62772, #57882 ) ;
#12553=CARTESIAN_POINT ( 'NONE',  ( 11.00000000000001776, -60.04052944165106709, -35.50000000000000000 ) ) ;
#12554=COLOUR_RGB ( '', 0.72549020, 0.75294118, 0.79215686) ;
#12559=STYLED_ITEM ( 'NONE', ( #29465 ), #23057 ) ;
#12567=STYLED_ITEM ( 'NONE', ( #3384 ), #35614 ) ;
#12569=( LENGTH_UNIT ( ) NAMED_UNIT ( * ) SI_UNIT ( .MILLI., .METRE. ) );
#12580=MECHANICAL_DESIGN_GEOMETRIC_PRESENTATION_REPRESENTATION('',(#50819),#5850);
#12587=ORIENTED_EDGE ( 'NONE', *, *, #53670, .F. ) ;
#12589=MECHANICAL_DESIGN_GEOMETRIC_PRESENTATION_REPRESENTATION('',(#30563),#37370);
#12590=SURFACE_SIDE_STYLE ('',( #61136 ) ) ;
#12594=ORIENTED_EDGE ( 'NONE', *, *, #30154, .T. ) ;
#12598=AXIS2_PLACEMENT_3D ( 'NONE', #44508, #56756, #56386 ) ;
#12604=VERTEX_POINT ( 'NONE', #45657 ) ;
#12605=DIRECTION ( 'NONE',  ( 0.000000000000000000, 1.000000000000000000, -0.000000000000000000 ) ) ;
#12609=STYLED_ITEM ( 'NONE', ( #46458 ), #60579 ) ;
#12612=SPHERICAL_SURFACE ( 'NONE', #68722, 1.000000000000000000 ) ;
#12623=SURFACE_SIDE_STYLE ('',( #23205 ) ) ;
#12624=EDGE_CURVE ( 'NONE', #18241, #23764, #14295, .T. ) ;
#12649=CARTESIAN_POINT ( 'NONE',  ( 3.000000000000030198, 42.00000000000000000, 80.00402776293826435 ) ) ;
#12655=( NAMED_UNIT ( * ) SI_UNIT ( $, .STERADIAN. ) SOLID_ANGLE_UNIT ( ) );
#12664=SURFACE_SIDE_STYLE ('',( #17637 ) ) ;
#12678=FILL_AREA_STYLE ('',( #39461 ) ) ;
#12690=SURFACE_SIDE_STYLE ('',( #60877 ) ) ;
#12700=ORIENTED_EDGE ( 'NONE', *, *, #47959, .F. ) ;
#12716=CIRCLE ( 'NONE', #44202, 1.000000000000000888 ) ;
#12718=CARTESIAN_POINT ( 'NONE',  ( 6.117035285937315159, 43.00000000000000000, -28.67160620906788537 ) ) ;
#12726=( NAMED_UNIT ( * ) SI_UNIT ( $, .STERADIAN. ) SOLID_ANGLE_UNIT ( ) );
#12730=FILL_AREA_STYLE_COLOUR ( '', #61658 ) ;
#12735=TOROIDAL_SURFACE ( 'NONE', #2600, 111.0000000000000142, 1.000000000000000000 ) ;
#12739=CIRCLE ( 'NONE', #61036, 2.000000000000001776 ) ;
#12741=ORIENTED_EDGE ( 'NONE', *, *, #31369, .F. ) ;
#12742=SURFACE_STYLE_FILL_AREA ( #28197 ) ;
#12745=CARTESIAN_POINT ( 'NONE',  ( 35.99999999999999289, 5.000000000000000000, -37.00402776293825724 ) ) ;
#12746=EDGE_CURVE ( 'NONE', #53049, #23835, #37547, .T. ) ;
#12747=COLOUR_RGB ( '', 0.66274510, 0.83137255, 0.94901961) ;
#12773=SURFACE_SIDE_STYLE ('',( #21602 ) ) ;
#12774=CARTESIAN_POINT ( 'NONE',  ( 12.00000000000001776, 14.00000000000000000, -29.68999999999999417 ) ) ;
#12780=ORIENTED_EDGE ( 'NONE', *, *, #11357, .T. ) ;
#12781=FILL_AREA_STYLE_COLOUR ( '', #43000 ) ;
#12784=DIRECTION ( 'NONE',  ( 0.000000000000000000, 0.000000000000000000, 1.000000000000000000 ) ) ;
#12809=SURFACE_SIDE_STYLE ('',( #28632 ) ) ;
#12814=( NAMED_UNIT ( * ) PLANE_ANGLE_UNIT ( ) SI_UNIT ( $, .RADIAN. ) );
#12821=SURFACE_STYLE_USAGE ( .BOTH. , #46629 ) ;
#12825=CIRCLE ( 'NONE', #27420, 0.9999999999999992228 ) ;
#12836=EDGE_CURVE ( 'NONE', #12357, #65192, #12123, .T. ) ;
#12838=VECTOR ( 'NONE', #41159, 1000.000000000000000 ) ;
#12843=CARTESIAN_POINT ( 'NONE',  ( 16.00000000000001776, 15.00000000000000000, 29.68999999999999417 ) ) ;
#12851=EDGE_CURVE ( 'NONE', #19928, #34574, #5441, .T. ) ;
#12862=CIRCLE ( 'NONE', #52221, 1.000000000000000888 ) ;
#12863=CARTESIAN_POINT ( 'NONE',  ( 57.00000000000000000, 5.000000000000000000, 77.00402776293825013 ) ) ;
#12871=DIRECTION ( 'NONE',  ( 0.000000000000000000, 0.000000000000000000, -1.000000000000000000 ) ) ;
#12874=CARTESIAN_POINT ( 'NONE',  ( 10.00000000000002309, 60.69879356856722552, 69.02971849933236115 ) ) ;
#12876=( NAMED_UNIT ( * ) SI_UNIT ( $, .STERADIAN. ) SOLID_ANGLE_UNIT ( ) );
#12879=COLOUR_RGB ( '', 0.09019608, 0.27058824, 0.51372549) ;
#12881=UNCERTAINTY_MEASURE_WITH_UNIT (LENGTH_MEASURE( 1.000000000000000082E-05 ), #51486, 'distance_accuracy_value', 'NONE');
#12887=AXIS2_PLACEMENT_3D ( 'NONE', #12553, #23458, #18192 ) ;
#12889=ORIENTED_EDGE ( 'NONE', *, *, #50599, .F. ) ;
#12899=ADVANCED_FACE ( 'NONE', ( #6164 ), #38913, .T. ) ;
#12911=UNCERTAINTY_MEASURE_WITH_UNIT (LENGTH_MEASURE( 1.000000000000000082E-05 ), #5440, 'distance_accuracy_value', 'NONE');
#12913=SURFACE_STYLE_FILL_AREA ( #27341 ) ;
#12922=SURFACE_STYLE_USAGE ( .BOTH. , #61115 ) ;
#12924=SURFACE_SIDE_STYLE ('',( #66040 ) ) ;
#12929=PRESENTATION_STYLE_ASSIGNMENT (( #61118 ) ) ;
#12930=( NAMED_UNIT ( * ) SI_UNIT ( $, .STERADIAN. ) SOLID_ANGLE_UNIT ( ) );
#12942=ORIENTED_EDGE ( 'NONE', *, *, #48423, .F. ) ;
#12944=ORIENTED_EDGE ( 'NONE', *, *, #31299, .F. ) ;
#12952=EDGE_CURVE ( 'NONE', #40860, #31338, #28643, .T. ) ;
#12963=AXIS2_PLACEMENT_3D ( 'NONE', #42885, #64278, #16130 ) ;
#12970=ORIENTED_EDGE ( 'NONE', *, *, #33679, .T. ) ;
#12980=EDGE_CURVE ( 'NONE', #49536, #26439, #50469, .T. ) ;
#12981=AXIS2_PLACEMENT_3D ( 'NONE', #25335, #62276, #62955 ) ;
#12984=CARTESIAN_POINT ( 'NONE',  ( 109.0067032876572455, 0.9999999999999991118, -19.20378738324562207 ) ) ;
#12990=CYLINDRICAL_SURFACE ( 'NONE', #31546, 1.000000000000000888 ) ;
#13002=MECHANICAL_DESIGN_GEOMETRIC_PRESENTATION_REPRESENTATION('',(#19738),#8551);
#13004=ORIENTED_EDGE ( 'NONE', *, *, #49144, .T. ) ;
#13009=DIRECTION ( 'NONE',  ( -0.000000000000000000, -1.000000000000000000, -0.000000000000000000 ) ) ;
#13020=FILL_AREA_STYLE ('',( #44044 ) ) ;
#13027=EDGE_CURVE ( 'NONE', #25731, #41380, #61351, .T. ) ;
#13028=ORIENTED_EDGE ( 'NONE', *, *, #27092, .T. ) ;
#13038=AXIS2_PLACEMENT_3D ( 'NONE', #16871, #1653, #33702 ) ;
#13045=DIRECTION ( 'NONE',  ( 0.000000000000000000, -1.000000000000000000, 0.000000000000000000 ) ) ;
#13046=UNCERTAINTY_MEASURE_WITH_UNIT (LENGTH_MEASURE( 1.000000000000000082E-05 ), #60929, 'distance_accuracy_value', 'NONE');
#13062=ORIENTED_EDGE ( 'NONE', *, *, #28224, .T. ) ;
#13071=CARTESIAN_POINT ( 'NONE',  ( 33.00000000000002132, 15.00000000000000000, 80.00402776293826435 ) ) ;
#13075=( LENGTH_UNIT ( ) NAMED_UNIT ( * ) SI_UNIT ( .MILLI., .METRE. ) );
#13076=AXIS2_PLACEMENT_3D ( 'NONE', #61038, #7582, #39986 ) ;
#13091=EDGE_CURVE ( 'NONE', #417, #51841, #41825, .T. ) ;
#13099=AXIS2_PLACEMENT_3D ( 'NONE', #61044, #54721, #38954 ) ;
#13106=CARTESIAN_POINT ( 'NONE',  ( 4.000000000000030198, 43.00000000000000000, 79.00402776293826435 ) ) ;
#13130=FILL_AREA_STYLE_COLOUR ( '', #68930 ) ;
#13134=FILL_AREA_STYLE_COLOUR ( '', #45665 ) ;
#13150=LINE ( 'NONE', #22337, #51085 ) ;
#13158=CYLINDRICAL_SURFACE ( 'NONE', #833, 5.000000000000004441 ) ;
#13165=CARTESIAN_POINT ( 'NONE',  ( 10.00000000000002132, 50.00000000000000000, 60.00000000000000711 ) ) ;
#13180=FILL_AREA_STYLE ('',( #39617 ) ) ;
#13181=DIRECTION ( 'NONE',  ( 0.000000000000000000, 0.000000000000000000, 1.000000000000000000 ) ) ;
#13184=VERTEX_POINT ( 'NONE', #25116 ) ;
#13185=CARTESIAN_POINT ( 'NONE',  ( 11.00000000000001776, 15.00000000000000000, 29.68999999999999417 ) ) ;
#13203=DIRECTION ( 'NONE',  ( 0.000000000000000000, -0.9396926207859105373, -0.3420201433256629953 ) ) ;
#13207=FILL_AREA_STYLE_COLOUR ( '', #52766 ) ;
#13217=CARTESIAN_POINT ( 'NONE',  ( 2.000000000000009326, 26.00000000000000355, -20.50000000000000355 ) ) ;
#13235=PRESENTATION_STYLE_ASSIGNMENT (( #13588 ) ) ;
#13236=VECTOR ( 'NONE', #66363, 1000.000000000000000 ) ;
#13239=DIRECTION ( 'NONE',  ( -0.000000000000000000, -1.000000000000000000, -0.000000000000000000 ) ) ;
#13240=CARTESIAN_POINT ( 'NONE',  ( 11.00000000000001776, 15.00000000000000000, -29.68999999999999417 ) ) ;
#13241=VECTOR ( 'NONE', #11748, 1000.000000000000000 ) ;
#13243=EDGE_CURVE ( 'NONE', #68594, #1306, #54092, .T. ) ;
#13259=VERTEX_POINT ( 'NONE', #54524 ) ;
#13261=CYLINDRICAL_SURFACE ( 'NONE', #1517, 4.999999999999997335 ) ;
#13279=ORIENTED_EDGE ( 'NONE', *, *, #25182, .F. ) ;
#13299=DIRECTION ( 'NONE',  ( -0.000000000000000000, 0.6691306063588591257, 0.7431448254773933559 ) ) ;
#13302=DIRECTION ( 'NONE',  ( 0.000000000000000000, 0.000000000000000000, 1.000000000000000000 ) ) ;
#13310=DIRECTION ( 'NONE',  ( -1.000000000000000000, 0.000000000000000000, 0.000000000000000000 ) ) ;
#13323=( GEOMETRIC_REPRESENTATION_CONTEXT ( 3 ) GLOBAL_UNCERTAINTY_ASSIGNED_CONTEXT ( ( #69297 ) ) GLOBAL_UNIT_ASSIGNED_CONTEXT ( ( #28097, #44365, #60468 ) ) REPRESENTATION_CONTEXT ( 'NONE', 'WORKASPACE' ) );
#13324=FILL_AREA_STYLE ('',( #3790 ) ) ;
#13327=CARTESIAN_POINT ( 'NONE',  ( 179.4361977533490347, 0.9999999999999991118, -103.7004518695263044 ) ) ;
#13329=CIRCLE ( 'NONE', #35786, 4.999999999999997335 ) ;
#13332=EDGE_CURVE ( 'NONE', #40021, #1731, #6671, .T. ) ;
#13336=PRESENTATION_STYLE_ASSIGNMENT (( #13695 ) ) ;
#13344=FILL_AREA_STYLE_COLOUR ( '', #66173 ) ;
#13345=STYLED_ITEM ( 'NONE', ( #27936 ), #51101 ) ;
#13348=DIRECTION ( 'NONE',  ( 0.000000000000000000, 0.000000000000000000, -1.000000000000000000 ) ) ;
#13351=COLOUR_RGB ( '', 0.09019608, 0.27058824, 0.51372549) ;
#13352=EDGE_LOOP ( 'NONE', ( #56978, #69105, #49028, #7508 ) ) ;
#13354=DIRECTION ( 'NONE',  ( -0.000000000000000000, -1.000000000000000000, -0.000000000000000000 ) ) ;
#13363=EDGE_CURVE ( 'NONE', #4175, #3674, #23225, .T. ) ;
#13364=ORIENTED_EDGE ( 'NONE', *, *, #14226, .F. ) ;
#13365=FACE_OUTER_BOUND ( 'NONE', #43722, .T. ) ;
#13372=DIRECTION ( 'NONE',  ( 0.000000000000000000, 0.6691306063588592368, -0.7431448254773934670 ) ) ;
#13386=ORIENTED_EDGE ( 'NONE', *, *, #48167, .T. ) ;
#13400=ORIENTED_EDGE ( 'NONE', *, *, #33752, .F. ) ;
#13405=EDGE_LOOP ( 'NONE', ( #31380, #36789, #14883, #57577 ) ) ;
#13415=FILL_AREA_STYLE_COLOUR ( '', #7829 ) ;
#13426=AXIS2_PLACEMENT_3D ( 'NONE', #3242, #25101, #56774 ) ;
#13431=( NAMED_UNIT ( * ) PLANE_ANGLE_UNIT ( ) SI_UNIT ( $, .RADIAN. ) );
#13441=CIRCLE ( 'NONE', #1023, 5.000000000000000888 ) ;
#13450=FILL_AREA_STYLE ('',( #56734 ) ) ;
#13453=EDGE_LOOP ( 'NONE', ( #40457, #3566, #9454, #20309, #28493, #54675 ) ) ;
#13462=DIRECTION ( 'NONE',  ( 0.000000000000000000, -1.000000000000000000, 0.000000000000000000 ) ) ;
#13470=FILL_AREA_STYLE ('',( #61643 ) ) ;
#13477=ORIENTED_EDGE ( 'NONE', *, *, #15183, .F. ) ;
#13485=CIRCLE ( 'NONE', #26913, 16.00000000000000000 ) ;
#13505=CARTESIAN_POINT ( 'NONE',  ( 92.41620014002536720, 5.000000000000000000, -24.00402776293825369 ) ) ;
#13511=EDGE_CURVE ( 'NONE', #29168, #10038, #51821, .T. ) ;
#13512=FACE_OUTER_BOUND ( 'NONE', #8372, .T. ) ;
#13514=DIRECTION ( 'NONE',  ( 7.304098846218139598E-16, 0.000000000000000000, -1.000000000000000000 ) ) ;
#13520=DIRECTION ( 'NONE',  ( 1.300977106640434891E-16, 0.000000000000000000, 1.000000000000000000 ) ) ;
#13529=DIRECTION ( 'NONE',  ( 0.000000000000000000, 0.000000000000000000, -1.000000000000000000 ) ) ;
#13544=CARTESIAN_POINT ( 'NONE',  ( 6.750018943533633298, 42.91041480136897945, 27.90050555725692405 ) ) ;
#13548=ORIENTED_EDGE ( 'NONE', *, *, #49481, .T. ) ;
#13566=FILL_AREA_STYLE ('',( #3320 ) ) ;
#13573=VERTEX_POINT ( 'NONE', #3081 ) ;
#13575=ADVANCED_FACE ( 'NONE', ( #45747 ), #40811, .F. ) ;
#13577=CARTESIAN_POINT ( 'NONE',  ( 31.00000000000002132, 42.00000000000000000, 75.00000000000000000 ) ) ;
#13578=FACE_OUTER_BOUND ( 'NONE', #59220, .T. ) ;
#13584=ADVANCED_FACE ( 'NONE', ( #30546 ), #47329, .F. ) ;
#13588=SURFACE_STYLE_USAGE ( .BOTH. , #9026 ) ;
#13598=( NAMED_UNIT ( * ) SI_UNIT ( $, .STERADIAN. ) SOLID_ANGLE_UNIT ( ) );
#13610=( LENGTH_UNIT ( ) NAMED_UNIT ( * ) SI_UNIT ( .MILLI., .METRE. ) );
#13611=ORIENTED_EDGE ( 'NONE', *, *, #49053, .F. ) ;
#13614=SURFACE_STYLE_FILL_AREA ( #3011 ) ;
#13615=UNCERTAINTY_MEASURE_WITH_UNIT (LENGTH_MEASURE( 1.000000000000000082E-05 ), #16571, 'distance_accuracy_value', 'NONE');
#13623=PRESENTATION_STYLE_ASSIGNMENT (( #2685 ) ) ;
#13628=COLOUR_RGB ( '', 0.08235294, 0.09019608, 0.10196078) ;
#13630=VECTOR ( 'NONE', #60677, 1000.000000000000000 ) ;
#13639=EDGE_LOOP ( 'NONE', ( #15057, #12427, #48113, #32225 ) ) ;
#13642=SURFACE_SIDE_STYLE ('',( #68173 ) ) ;
#13659=( GEOMETRIC_REPRESENTATION_CONTEXT ( 3 ) GLOBAL_UNCERTAINTY_ASSIGNED_CONTEXT ( ( #59568 ) ) GLOBAL_UNIT_ASSIGNED_CONTEXT ( ( #52366, #61825, #24538 ) ) REPRESENTATION_CONTEXT ( 'NONE', 'WORKASPACE' ) );
#13663=ORIENTED_EDGE ( 'NONE', *, *, #56423, .T. ) ;
#13671=CARTESIAN_POINT ( 'NONE',  ( 27.00000000000001776, -60.04052944165106709, 34.49999999999999289 ) ) ;
#13676=COLOUR_RGB ( '', 0.08235294, 0.09019608, 0.10196078) ;
#13680=CIRCLE ( 'NONE', #58618, 1.000000000000000888 ) ;
#13682=DIRECTION ( 'NONE',  ( 0.000000000000000000, -0.000000000000000000, 1.000000000000000000 ) ) ;
#13684=FACE_OUTER_BOUND ( 'NONE', #46519, .T. ) ;
#13687=DIRECTION ( 'NONE',  ( 0.000000000000000000, 0.000000000000000000, -1.000000000000000000 ) ) ;
#13688=MECHANICAL_DESIGN_GEOMETRIC_PRESENTATION_REPRESENTATION('',(#12559),#4693);
#13689=PRESENTATION_STYLE_ASSIGNMENT (( #24239 ) ) ;
#13695=SURFACE_STYLE_USAGE ( .BOTH. , #14051 ) ;
#13696=UNCERTAINTY_MEASURE_WITH_UNIT (LENGTH_MEASURE( 1.000000000000000082E-05 ), #38964, 'distance_accuracy_value', 'NONE');
#13707=( NAMED_UNIT ( * ) PLANE_ANGLE_UNIT ( ) SI_UNIT ( $, .RADIAN. ) );
#13711=EDGE_CURVE ( 'NONE', #35184, #34574, #68916, .T. ) ;
#13713=CARTESIAN_POINT ( 'NONE',  ( 33.00000000000000000, 15.00000000000000000, -80.00402776293826435 ) ) ;
#13728=PRESENTATION_STYLE_ASSIGNMENT (( #40493 ) ) ;
#13735=VERTEX_POINT ( 'NONE', #1259 ) ;
#13754=UNCERTAINTY_MEASURE_WITH_UNIT (LENGTH_MEASURE( 1.000000000000000082E-05 ), #5820, 'distance_accuracy_value', 'NONE');
#13765=AXIS2_PLACEMENT_3D ( 'NONE', #41304, #30342, #36743 ) ;
#13778=SURFACE_SIDE_STYLE ('',( #23977 ) ) ;
#13786=UNCERTAINTY_MEASURE_WITH_UNIT (LENGTH_MEASURE( 1.000000000000000082E-05 ), #5457, 'distance_accuracy_value', 'NONE');
#13805=MECHANICAL_DESIGN_GEOMETRIC_PRESENTATION_REPRESENTATION('',(#64375),#60934);
#13825=EDGE_CURVE ( 'NONE', #19539, #29216, #38334, .T. ) ;
#13826=( NAMED_UNIT ( * ) SI_UNIT ( $, .STERADIAN. ) SOLID_ANGLE_UNIT ( ) );
#13830=( GEOMETRIC_REPRESENTATION_CONTEXT ( 3 ) GLOBAL_UNCERTAINTY_ASSIGNED_CONTEXT ( ( #41062 ) ) GLOBAL_UNIT_ASSIGNED_CONTEXT ( ( #47561, #58751, #43644 ) ) REPRESENTATION_CONTEXT ( 'NONE', 'WORKASPACE' ) );
#13832=CARTESIAN_POINT ( 'NONE',  ( 8.000000000000035527, 5.000000000000000000, 77.00402776293825013 ) ) ;
#13835=SURFACE_SIDE_STYLE ('',( #66963 ) ) ;
#13841=ORIENTED_EDGE ( 'NONE', *, *, #28157, .F. ) ;
#13842=ADVANCED_FACE ( 'NONE', ( #11879 ), #39336, .T. ) ;
#13847=DIRECTION ( 'NONE',  ( 1.000000000000000000, 0.000000000000000000, 4.625929269271505635E-16 ) ) ;
#13853=( NAMED_UNIT ( * ) SI_UNIT ( $, .STERADIAN. ) SOLID_ANGLE_UNIT ( ) );
#13857=CARTESIAN_POINT ( 'NONE',  ( 0.000000000000000000, 0.9999999999999991118, 79.00402776293826435 ) ) ;
#13858=DIRECTION ( 'NONE',  ( -1.000000000000000000, -0.000000000000000000, -0.000000000000000000 ) ) ;
#13870=MECHANICAL_DESIGN_GEOMETRIC_PRESENTATION_REPRESENTATION('',(#16157),#53202);
#13873=FACE_OUTER_BOUND ( 'NONE', #52064, .T. ) ;
#13875=STYLED_ITEM ( 'NONE', ( #56177 ), #61803 ) ;
#13876=CARTESIAN_POINT ( 'NONE',  ( 57.00000000000000000, 14.00000000000000000, 60.00402776293827145 ) ) ;
#13883=CIRCLE ( 'NONE', #43108, 1.000000000000000888 ) ;
#13894=ORIENTED_EDGE ( 'NONE', *, *, #14225, .T. ) ;
#13898=AXIS2_PLACEMENT_3D ( 'NONE', #8031, #46045, #29480 ) ;
#13907=EDGE_CURVE ( 'NONE', #1374, #53049, #62133, .T. ) ;
#13910=MECHANICAL_DESIGN_GEOMETRIC_PRESENTATION_REPRESENTATION('',(#4919),#25155);
#13923=EDGE_LOOP ( 'NONE', ( #46763, #48105, #64949, #59384 ) ) ;
#13929=DIRECTION ( 'NONE',  ( -1.300977106640434891E-16, 0.000000000000000000, -1.000000000000000000 ) ) ;
#13951=STYLED_ITEM ( 'NONE', ( #14137 ), #31262 ) ;
#13954=FILL_AREA_STYLE_COLOUR ( '', #8955 ) ;
#13960=PLANE ( 'NONE',  #22258 ) ;
#13961=CARTESIAN_POINT ( 'NONE',  ( 0.7152599553061413928, 42.96841831342781859, -45.59272038898399870 ) ) ;
#13966=ADVANCED_FACE ( 'NONE', ( #23816, #51955 ), #13960, .T. ) ;
#13968=CARTESIAN_POINT ( 'NONE',  ( 57.00000000000000000, 14.00000000000000000, -79.00402776293826435 ) ) ;
#13990=EDGE_CURVE ( 'NONE', #35716, #9757, #4784, .T. ) ;
#13994=DIRECTION ( 'NONE',  ( 0.000000000000000000, -0.000000000000000000, 1.000000000000000000 ) ) ;
#13997=CIRCLE ( 'NONE', #35347, 2.499999999999998668 ) ;
#14001=STYLED_ITEM ( 'NONE', ( #29154 ), #31599 ) ;
#14004=SURFACE_STYLE_USAGE ( .BOTH. , #13642 ) ;
#14005=( NAMED_UNIT ( * ) PLANE_ANGLE_UNIT ( ) SI_UNIT ( $, .RADIAN. ) );
#14010=CARTESIAN_POINT ( 'NONE',  ( 31.00000000000002132, 15.00000000000000000, 79.00402776293823592 ) ) ;
#14018=LINE ( 'NONE', #62875, #46336 ) ;
#14021=VERTEX_POINT ( 'NONE', #41771 ) ;
#14028=CARTESIAN_POINT ( 'NONE',  ( 57.00000000000000000, 16.00000000000000000, -72.50402776293826435 ) ) ;
#14042=SURFACE_SIDE_STYLE ('',( #52723 ) ) ;
#14043=SURFACE_SIDE_STYLE ('',( #24566 ) ) ;
#14044=COLOUR_RGB ( '', 0.08235294, 0.09019608, 0.10196078) ;
#14049=FILL_AREA_STYLE_COLOUR ( '', #44386 ) ;
#14051=SURFACE_SIDE_STYLE ('',( #3433 ) ) ;
#14052=VECTOR ( 'NONE', #3558, 1000.000000000000114 ) ;
#14067=LINE ( 'NONE', #67888, #63406 ) ;
#14070=AXIS2_PLACEMENT_3D ( 'NONE', #34292, #56083, #66288 ) ;
#14071=DIRECTION ( 'NONE',  ( 0.000000000000000000, 0.9396926207859082059, 0.3420201433256693790 ) ) ;
#14072=DIRECTION ( 'NONE',  ( 0.000000000000000000, 1.000000000000000000, 0.000000000000000000 ) ) ;
#14074=ORIENTED_EDGE ( 'NONE', *, *, #33430, .F. ) ;
#14081=CARTESIAN_POINT ( 'NONE',  ( 0.000000000000000000, 42.00000000000000000, -36.49999999999999289 ) ) ;
#14085=AXIS2_PLACEMENT_3D ( 'NONE', #44990, #23163, #17221 ) ;
#14089=CYLINDRICAL_SURFACE ( 'NONE', #20529, 5.000000000000004441 ) ;
#14109=CARTESIAN_POINT ( 'NONE',  ( 23.50000000000001776, 42.00000000000000000, -29.68999999999999417 ) ) ;
#14111=ORIENTED_EDGE ( 'NONE', *, *, #46454, .T. ) ;
#14118=LINE ( 'NONE', #51759, #30806 ) ;
#14119=ORIENTED_EDGE ( 'NONE', *, *, #33752, .T. ) ;
#14120=CARTESIAN_POINT ( 'NONE',  ( 1.000000000000000000, 42.00000000000000000, -79.00402776293826435 ) ) ;
#14124=DIRECTION ( 'NONE',  ( -1.000000000000000000, 0.000000000000000000, 0.000000000000000000 ) ) ;
#14126=LINE ( 'NONE', #9899, #10615 ) ;
#14132=( NAMED_UNIT ( * ) PLANE_ANGLE_UNIT ( ) SI_UNIT ( $, .RADIAN. ) );
#14137=PRESENTATION_STYLE_ASSIGNMENT (( #56699 ) ) ;
#14138=CIRCLE ( 'NONE', #59059, 5.000000000000004441 ) ;
#14169=CARTESIAN_POINT ( 'NONE',  ( 1.000000000000000000, 0.000000000000000000, -79.00402776293826435 ) ) ;
#14172=MECHANICAL_DESIGN_GEOMETRIC_PRESENTATION_REPRESENTATION('',(#60213),#50081);
#14196=ORIENTED_EDGE ( 'NONE', *, *, #64155, .T. ) ;
#14199=DIRECTION ( 'NONE',  ( -1.982541115402069054E-16, -0.000000000000000000, 1.000000000000000000 ) ) ;
#14225=EDGE_CURVE ( 'NONE', #41529, #30954, #29345, .T. ) ;
#14226=EDGE_CURVE ( 'NONE', #13735, #9516, #42534, .T. ) ;
#14227=( GEOMETRIC_REPRESENTATION_CONTEXT ( 3 ) GLOBAL_UNCERTAINTY_ASSIGNED_CONTEXT ( ( #24795 ) ) GLOBAL_UNIT_ASSIGNED_CONTEXT ( ( #24519, #19247, #63568 ) ) REPRESENTATION_CONTEXT ( 'NONE', 'WORKASPACE' ) );
#14228=CARTESIAN_POINT ( 'NONE',  ( 98.00000000000000000, 16.00000000000000000, 0.000000000000000000 ) ) ;
#14233=( NAMED_UNIT ( * ) PLANE_ANGLE_UNIT ( ) SI_UNIT ( $, .RADIAN. ) );
#14238=DIRECTION ( 'NONE',  ( 0.000000000000000000, 0.000000000000000000, -1.000000000000000000 ) ) ;
#14241=CARTESIAN_POINT ( 'NONE',  ( 3.000000000000002665, 43.00000000000000000, -90.00000000000000000 ) ) ;
#14243=ORIENTED_EDGE ( 'NONE', *, *, #45130, .F. ) ;
#14248=( NAMED_UNIT ( * ) PLANE_ANGLE_UNIT ( ) SI_UNIT ( $, .RADIAN. ) );
#14251=ORIENTED_EDGE ( 'NONE', *, *, #25060, .F. ) ;
#14252=( LENGTH_UNIT ( ) NAMED_UNIT ( * ) SI_UNIT ( .MILLI., .METRE. ) );
#14255=EDGE_CURVE ( 'NONE', #15573, #50024, #8267, .T. ) ;
#14261=( LENGTH_UNIT ( ) NAMED_UNIT ( * ) SI_UNIT ( .MILLI., .METRE. ) );
#14262=UNCERTAINTY_MEASURE_WITH_UNIT (LENGTH_MEASURE( 1.000000000000000082E-05 ), #2712, 'distance_accuracy_value', 'NONE');
#14264=PRESENTATION_STYLE_ASSIGNMENT (( #56119 ) ) ;
#14268=ORIENTED_EDGE ( 'NONE', *, *, #14255, .F. ) ;
#14269=AXIS2_PLACEMENT_3D ( 'NONE', #42355, #10301, #21174 ) ;
#14272=MECHANICAL_DESIGN_GEOMETRIC_PRESENTATION_REPRESENTATION('',(#5272),#62563);
#14285=CIRCLE ( 'NONE', #49120, 5.000000000000000888 ) ;
#14295=LINE ( 'NONE', #35057, #55195 ) ;
#14296=UNCERTAINTY_MEASURE_WITH_UNIT (LENGTH_MEASURE( 1.000000000000000082E-05 ), #11571, 'distance_accuracy_value', 'NONE');
#14302=LINE ( 'NONE', #25204, #39897 ) ;
#14308=( NAMED_UNIT ( * ) PLANE_ANGLE_UNIT ( ) SI_UNIT ( $, .RADIAN. ) );
#14312=SURFACE_SIDE_STYLE ('',( #46365 ) ) ;
#14313=VECTOR ( 'NONE', #9540, 1000.000000000000000 ) ;
#14318=CARTESIAN_POINT ( 'NONE',  ( 32.00000000000000000, 50.00000000000000000, -60.00000000000000711 ) ) ;
#14327=CARTESIAN_POINT ( 'NONE',  ( 22.00000000000002132, 43.00000000000000000, 90.00000000000000000 ) ) ;
#14334=ORIENTED_EDGE ( 'NONE', *, *, #46016, .T. ) ;
#14337=( LENGTH_UNIT ( ) NAMED_UNIT ( * ) SI_UNIT ( .MILLI., .METRE. ) );
#14339=FACE_OUTER_BOUND ( 'NONE', #62496, .T. ) ;
#14349=MECHANICAL_DESIGN_GEOMETRIC_PRESENTATION_REPRESENTATION('',(#3047),#44733);
#14351=LINE ( 'NONE', #3406, #47451 ) ;
#14355=CARTESIAN_POINT ( 'NONE',  ( 30.99999999999999289, 5.000000000000000000, 24.00402776293822171 ) ) ;
#14361=FACE_OUTER_BOUND ( 'NONE', #16868, .T. ) ;
#14368=( NAMED_UNIT ( * ) SI_UNIT ( $, .STERADIAN. ) SOLID_ANGLE_UNIT ( ) );
#14378=EDGE_CURVE ( 'NONE', #24720, #20026, #31779, .T. ) ;
#14379=CARTESIAN_POINT ( 'NONE',  ( 23.50000000000001776, 43.00000000000000000, 29.68999999999999417 ) ) ;
#14390=EDGE_LOOP ( 'NONE', ( #27952, #32551, #19073, #30085 ) ) ;
#14420=UNCERTAINTY_MEASURE_WITH_UNIT (LENGTH_MEASURE( 1.000000000000000082E-05 ), #12066, 'distance_accuracy_value', 'NONE');
#14422=VECTOR ( 'NONE', #48593, 1000.000000000000000 ) ;
#14425=ORIENTED_EDGE ( 'NONE', *, *, #42722, .T. ) ;
#14434=STYLED_ITEM ( 'NONE', ( #30623 ), #43263 ) ;
#14440=CARTESIAN_POINT ( 'NONE',  ( 27.00000000000001776, 42.00000000000000000, -36.50000000000000000 ) ) ;
#14446=ORIENTED_EDGE ( 'NONE', *, *, #40871, .F. ) ;
#14449=EDGE_CURVE ( 'NONE', #45721, #57515, #15990, .T. ) ;
#14451=SURFACE_STYLE_FILL_AREA ( #42298 ) ;
#14453=VECTOR ( 'NONE', #21017, 1000.000000000000000 ) ;
#14457=DIRECTION ( 'NONE',  ( 8.391040747885011388E-17, 0.7641995406119433953, 0.6449798928094538919 ) ) ;
#14458=SURFACE_STYLE_FILL_AREA ( #53156 ) ;
#14459=COLOUR_RGB ( '', 0.40784314, 0.44705882, 0.49803922) ;
#14466=DIRECTION ( 'NONE',  ( 0.000000000000000000, -1.000000000000000000, -0.000000000000000000 ) ) ;
#14478=EDGE_LOOP ( 'NONE', ( #40305, #10120, #43944 ) ) ;
#14486=PRESENTATION_STYLE_ASSIGNMENT (( #19769 ) ) ;
#14490=ORIENTED_EDGE ( 'NONE', *, *, #44972, .T. ) ;
#14495=MECHANICAL_DESIGN_GEOMETRIC_PRESENTATION_REPRESENTATION('',(#15630),#30193);
#14496=SURFACE_STYLE_FILL_AREA ( #4630 ) ;
#14500=ADVANCED_FACE ( 'NONE', ( #57480 ), #68360, .T. ) ;
#14502=DIRECTION ( 'NONE',  ( 0.000000000000000000, -1.000000000000000000, 0.000000000000000000 ) ) ;
#14527=( LENGTH_UNIT ( ) NAMED_UNIT ( * ) SI_UNIT ( .MILLI., .METRE. ) );
#14535=( NAMED_UNIT ( * ) SI_UNIT ( $, .STERADIAN. ) SOLID_ANGLE_UNIT ( ) );
#14538=EDGE_CURVE ( 'NONE', #26431, #57943, #27168, .T. ) ;
#14540=PRESENTATION_STYLE_ASSIGNMENT (( #24390 ) ) ;
#14541=ORIENTED_EDGE ( 'NONE', *, *, #57522, .F. ) ;
#14543=DIRECTION ( 'NONE',  ( 0.000000000000000000, 1.000000000000000000, 0.000000000000000000 ) ) ;
#14549=CARTESIAN_POINT ( 'NONE',  ( 24.70577775730028236, 25.82240647180052662, -27.50000000000001421 ) ) ;
#14554=DIRECTION ( 'NONE',  ( -1.000000000000000000, -0.000000000000000000, -0.000000000000000000 ) ) ;
#14556=EDGE_LOOP ( 'NONE', ( #68097, #41648, #55175 ) ) ;
#14577=CARTESIAN_POINT ( 'NONE',  ( 32.00000000000000000, 43.00000000000000000, -80.00402776293826435 ) ) ;
#14582=TOROIDAL_SURFACE ( 'NONE', #19075, 111.0000000000000142, 1.000000000000000000 ) ;
#14584=VERTEX_POINT ( 'NONE', #54614 ) ;
#14591=DIRECTION ( 'NONE',  ( -0.000000000000000000, -1.000000000000000000, -0.000000000000000000 ) ) ;
#14613=FILL_AREA_STYLE_COLOUR ( '', #61529 ) ;
#14616=ORIENTED_EDGE ( 'NONE', *, *, #485, .F. ) ;
#14625=COLOUR_RGB ( '', 0.66274510, 0.83137255, 0.94901961) ;
#14656=FILL_AREA_STYLE ('',( #51947 ) ) ;
#14660=STYLED_ITEM ( 'NONE', ( #30741 ), #21188 ) ;
#14665=CARTESIAN_POINT ( 'NONE',  ( 0.8561458320465512584, 43.00000000000000711, -45.61250543006185154 ) ) ;
#14666=CIRCLE ( 'NONE', #60678, 1.000000000000000888 ) ;
#14667=DIRECTION ( 'NONE',  ( 0.000000000000000000, 0.000000000000000000, -1.000000000000000000 ) ) ;
#14668=FACE_OUTER_BOUND ( 'NONE', #23712, .T. ) ;
#14673=CARTESIAN_POINT ( 'NONE',  ( 26.00000000000001776, 42.00000000000000000, -29.68999999999999417 ) ) ;
#14675=ORIENTED_EDGE ( 'NONE', *, *, #47560, .F. ) ;
#14678=COLOUR_RGB ( '', 0.40784314, 0.44705882, 0.49803922) ;
#14684=ORIENTED_EDGE ( 'NONE', *, *, #62802, .F. ) ;
#14691=ORIENTED_EDGE ( 'NONE', *, *, #17368, .T. ) ;
#14696=ORIENTED_EDGE ( 'NONE', *, *, #45785, .T. ) ;
#14697=( LENGTH_UNIT ( ) NAMED_UNIT ( * ) SI_UNIT ( .MILLI., .METRE. ) );
#14698=SURFACE_STYLE_FILL_AREA ( #4099 ) ;
#14701=STYLED_ITEM ( 'NONE', ( #28448 ), #12291 ) ;
#14709=AXIS2_PLACEMENT_3D ( 'NONE', #1088, #38847, #65534 ) ;
#14711=ORIENTED_EDGE ( 'NONE', *, *, #1698, .T. ) ;
#14737=FACE_OUTER_BOUND ( 'NONE', #18592, .T. ) ;
#14738=AXIS2_PLACEMENT_3D ( 'NONE', #21304, #36843, #42825 ) ;
#14751=( NAMED_UNIT ( * ) SI_UNIT ( $, .STERADIAN. ) SOLID_ANGLE_UNIT ( ) );
#14770=DIRECTION ( 'NONE',  ( 6.938893903907233900E-15, -0.4705882352941119229, 0.8823529411764736707 ) ) ;
#14771=( NAMED_UNIT ( * ) PLANE_ANGLE_UNIT ( ) SI_UNIT ( $, .RADIAN. ) );
#14793=CARTESIAN_POINT ( 'NONE',  ( 2.000000000000022204, 50.00000000000000000, 55.00000000000000711 ) ) ;
#14798=EDGE_CURVE ( 'NONE', #42205, #39971, #59961, .T. ) ;
#14801=DIRECTION ( 'NONE',  ( -0.000000000000000000, -1.000000000000000000, -0.000000000000000000 ) ) ;
#14808=ADVANCED_FACE ( 'NONE', ( #32898, #53325, #17087, #16404, #27585, #11777, #26555 ), #49102, .T. ) ;
#14820=CARTESIAN_POINT ( 'NONE',  ( 23.06857045728888522, 24.64236968870869404, 27.22624481166502264 ) ) ;
#14824=VERTEX_POINT ( 'NONE', #18452 ) ;
#14831=ORIENTED_EDGE ( 'NONE', *, *, #25060, .T. ) ;
#14834=( LENGTH_UNIT ( ) NAMED_UNIT ( * ) SI_UNIT ( .MILLI., .METRE. ) );
#14840=TOROIDAL_SURFACE ( 'NONE', #15961, 24.00000000000001421, 1.000000000000000000 ) ;
#14851=( LENGTH_UNIT ( ) NAMED_UNIT ( * ) SI_UNIT ( .MILLI., .METRE. ) );
#14862=VECTOR ( 'NONE', #5478, 1000.000000000000000 ) ;
#14864=ORIENTED_EDGE ( 'NONE', *, *, #29228, .F. ) ;
#14878=ADVANCED_FACE ( 'NONE', ( #34275 ), #56777, .T. ) ;
#14883=ORIENTED_EDGE ( 'NONE', *, *, #6342, .F. ) ;
#14886=DIRECTION ( 'NONE',  ( -0.000000000000000000, -1.000000000000000000, -0.000000000000000000 ) ) ;
#14896=CARTESIAN_POINT ( 'NONE',  ( 2.999999999999990230, 0.000000000000000000, 37.00402776293829277 ) ) ;
#14900=CARTESIAN_POINT ( 'NONE',  ( 32.00000000000001421, 42.00000000000000711, 44.99999999999998579 ) ) ;
#14910=ORIENTED_EDGE ( 'NONE', *, *, #12624, .F. ) ;
#14924=FILL_AREA_STYLE_COLOUR ( '', #65135 ) ;
#14930=EDGE_CURVE ( 'NONE', #3143, #41012, #2906, .T. ) ;
#14933=CARTESIAN_POINT ( 'NONE',  ( 28.58578643762690419, 42.99999999999999289, -79.58981420056515788 ) ) ;
#14948=PRESENTATION_STYLE_ASSIGNMENT (( #63107 ) ) ;
#14960=VECTOR ( 'NONE', #46290, 1000.000000000000000 ) ;
#14961=CARTESIAN_POINT ( 'NONE',  ( 22.99999999999995026, 5.000000000000000000, 77.00402776293825013 ) ) ;
#14969=CARTESIAN_POINT ( 'NONE',  ( 27.00000000000001776, 15.00000000000000000, 34.49999999999999289 ) ) ;
#14970=ORIENTED_EDGE ( 'NONE', *, *, #46279, .T. ) ;
#14974=( NAMED_UNIT ( * ) PLANE_ANGLE_UNIT ( ) SI_UNIT ( $, .RADIAN. ) );
#14975=COLOUR_RGB ( '', 0.66274510, 0.83137255, 0.94901961) ;
#14976=EDGE_CURVE ( 'NONE', #56887, #65467, #41313, .T. ) ;
#14990=CARTESIAN_POINT ( 'NONE',  ( 25.00000000000001421, 43.00000000000000000, 34.49999999999999289 ) ) ;
#14996=( NAMED_UNIT ( * ) PLANE_ANGLE_UNIT ( ) SI_UNIT ( $, .RADIAN. ) );
#15009=CARTESIAN_POINT ( 'NONE',  ( 22.99999999999999645, 5.000000000000000000, -72.00402776293825013 ) ) ;
#15011=( NAMED_UNIT ( * ) PLANE_ANGLE_UNIT ( ) SI_UNIT ( $, .RADIAN. ) );
#15015=CIRCLE ( 'NONE', #2577, 1.000000000000000888 ) ;
#15018=EDGE_CURVE ( 'NONE', #10014, #9623, #9981, .T. ) ;
#15028=STYLED_ITEM ( 'NONE', ( #14948 ), #37626 ) ;
#15041=EDGE_CURVE ( 'NONE', #20378, #15573, #48251, .T. ) ;
#15047=SURFACE_STYLE_USAGE ( .BOTH. , #52657 ) ;
#15049=DIRECTION ( 'NONE',  ( 0.000000000000000000, 1.000000000000000000, 0.000000000000000000 ) ) ;
#15051=CIRCLE ( 'NONE', #38668, 4.999999999999997335 ) ;
#15057=ORIENTED_EDGE ( 'NONE', *, *, #27021, .F. ) ;
#15062=EDGE_LOOP ( 'NONE', ( #53841, #65548, #38839, #27181, #40520 ) ) ;
#15066=ADVANCED_FACE ( 'NONE', ( #54601 ), #38487, .F. ) ;
#15079=CARTESIAN_POINT ( 'NONE',  ( 26.00000000000001776, 15.00000000000000000, 35.50000000000000000 ) ) ;
#15092=CARTESIAN_POINT ( 'NONE',  ( 107.0858988931383777, 5.000000000000000000, -16.89933289725613363 ) ) ;
#15094=CARTESIAN_POINT ( 'NONE',  ( 36.00000000000002842, 5.000000000000000000, -32.00402776293825724 ) ) ;
#15099=AXIS2_PLACEMENT_3D ( 'NONE', #28914, #67618, #66214 ) ;
#15101=ORIENTED_EDGE ( 'NONE', *, *, #61932, .T. ) ;
#15109=STYLED_ITEM ( 'NONE', ( #42811 ), #26993 ) ;
#15121=AXIS2_PLACEMENT_3D ( 'NONE', #39273, #59995, #1187 ) ;
#15125=UNCERTAINTY_MEASURE_WITH_UNIT (LENGTH_MEASURE( 1.000000000000000082E-05 ), #41508, 'distance_accuracy_value', 'NONE');
#15136=ORIENTED_EDGE ( 'NONE', *, *, #4689, .T. ) ;
#15141=MECHANICAL_DESIGN_GEOMETRIC_PRESENTATION_REPRESENTATION('',(#14001),#65660);
#15142=PRESENTATION_STYLE_ASSIGNMENT (( #41875 ) ) ;
#15158=( GEOMETRIC_REPRESENTATION_CONTEXT ( 3 ) GLOBAL_UNCERTAINTY_ASSIGNED_CONTEXT ( ( #68689 ) ) GLOBAL_UNIT_ASSIGNED_CONTEXT ( ( #14834, #52816, #44367 ) ) REPRESENTATION_CONTEXT ( 'NONE', 'WORKASPACE' ) );
#15160=VECTOR ( 'NONE', #69221, 1000.000000000000000 ) ;
#15183=EDGE_CURVE ( 'NONE', #65559, #62752, #56327, .T. ) ;
#15209=ADVANCED_FACE ( 'NONE', ( #24323 ), #62996, .F. ) ;
#15220=SURFACE_STYLE_FILL_AREA ( #41589 ) ;
#15232=EDGE_CURVE ( 'NONE', #13259, #23198, #57032, .T. ) ;
#15239=FACE_OUTER_BOUND ( 'NONE', #49577, .T. ) ;
#15240=FILL_AREA_STYLE ('',( #8549 ) ) ;
#15248=DIRECTION ( 'NONE',  ( -0.000000000000000000, 0.3420201433256694346, 0.9396926207859082059 ) ) ;
#15249=ORIENTED_EDGE ( 'NONE', *, *, #10042, .F. ) ;
#15251=UNCERTAINTY_MEASURE_WITH_UNIT (LENGTH_MEASURE( 1.000000000000000082E-05 ), #14851, 'distance_accuracy_value', 'NONE');
#15254=DIRECTION ( 'NONE',  ( -1.000000000000000000, 0.000000000000000000, 0.000000000000000000 ) ) ;
#15256=SURFACE_SIDE_STYLE ('',( #42004 ) ) ;
#15259=EDGE_LOOP ( 'NONE', ( #37149, #57746, #62306, #46864 ) ) ;
#15267=ORIENTED_EDGE ( 'NONE', *, *, #66636, .F. ) ;
#15272=EDGE_LOOP ( 'NONE', ( #53429, #1019, #29915, #1336 ) ) ;
#15273=FILL_AREA_STYLE_COLOUR ( '', #49689 ) ;
#15277=PLANE ( 'NONE',  #13765 ) ;
#15280=FILL_AREA_STYLE_COLOUR ( '', #998 ) ;
#15283=( NAMED_UNIT ( * ) SI_UNIT ( $, .STERADIAN. ) SOLID_ANGLE_UNIT ( ) );
#15286=AXIS2_PLACEMENT_3D ( 'NONE', #34140, #17967, #44054 ) ;
#15304=( LENGTH_UNIT ( ) NAMED_UNIT ( * ) SI_UNIT ( .MILLI., .METRE. ) );
#15305=ADVANCED_FACE ( 'NONE', ( #3889, #53495 ), #48605, .T. ) ;
#15308=VERTEX_POINT ( 'NONE', #4223 ) ;
#15316=DIRECTION ( 'NONE',  ( -0.000000000000000000, -1.000000000000000000, -0.000000000000000000 ) ) ;
#15332=DIRECTION ( 'NONE',  ( 0.000000000000000000, 0.3420201433256629953, -0.9396926207859104263 ) ) ;
#15334=DIRECTION ( 'NONE',  ( -1.000000000000000000, 0.000000000000000000, 0.000000000000000000 ) ) ;
#15337=MECHANICAL_DESIGN_GEOMETRIC_PRESENTATION_REPRESENTATION('',(#17583),#19815);
#15347=CARTESIAN_POINT ( 'NONE',  ( 92.41620014002536720, 5.000000000000000000, 29.00402776293826079 ) ) ;
#15348=DIRECTION ( 'NONE',  ( -1.000000000000000000, 0.000000000000000000, -0.000000000000000000 ) ) ;
#15354=( LENGTH_UNIT ( ) NAMED_UNIT ( * ) SI_UNIT ( .MILLI., .METRE. ) );
#15360=DIRECTION ( 'NONE',  ( 0.000000000000000000, 1.000000000000000000, -0.000000000000000000 ) ) ;
#15361=PRODUCT_DEFINITION_SHAPE ( 'NONE', 'NONE',  #29610 ) ;
#15362=ORIENTED_EDGE ( 'NONE', *, *, #26440, .F. ) ;
#15367=FILL_AREA_STYLE_COLOUR ( '', #65840 ) ;
#15390=DIRECTION ( 'NONE',  ( 0.000000000000000000, 0.000000000000000000, -1.000000000000000000 ) ) ;
#15391=CARTESIAN_POINT ( 'NONE',  ( 29.00000000000002842, 0.000000000000000000, 3.902931319921305165E-16 ) ) ;
#15395=( NAMED_UNIT ( * ) SI_UNIT ( $, .STERADIAN. ) SOLID_ANGLE_UNIT ( ) );
#15398=SURFACE_SIDE_STYLE ('',( #9054 ) ) ;
#15399=ORIENTED_EDGE ( 'NONE', *, *, #24584, .T. ) ;
#15401=VECTOR ( 'NONE', #36471, 1000.000000000000000 ) ;
#15402=CARTESIAN_POINT ( 'NONE',  ( 27.99999999999999289, 43.00000000000000000, -90.00000000000000000 ) ) ;
#15403=FILL_AREA_STYLE_COLOUR ( '', #61223 ) ;
#15405=VERTEX_POINT ( 'NONE', #60472 ) ;
#15409=FACE_OUTER_BOUND ( 'NONE', #28416, .T. ) ;
#15428=( LENGTH_UNIT ( ) NAMED_UNIT ( * ) SI_UNIT ( .MILLI., .METRE. ) );
#15436=FILL_AREA_STYLE ('',( #57269 ) ) ;
#15447=VERTEX_POINT ( 'NONE', #6326 ) ;
#15449=PLANE ( 'NONE',  #36983 ) ;
#15463=DIRECTION ( 'NONE',  ( 0.000000000000000000, 0.000000000000000000, -1.000000000000000000 ) ) ;
#15466=ORIENTED_EDGE ( 'NONE', *, *, #57141, .F. ) ;
#15468=( LENGTH_UNIT ( ) NAMED_UNIT ( * ) SI_UNIT ( .MILLI., .METRE. ) );
#15470=( LENGTH_UNIT ( ) NAMED_UNIT ( * ) SI_UNIT ( .MILLI., .METRE. ) );
#15478=CYLINDRICAL_SURFACE ( 'NONE', #68746, 12.50000000000001066 ) ;
#15479=SURFACE_STYLE_USAGE ( .BOTH. , #5221 ) ;
#15481=EDGE_LOOP ( 'NONE', ( #24989, #5676, #60691, #43199 ) ) ;
#15483=ORIENTED_EDGE ( 'NONE', *, *, #38592, .F. ) ;
#15491=DIRECTION ( 'NONE',  ( 0.000000000000000000, 0.000000000000000000, -1.000000000000000000 ) ) ;
#15493=ORIENTED_EDGE ( 'NONE', *, *, #57446, .F. ) ;
#15499=ORIENTED_EDGE ( 'NONE', *, *, #31477, .T. ) ;
#15516=CARTESIAN_POINT ( 'NONE',  ( 28.00000000000002842, 43.00000000000000000, 0.000000000000000000 ) ) ;
#15521=CARTESIAN_POINT ( 'NONE',  ( 22.83826606206589815, 27.22759712782712072, 27.27819404924646207 ) ) ;
#15525=ORIENTED_EDGE ( 'NONE', *, *, #43877, .F. ) ;
#15526=PRESENTATION_STYLE_ASSIGNMENT (( #10914 ) ) ;
#15529=DIRECTION ( 'NONE',  ( -0.000000000000000000, -1.000000000000000000, -0.000000000000000000 ) ) ;
#15533=EDGE_CURVE ( 'NONE', #15954, #42614, #67157, .T. ) ;
#15555=ORIENTED_EDGE ( 'NONE', *, *, #63233, .F. ) ;
#15562=CARTESIAN_POINT ( 'NONE',  ( 57.00000000000000000, 0.000000000000000000, -65.00402776293825013 ) ) ;
#15565=ORIENTED_EDGE ( 'NONE', *, *, #36629, .T. ) ;
#15570=ORIENTED_EDGE ( 'NONE', *, *, #25115, .F. ) ;
#15573=VERTEX_POINT ( 'NONE', #19659 ) ;
#15580=COLOUR_RGB ( '', 0.09019608, 0.27058824, 0.51372549) ;
#15583=ADVANCED_FACE ( 'NONE', ( #9121 ), #67497, .T. ) ;
#15591=CARTESIAN_POINT ( 'NONE',  ( 31.64575758289396745, 42.77450929379339328, 45.47201693779177134 ) ) ;
#15600=CIRCLE ( 'NONE', #63864, 1.000000000000001998 ) ;
#15601=SURFACE_STYLE_FILL_AREA ( #43056 ) ;
#15605=ORIENTED_EDGE ( 'NONE', *, *, #13511, .T. ) ;
#15607=FILL_AREA_STYLE_COLOUR ( '', #7772 ) ;
#15610=FILL_AREA_STYLE_COLOUR ( '', #33932 ) ;
#15615=VERTEX_POINT ( 'NONE', #16146 ) ;
#15618=DIRECTION ( 'NONE',  ( 0.000000000000000000, -0.000000000000000000, -1.000000000000000000 ) ) ;
#15628=CARTESIAN_POINT ( 'NONE',  ( 1.000000000000000000, 42.00000000000000000, -79.00402776293826435 ) ) ;
#15630=STYLED_ITEM ( 'NONE', ( #64332 ), #10190 ) ;
#15632=PRESENTATION_STYLE_ASSIGNMENT (( #53265 ) ) ;
#15636=MECHANICAL_DESIGN_GEOMETRIC_PRESENTATION_REPRESENTATION('',(#17868),#54904);
#15637=CARTESIAN_POINT ( 'NONE',  ( 31.00000000000001421, 14.00000000000000000, 36.49999999999999289 ) ) ;
#15638=( LENGTH_UNIT ( ) NAMED_UNIT ( * ) SI_UNIT ( .MILLI., .METRE. ) );
#15641=DIRECTION ( 'NONE',  ( 0.7681514953298232973, -6.664128951862614066E-15, 0.6402681315062906942 ) ) ;
#15646=SURFACE_SIDE_STYLE ('',( #63799 ) ) ;
#15658=FILL_AREA_STYLE_COLOUR ( '', #26022 ) ;
#15661=FACE_OUTER_BOUND ( 'NONE', #28640, .T. ) ;
#15680=EDGE_CURVE ( 'NONE', #18052, #61901, #885, .T. ) ;
#15681=( GEOMETRIC_REPRESENTATION_CONTEXT ( 3 ) GLOBAL_UNCERTAINTY_ASSIGNED_CONTEXT ( ( #17326 ) ) GLOBAL_UNIT_ASSIGNED_CONTEXT ( ( #67704, #19499, #36435 ) ) REPRESENTATION_CONTEXT ( 'NONE', 'WORKASPACE' ) );
#15684=CIRCLE ( 'NONE', #21266, 4.999999999999997335 ) ;
#15686=DIRECTION ( 'NONE',  ( 0.000000000000000000, 0.000000000000000000, -1.000000000000000000 ) ) ;
#15698=CIRCLE ( 'NONE', #48356, 1.000000000000001110 ) ;
#15700=FACE_OUTER_BOUND ( 'NONE', #7653, .T. ) ;
#15707=CARTESIAN_POINT ( 'NONE',  ( 3.000000000000030198, 34.80256050929376954, 80.00402776293826435 ) ) ;
#15716=COLOUR_RGB ( '', 0.09019608, 0.27058824, 0.51372549) ;
#15720=FILL_AREA_STYLE_COLOUR ( '', #65581 ) ;
#15721=COLOUR_RGB ( '', 0.08235294, 0.09019608, 0.10196078) ;
#15723=DIRECTION ( 'NONE',  ( 0.000000000000000000, 1.000000000000000000, -0.000000000000000000 ) ) ;
#15734=PRESENTATION_STYLE_ASSIGNMENT (( #20290 ) ) ;
#15736=ORIENTED_EDGE ( 'NONE', *, *, #18413, .F. ) ;
#15745=EDGE_CURVE ( 'NONE', #23974, #67099, #18028, .T. ) ;
#15754=ADVANCED_FACE ( 'NONE', ( #59344 ), #48863, .T. ) ;
#15756=( NAMED_UNIT ( * ) SI_UNIT ( $, .STERADIAN. ) SOLID_ANGLE_UNIT ( ) );
#15759=EDGE_LOOP ( 'NONE', ( #29082, #64326, #15525, #56317 ) ) ;
#15760=SURFACE_STYLE_FILL_AREA ( #38625 ) ;
#15782=COLOUR_RGB ( '', 0.31764706, 0.68627451, 0.89019608) ;
#15784=( LENGTH_UNIT ( ) NAMED_UNIT ( * ) SI_UNIT ( .MILLI., .METRE. ) );
#15789=DIRECTION ( 'NONE',  ( 0.000000000000000000, -1.000000000000000000, 0.000000000000000000 ) ) ;
#15795=( GEOMETRIC_REPRESENTATION_CONTEXT ( 3 ) GLOBAL_UNCERTAINTY_ASSIGNED_CONTEXT ( ( #58032 ) ) GLOBAL_UNIT_ASSIGNED_CONTEXT ( ( #51349, #13707, #68227 ) ) REPRESENTATION_CONTEXT ( 'NONE', 'WORKASPACE' ) );
#15805=STYLED_ITEM ( 'NONE', ( #3705 ), #69613 ) ;
#15817=( NAMED_UNIT ( * ) PLANE_ANGLE_UNIT ( ) SI_UNIT ( $, .RADIAN. ) );
#15826=ADVANCED_FACE ( 'NONE', ( #51248 ), #56871, .T. ) ;
#15832=CARTESIAN_POINT ( 'NONE',  ( 57.00000000000000000, 16.00000000000000000, 60.00402776293825724 ) ) ;
#15843=UNCERTAINTY_MEASURE_WITH_UNIT (LENGTH_MEASURE( 1.000000000000000082E-05 ), #14527, 'distance_accuracy_value', 'NONE');
#15845=CARTESIAN_POINT ( 'NONE',  ( 82.09357085539566867, 5.000000000000000000, -32.00402776293823592 ) ) ;
#15857=UNCERTAINTY_MEASURE_WITH_UNIT (LENGTH_MEASURE( 1.000000000000000082E-05 ), #2658, 'distance_accuracy_value', 'NONE');
#15858=VECTOR ( 'NONE', #40041, 1000.000000000000000 ) ;
#15864=VERTEX_POINT ( 'NONE', #13240 ) ;
#15868=ORIENTED_EDGE ( 'NONE', *, *, #65445, .F. ) ;
#15870=PRESENTATION_STYLE_ASSIGNMENT (( #59789 ) ) ;
#15875=STYLED_ITEM ( 'NONE', ( #1893 ), #45663 ) ;
#15878=( LENGTH_UNIT ( ) NAMED_UNIT ( * ) SI_UNIT ( .MILLI., .METRE. ) );
#15879=STYLED_ITEM ( 'NONE', ( #13336 ), #13584 ) ;
#15884=( NAMED_UNIT ( * ) PLANE_ANGLE_UNIT ( ) SI_UNIT ( $, .RADIAN. ) );
#15887=UNCERTAINTY_MEASURE_WITH_UNIT (LENGTH_MEASURE( 1.000000000000000082E-05 ), #33268, 'distance_accuracy_value', 'NONE');
#15897=DIRECTION ( 'NONE',  ( 0.000000000000000000, 1.000000000000000000, 0.000000000000000000 ) ) ;
#15899=LINE ( 'NONE', #16932, #28434 ) ;
#15905=DIRECTION ( 'NONE',  ( 0.000000000000000000, -1.000000000000000000, 0.000000000000000000 ) ) ;
#15907=ADVANCED_FACE ( 'NONE', ( #68130 ), #43438, .T. ) ;
#15918=FACE_OUTER_BOUND ( 'NONE', #54653, .T. ) ;
#15921=SURFACE_STYLE_FILL_AREA ( #69366 ) ;
#15928=EDGE_CURVE ( 'NONE', #23835, #1731, #46775, .T. ) ;
#15936=PRESENTATION_STYLE_ASSIGNMENT (( #6719 ) ) ;
#15938=CIRCLE ( 'NONE', #63097, 4.999999999999997335 ) ;
#15940=( GEOMETRIC_REPRESENTATION_CONTEXT ( 3 ) GLOBAL_UNCERTAINTY_ASSIGNED_CONTEXT ( ( #6115 ) ) GLOBAL_UNIT_ASSIGNED_CONTEXT ( ( #58706, #14771, #5220 ) ) REPRESENTATION_CONTEXT ( 'NONE', 'WORKASPACE' ) );
#15942=ORIENTED_EDGE ( 'NONE', *, *, #52226, .F. ) ;
#15946=STYLED_ITEM ( 'NONE', ( #27024 ), #35453 ) ;
#15954=VERTEX_POINT ( 'NONE', #59888 ) ;
#15956=FACE_OUTER_BOUND ( 'NONE', #57506, .T. ) ;
#15961=AXIS2_PLACEMENT_3D ( 'NONE', #34342, #60705, #49837 ) ;
#15964=EDGE_CURVE ( 'NONE', #47636, #1286, #11705, .T. ) ;
#15985=COLOUR_RGB ( '', 0.40784314, 0.44705882, 0.49803922) ;
#15987=DIRECTION ( 'NONE',  ( 0.000000000000000000, 0.000000000000000000, -1.000000000000000000 ) ) ;
#15990=LINE ( 'NONE', #9669, #11044 ) ;
#15999=MECHANICAL_DESIGN_GEOMETRIC_PRESENTATION_REPRESENTATION('',(#54105),#45177);
#16010=AXIS2_PLACEMENT_3D ( 'NONE', #9634, #4292, #68715 ) ;
#16011=ORIENTED_EDGE ( 'NONE', *, *, #61318, .T. ) ;
#16019=EDGE_CURVE ( 'NONE', #41524, #66584, #3270, .T. ) ;
#16021=FILL_AREA_STYLE ('',( #21240 ) ) ;
#16027=ORIENTED_EDGE ( 'NONE', *, *, #41616, .F. ) ;
#16030=CARTESIAN_POINT ( 'NONE',  ( 6.414213562373110022, 17.78868675966042190, -3.144186300207962859E-15 ) ) ;
#16031=( LENGTH_UNIT ( ) NAMED_UNIT ( * ) SI_UNIT ( .MILLI., .METRE. ) );
#16036=ORIENTED_EDGE ( 'NONE', *, *, #30550, .F. ) ;
#16040=CARTESIAN_POINT ( 'NONE',  ( 57.00000000000000000, 5.000000000000000000, 60.00402776293825724 ) ) ;
#16081=PLANE ( 'NONE',  #68971 ) ;
#16082=CARTESIAN_POINT ( 'NONE',  ( 31.00000000000001421, -60.04052944165106709, 35.50000000000000000 ) ) ;
#16085=EDGE_CURVE ( 'NONE', #49984, #54537, #56337, .T. ) ;
#16094=CARTESIAN_POINT ( 'NONE',  ( 4.000000000000001776, 34.36176364315826248, -80.00402776293826435 ) ) ;
#16095=EDGE_CURVE ( 'NONE', #49856, #23486, #38160, .T. ) ;
#16114=ORIENTED_EDGE ( 'NONE', *, *, #6655, .F. ) ;
#16121=PLANE ( 'NONE',  #58959 ) ;
#16124=LINE ( 'NONE', #37601, #247 ) ;
#16130=DIRECTION ( 'NONE',  ( -1.156482317317870739E-15, 0.000000000000000000, -1.000000000000000000 ) ) ;
#16142=SURFACE_SIDE_STYLE ('',( #63264 ) ) ;
#16143=AXIS2_PLACEMENT_3D ( 'NONE', #26335, #47876, #21069 ) ;
#16146=CARTESIAN_POINT ( 'NONE',  ( 30.99999999999999289, 0.000000000000000000, 37.00402776293829277 ) ) ;
#16151=EDGE_CURVE ( 'NONE', #49912, #56811, #40547, .T. ) ;
#16152=CARTESIAN_POINT ( 'NONE',  ( 30.99999999999999289, 0.000000000000000000, 24.00402776293822171 ) ) ;
#16157=STYLED_ITEM ( 'NONE', ( #65962 ), #9068 ) ;
#16166=EDGE_LOOP ( 'NONE', ( #31468, #47829 ) ) ;
#16167=STYLED_ITEM ( 'NONE', ( #36521 ), #48348 ) ;
#16169=COLOUR_RGB ( '', 0.72549020, 0.75294118, 0.79215686) ;
#16176=SURFACE_STYLE_USAGE ( .BOTH. , #42568 ) ;
#16186=( NAMED_UNIT ( * ) PLANE_ANGLE_UNIT ( ) SI_UNIT ( $, .RADIAN. ) );
#16189=VECTOR ( 'NONE', #16803, 1000.000000000000000 ) ;
#16212=CARTESIAN_POINT ( 'NONE',  ( 6.330869393641157750, 43.00000000000000000, -28.38386403503541899 ) ) ;
#16215=VECTOR ( 'NONE', #34943, 1000.000000000000000 ) ;
#16219=ORIENTED_EDGE ( 'NONE', *, *, #40533, .F. ) ;
#16222=CARTESIAN_POINT ( 'NONE',  ( 31.00000000000000711, 42.00000000000000000, -35.50000000000000000 ) ) ;
#16227=( NAMED_UNIT ( * ) SI_UNIT ( $, .STERADIAN. ) SOLID_ANGLE_UNIT ( ) );
#16230=( NAMED_UNIT ( * ) SI_UNIT ( $, .STERADIAN. ) SOLID_ANGLE_UNIT ( ) );
#16235=DIRECTION ( 'NONE',  ( -1.982541115402069054E-16, 0.000000000000000000, 1.000000000000000000 ) ) ;
#16236=SURFACE_STYLE_USAGE ( .BOTH. , #64389 ) ;
#16237=EDGE_CURVE ( 'NONE', #56481, #63720, #15698, .T. ) ;
#16241=DIRECTION ( 'NONE',  ( 1.000000000000000000, -0.000000000000000000, -1.300977106640434891E-16 ) ) ;
#16242=CIRCLE ( 'NONE', #26327, 5.000000000000000888 ) ;
#16249=COLOUR_RGB ( '', 0.40784314, 0.44705882, 0.49803922) ;
#16250=ORIENTED_EDGE ( 'NONE', *, *, #9760, .T. ) ;
#16252=AXIS2_PLACEMENT_3D ( 'NONE', #44715, #66105, #29871 ) ;
#16260=EDGE_LOOP ( 'NONE', ( #43220, #32483, #23115, #5993 ) ) ;
#16261=EDGE_LOOP ( 'NONE', ( #23022, #25680, #64635, #27368 ) ) ;
#16276=MECHANICAL_DESIGN_GEOMETRIC_PRESENTATION_REPRESENTATION('',(#53353),#21872);
#16278=( LENGTH_UNIT ( ) NAMED_UNIT ( * ) SI_UNIT ( .MILLI., .METRE. ) );
#16281=CARTESIAN_POINT ( 'NONE',  ( 0.7152599553061416149, 42.96841831342779017, -74.40727961101599419 ) ) ;
#16303=STYLED_ITEM ( 'NONE', ( #19509 ), #56294 ) ;
#16310=ORIENTED_EDGE ( 'NONE', *, *, #16849, .F. ) ;
#16318=CARTESIAN_POINT ( 'NONE',  ( 8.000000000000030198, 5.000000000000000000, 29.00402776293826079 ) ) ;
#16319=PRESENTATION_STYLE_ASSIGNMENT (( #69073 ) ) ;
#16324=EDGE_CURVE ( 'NONE', #22411, #44784, #53926, .T. ) ;
#16327=COLOUR_RGB ( '', 0.66274510, 0.83137255, 0.94901961) ;
#16331=CARTESIAN_POINT ( 'NONE',  ( 1.000000000000000000, 0.9999999999999991118, 79.00402776293826435 ) ) ;
#16332=EDGE_CURVE ( 'NONE', #52016, #31350, #30306, .T. ) ;
#16336=STYLED_ITEM ( 'NONE', ( #22991 ), #38953 ) ;
#16337=CARTESIAN_POINT ( 'NONE',  ( 6.000000000000017764, 42.74314482547740113, -27.71473342867655987 ) ) ;
#16343=ORIENTED_EDGE ( 'NONE', *, *, #31527, .T. ) ;
#16347=LINE ( 'NONE', #54619, #59696 ) ;
#16349=ADVANCED_FACE ( 'NONE', ( #28824 ), #7721, .T. ) ;
#16354=ORIENTED_EDGE ( 'NONE', *, *, #13027, .F. ) ;
#16360=ORIENTED_EDGE ( 'NONE', *, *, #67266, .T. ) ;
#16364=VERTEX_POINT ( 'NONE', #12649 ) ;
#16369=DIRECTION ( 'NONE',  ( 0.000000000000000000, -1.000000000000000000, 0.000000000000000000 ) ) ;
#16373=VECTOR ( 'NONE', #33319, 1000.000000000000000 ) ;
#16374=DIRECTION ( 'NONE',  ( 0.000000000000000000, 0.000000000000000000, -1.000000000000000000 ) ) ;
#16376=VERTEX_POINT ( 'NONE', #11967 ) ;
#16379=PLANE ( 'NONE',  #29686 ) ;
#16382=EDGE_LOOP ( 'NONE', ( #63963, #34123, #27262 ) ) ;
#16388=CARTESIAN_POINT ( 'NONE',  ( 31.28474004469385861, 42.96841831342779727, -45.59272038898399160 ) ) ;
#16403=DIRECTION ( 'NONE',  ( -1.000000000000000000, -0.000000000000000000, 1.300977106640434891E-16 ) ) ;
#16404=FACE_OUTER_BOUND ( 'NONE', #31897, .T. ) ;
#16406=EDGE_CURVE ( 'NONE', #23835, #51461, #18295, .T. ) ;
#16408=FILL_AREA_STYLE ('',( #63848 ) ) ;
#16411=CARTESIAN_POINT ( 'NONE',  ( 57.00000000000000000, 13.00000000000000178, 79.00402776293826435 ) ) ;
#16414=ORIENTED_EDGE ( 'NONE', *, *, #10343, .T. ) ;
#16418=PRESENTATION_STYLE_ASSIGNMENT (( #119 ) ) ;
#16419=UNCERTAINTY_MEASURE_WITH_UNIT (LENGTH_MEASURE( 1.000000000000000082E-05 ), #7799, 'distance_accuracy_value', 'NONE');
#16428=AXIS2_PLACEMENT_3D ( 'NONE', #46760, #56909, #55867 ) ;
#16452=FILL_AREA_STYLE_COLOUR ( '', #50094 ) ;
#16470=LINE ( 'NONE', #55444, #52087 ) ;
#16472=FILL_AREA_STYLE_COLOUR ( '', #65270 ) ;
#16477=CARTESIAN_POINT ( 'NONE',  ( 35.99999999999999289, 5.000000000000000000, -24.00402776293825369 ) ) ;
#16479=CARTESIAN_POINT ( 'NONE',  ( 0.000000000000000000, 42.00000000000000000, -80.00402776293826435 ) ) ;
#16527=( NAMED_UNIT ( * ) PLANE_ANGLE_UNIT ( ) SI_UNIT ( $, .RADIAN. ) );
#16528=VECTOR ( 'NONE', #44913, 1000.000000000000000 ) ;
#16530=VERTEX_POINT ( 'NONE', #67507 ) ;
#16533=ORIENTED_EDGE ( 'NONE', *, *, #42548, .T. ) ;
#16539=SURFACE_SIDE_STYLE ('',( #64344 ) ) ;
#16541=DIRECTION ( 'NONE',  ( 0.000000000000000000, 0.000000000000000000, 1.000000000000000000 ) ) ;
#16558=UNCERTAINTY_MEASURE_WITH_UNIT (LENGTH_MEASURE( 1.000000000000000082E-05 ), #802, 'distance_accuracy_value', 'NONE');
#16569=FILL_AREA_STYLE_COLOUR ( '', #68541 ) ;
#16571=( LENGTH_UNIT ( ) NAMED_UNIT ( * ) SI_UNIT ( .MILLI., .METRE. ) );
#16572=SURFACE_SIDE_STYLE ('',( #32700 ) ) ;
#16581=SURFACE_STYLE_USAGE ( .BOTH. , #59428 ) ;
#16582=SURFACE_STYLE_FILL_AREA ( #53820 ) ;
#16583=AXIS2_PLACEMENT_3D ( 'NONE', #53873, #68415, #57512 ) ;
#16597=ORIENTED_EDGE ( 'NONE', *, *, #34896, .T. ) ;
#16598=DIRECTION ( 'NONE',  ( 0.000000000000000000, -0.3420201433256629953, -0.9396926207859104263 ) ) ;
#16602=AXIS2_PLACEMENT_3D ( 'NONE', #62860, #40405, #4823 ) ;
#16605=CARTESIAN_POINT ( 'NONE',  ( 23.00000000000000000, 5.000000000000000000, -24.00402776293825013 ) ) ;
#16612=ORIENTED_EDGE ( 'NONE', *, *, #17349, .F. ) ;
#16616=ORIENTED_EDGE ( 'NONE', *, *, #68650, .F. ) ;
#16628=( NAMED_UNIT ( * ) PLANE_ANGLE_UNIT ( ) SI_UNIT ( $, .RADIAN. ) );
#16646=EDGE_LOOP ( 'NONE', ( #50620, #61471, #10575, #41954 ) ) ;
#16647=PRESENTATION_STYLE_ASSIGNMENT (( #38476 ) ) ;
#16649=PRESENTATION_STYLE_ASSIGNMENT (( #64466 ) ) ;
#16651=DIRECTION ( 'NONE',  ( -0.000000000000000000, -1.000000000000000000, -0.000000000000000000 ) ) ;
#16655=ADVANCED_FACE ( 'NONE', ( #21749 ), #33677, .T. ) ;
#16666=AXIS2_PLACEMENT_3D ( 'NONE', #3713, #51255, #41417 ) ;
#16668=CARTESIAN_POINT ( 'NONE',  ( 1.000000000000000000, 42.00000000000000000, 0.000000000000000000 ) ) ;
#16671=( GEOMETRIC_REPRESENTATION_CONTEXT ( 3 ) GLOBAL_UNCERTAINTY_ASSIGNED_CONTEXT ( ( #9397 ) ) GLOBAL_UNIT_ASSIGNED_CONTEXT ( ( #40987, #2567, #66998 ) ) REPRESENTATION_CONTEXT ( 'NONE', 'WORKASPACE' ) );
#16681=LINE ( 'NONE', #60253, #50730 ) ;
#16682=ADVANCED_FACE ( 'NONE', ( #6578 ), #31478, .T. ) ;
#16689=SURFACE_STYLE_USAGE ( .BOTH. , #64509 ) ;
#16696=DIRECTION ( 'NONE',  ( -1.300977106640434891E-16, 0.000000000000000000, -1.000000000000000000 ) ) ;
#16706=EDGE_CURVE ( 'NONE', #9623, #37678, #43309, .T. ) ;
#16708=( NAMED_UNIT ( * ) PLANE_ANGLE_UNIT ( ) SI_UNIT ( $, .RADIAN. ) );
#16709=ORIENTED_EDGE ( 'NONE', *, *, #39651, .T. ) ;
#16710=DIRECTION ( 'NONE',  ( 0.000000000000000000, 0.000000000000000000, -1.000000000000000000 ) ) ;
#16720=ORIENTED_EDGE ( 'NONE', *, *, #2144, .T. ) ;
#16722=CARTESIAN_POINT ( 'NONE',  ( 31.00000000000000000, 42.00000000000000000, -80.00402776293826435 ) ) ;
#16725=ORIENTED_EDGE ( 'NONE', *, *, #33304, .T. ) ;
#16736=CARTESIAN_POINT ( 'NONE',  ( 22.00000000000000711, 50.00000000000000000, -60.00000000000000711 ) ) ;
#16743=AXIS2_PLACEMENT_3D ( 'NONE', #58324, #46799, #31581 ) ;
#16744=MECHANICAL_DESIGN_GEOMETRIC_PRESENTATION_REPRESENTATION('',(#23426),#36999);
#16755=VECTOR ( 'NONE', #17014, 1000.000000000000000 ) ;
#16791=AXIS2_PLACEMENT_3D ( 'NONE', #11333, #9971, #36741 ) ;
#16799=MECHANICAL_DESIGN_GEOMETRIC_PRESENTATION_REPRESENTATION('',(#25751),#969);
#16803=DIRECTION ( 'NONE',  ( 1.000000000000000000, 0.000000000000000000, 4.625929269271505635E-16 ) ) ;
#16808=FILL_AREA_STYLE_COLOUR ( '', #39913 ) ;
#16810=( NAMED_UNIT ( * ) PLANE_ANGLE_UNIT ( ) SI_UNIT ( $, .RADIAN. ) );
#16816=CARTESIAN_POINT ( 'NONE',  ( 6.000000000000017764, 26.00000000000000355, -27.50000000000000355 ) ) ;
#16825=AXIS2_PLACEMENT_3D ( 'NONE', #23419, #54728, #11490 ) ;
#16828=VECTOR ( 'NONE', #39506, 1000.000000000000000 ) ;
#16832=CARTESIAN_POINT ( 'NONE',  ( 24.70582419978697786, 25.82281152269784386, 27.50002557046276763 ) ) ;
#16842=( BOUNDED_CURVE ( )  B_SPLINE_CURVE ( 3, ( #31841, #32523, #43506, #36487 ),
 .UNSPECIFIED., .F., .F. ) 
 B_SPLINE_CURVE_WITH_KNOTS ( ( 4, 4 ),
 ( 1.570796326794896558, 3.141592653589792228 ),
 .UNSPECIFIED. ) 
 CURVE ( )  GEOMETRIC_REPRESENTATION_ITEM ( )  RATIONAL_B_SPLINE_CURVE ( ( 1.000000000000000000, 0.8047378541243652705, 0.8047378541243652705, 1.000000000000000000 ) ) 
 REPRESENTATION_ITEM ( '' )  );
#16843=COLOUR_RGB ( '', 0.40784314, 0.44705882, 0.49803922) ;
#16844=FACE_OUTER_BOUND ( 'NONE', #58789, .T. ) ;
#16849=EDGE_CURVE ( 'NONE', #25215, #22405, #50563, .T. ) ;
#16856=DIRECTION ( 'NONE',  ( 0.000000000000000000, 1.000000000000000000, -0.000000000000000000 ) ) ;
#16857=COLOUR_RGB ( '', 0.72549020, 0.75294118, 0.79215686) ;
#16864=ADVANCED_FACE ( 'NONE', ( #34705 ), #58958, .F. ) ;
#16866=FILL_AREA_STYLE_COLOUR ( '', #38098 ) ;
#16867=LINE ( 'NONE', #33025, #50157 ) ;
#16868=EDGE_LOOP ( 'NONE', ( #518, #54575, #5296, #66856 ) ) ;
#16871=CARTESIAN_POINT ( 'NONE',  ( 11.00000000000001776, 26.00000000000000355, -24.00000000000000355 ) ) ;
#16877=PLANE ( 'NONE',  #54102 ) ;
#16887=ORIENTED_EDGE ( 'NONE', *, *, #28441, .F. ) ;
#16891=CYLINDRICAL_SURFACE ( 'NONE', #58842, 4.999999999999997335 ) ;
#16895=ORIENTED_EDGE ( 'NONE', *, *, #46261, .T. ) ;
#16899=ORIENTED_EDGE ( 'NONE', *, *, #62291, .T. ) ;
#16905=PLANE ( 'NONE',  #66648 ) ;
#16914=VECTOR ( 'NONE', #67076, 1000.000000000000000 ) ;
#16920=LINE ( 'NONE', #26729, #51010 ) ;
#16924=( NAMED_UNIT ( * ) SI_UNIT ( $, .STERADIAN. ) SOLID_ANGLE_UNIT ( ) );
#16925=STYLED_ITEM ( 'NONE', ( #62908 ), #44851 ) ;
#16930=CARTESIAN_POINT ( 'NONE',  ( 32.00000000000002132, 42.00000000000000000, 75.00000000000000000 ) ) ;
#16932=CARTESIAN_POINT ( 'NONE',  ( 8.000000000000030198, 5.000000000000000000, 29.00402776293826079 ) ) ;
#16938=MECHANICAL_DESIGN_GEOMETRIC_PRESENTATION_REPRESENTATION('',(#4380),#2225);
#16946=ORIENTED_EDGE ( 'NONE', *, *, #15232, .T. ) ;
#16982=DIRECTION ( 'NONE',  ( 0.000000000000000000, 0.000000000000000000, -1.000000000000000000 ) ) ;
#16986=SURFACE_SIDE_STYLE ('',( #44097 ) ) ;
#16995=( GEOMETRIC_REPRESENTATION_CONTEXT ( 3 ) GLOBAL_UNCERTAINTY_ASSIGNED_CONTEXT ( ( #41244 ) ) GLOBAL_UNIT_ASSIGNED_CONTEXT ( ( #12569, #27096, #54193 ) ) REPRESENTATION_CONTEXT ( 'NONE', 'WORKASPACE' ) );
#17013=VERTEX_POINT ( 'NONE', #27256 ) ;
#17014=DIRECTION ( 'NONE',  ( 1.000000000000000000, -0.000000000000000000, -1.300977106640434891E-16 ) ) ;
#17015=FACE_OUTER_BOUND ( 'NONE', #18722, .T. ) ;
#17017=MECHANICAL_DESIGN_GEOMETRIC_PRESENTATION_REPRESENTATION('',(#23721),#42908);
#17035=SURFACE_STYLE_FILL_AREA ( #50405 ) ;
#17039=DIRECTION ( 'NONE',  ( 0.000000000000000000, 0.000000000000000000, 1.000000000000000000 ) ) ;
#17053=SURFACE_STYLE_USAGE ( .BOTH. , #10712 ) ;
#17056=SURFACE_SIDE_STYLE ('',( #65908 ) ) ;
#17061=DIRECTION ( 'NONE',  ( -0.000000000000000000, -0.000000000000000000, -1.000000000000000000 ) ) ;
#17075=( LENGTH_UNIT ( ) NAMED_UNIT ( * ) SI_UNIT ( .MILLI., .METRE. ) );
#17081=VECTOR ( 'NONE', #24406, 1000.000000000000000 ) ;
#17087=FACE_BOUND ( 'NONE', #52153, .T. ) ;
#17118=STYLED_ITEM ( 'NONE', ( #46608 ), #25726 ) ;
#17119=SURFACE_STYLE_USAGE ( .BOTH. , #38929 ) ;
#17120=PRESENTATION_STYLE_ASSIGNMENT (( #50488 ) ) ;
#17122=CARTESIAN_POINT ( 'NONE',  ( 6.000000000000017764, -0.1486183402614471571, 18.42691897641805099 ) ) ;
#17126=FILL_AREA_STYLE_COLOUR ( '', #66748 ) ;
#17137=LINE ( 'NONE', #64931, #68174 ) ;
#17142=MECHANICAL_DESIGN_GEOMETRIC_PRESENTATION_REPRESENTATION('',(#44128),#29448);
#17146=ORIENTED_EDGE ( 'NONE', *, *, #15680, .F. ) ;
#17154=SURFACE_STYLE_USAGE ( .BOTH. , #32586 ) ;
#17161=( GEOMETRIC_REPRESENTATION_CONTEXT ( 3 ) GLOBAL_UNCERTAINTY_ASSIGNED_CONTEXT ( ( #1816 ) ) GLOBAL_UNIT_ASSIGNED_CONTEXT ( ( #38811, #712, #59163 ) ) REPRESENTATION_CONTEXT ( 'NONE', 'WORKASPACE' ) );
#17167=SURFACE_STYLE_FILL_AREA ( #37952 ) ;
#17183=CARTESIAN_POINT ( 'NONE',  ( 24.16082825257855760, 24.77175885999242766, 27.27794882343791372 ) ) ;
#17192=( LENGTH_UNIT ( ) NAMED_UNIT ( * ) SI_UNIT ( .MILLI., .METRE. ) );
#17215=FILL_AREA_STYLE ('',( #65367 ) ) ;
#17217=DIRECTION ( 'NONE',  ( 0.000000000000000000, 0.000000000000000000, -1.000000000000000000 ) ) ;
#17221=DIRECTION ( 'NONE',  ( 0.000000000000000000, 0.000000000000000000, -1.000000000000000000 ) ) ;
#17229=DIRECTION ( 'NONE',  ( 1.000000000000000000, 0.000000000000000000, 0.000000000000000000 ) ) ;
#17236=VERTEX_POINT ( 'NONE', #37118 ) ;
#17242=ORIENTED_EDGE ( 'NONE', *, *, #68650, .T. ) ;
#17243=MECHANICAL_DESIGN_GEOMETRIC_PRESENTATION_REPRESENTATION('',(#40788),#57635);
#17248=( LENGTH_UNIT ( ) NAMED_UNIT ( * ) SI_UNIT ( .MILLI., .METRE. ) );
#17255=VERTEX_POINT ( 'NONE', #63464 ) ;
#17258=CARTESIAN_POINT ( 'NONE',  ( 0.000000000000000000, 13.00000000000000178, 36.50000000000000000 ) ) ;
#17266=CARTESIAN_POINT ( 'NONE',  ( 10.00000000000001776, 43.00000000000000000, -29.68999999999999417 ) ) ;
#17270=ORIENTED_EDGE ( 'NONE', *, *, #62719, .F. ) ;
#17272=ADVANCED_FACE ( 'NONE', ( #69431 ), #31422, .F. ) ;
#17275=( NAMED_UNIT ( * ) SI_UNIT ( $, .STERADIAN. ) SOLID_ANGLE_UNIT ( ) );
#17283=VECTOR ( 'NONE', #18573, 1000.000000000000000 ) ;
#17287=VERTEX_POINT ( 'NONE', #17379 ) ;
#17305=SURFACE_STYLE_USAGE ( .BOTH. , #671 ) ;
#17308=VERTEX_POINT ( 'NONE', #54274 ) ;
#17316=CARTESIAN_POINT ( 'NONE',  ( 28.00000000000000000, 43.00000000000000000, -90.00000000000000000 ) ) ;
#17317=EDGE_LOOP ( 'NONE', ( #36447, #9765 ) ) ;
#17326=UNCERTAINTY_MEASURE_WITH_UNIT (LENGTH_MEASURE( 1.000000000000000082E-05 ), #67704, 'distance_accuracy_value', 'NONE');
#17338=UNCERTAINTY_MEASURE_WITH_UNIT (LENGTH_MEASURE( 1.000000000000000082E-05 ), #46025, 'distance_accuracy_value', 'NONE');
#17343=B_SPLINE_CURVE_WITH_KNOTS ( 'NONE', 3,
 ( #25551, #47787, #68148, #69189, #20989, #31170, #57584, #36152, #20648, #9415, #42159, #30836 ),
 .UNSPECIFIED., .F., .F.,
 ( 4, 2, 2, 2, 2, 4 ),
 ( 0.000000000000000000, 0.0005293381373090682695, 0.001058676274618136539, 0.001323345343272677721, 0.001588014411927218686, 0.002117352549236312977 ),
 .UNSPECIFIED. ) ;
#17349=EDGE_CURVE ( 'NONE', #56901, #61113, #16347, .T. ) ;
#17354=DIRECTION ( 'NONE',  ( -1.000000000000000000, 0.000000000000000000, 0.000000000000000000 ) ) ;
#17361=SURFACE_STYLE_FILL_AREA ( #61592 ) ;
#17365=VECTOR ( 'NONE', #12084, 1000.000000000000227 ) ;
#17368=EDGE_CURVE ( 'NONE', #8636, #51304, #16681, .T. ) ;
#17372=( GEOMETRIC_REPRESENTATION_CONTEXT ( 3 ) GLOBAL_UNCERTAINTY_ASSIGNED_CONTEXT ( ( #21387 ) ) GLOBAL_UNIT_ASSIGNED_CONTEXT ( ( #45938, #46299, #25148 ) ) REPRESENTATION_CONTEXT ( 'NONE', 'WORKASPACE' ) );
#17375=PRESENTATION_STYLE_ASSIGNMENT (( #28560 ) ) ;
#17379=CARTESIAN_POINT ( 'NONE',  ( 1.000000000000000000, 42.00000000000000000, 80.00402776293826435 ) ) ;
#17380=DIRECTION ( 'NONE',  ( 0.000000000000000000, 1.000000000000000000, 0.000000000000000000 ) ) ;
#17381=CARTESIAN_POINT ( 'NONE',  ( 0.8561460859850876792, 43.00000000000000711, 74.38749456993821241 ) ) ;
#17387=SURFACE_STYLE_USAGE ( .BOTH. , #28577 ) ;
#17393=AXIS2_PLACEMENT_3D ( 'NONE', #19857, #68404, #62755 ) ;
#17395=FILL_AREA_STYLE ('',( #5744 ) ) ;
#17397=VECTOR ( 'NONE', #16241, 1000.000000000000000 ) ;
#17400=AXIS2_PLACEMENT_3D ( 'NONE', #66130, #66854, #40138 ) ;
#17403=CARTESIAN_POINT ( 'NONE',  ( 31.00000000000000000, 42.00000000000000000, -75.00000000000001421 ) ) ;
#17404=( LENGTH_UNIT ( ) NAMED_UNIT ( * ) SI_UNIT ( .MILLI., .METRE. ) );
#17406=FACE_OUTER_BOUND ( 'NONE', #834, .T. ) ;
#17416=STYLED_ITEM ( 'NONE', ( #35836 ), #63851 ) ;
#17422=ADVANCED_FACE ( 'NONE', ( #6776 ), #38146, .F. ) ;
#17427=( GEOMETRIC_REPRESENTATION_CONTEXT ( 3 ) GLOBAL_UNCERTAINTY_ASSIGNED_CONTEXT ( ( #17338 ) ) GLOBAL_UNIT_ASSIGNED_CONTEXT ( ( #46025, #46380, #63558 ) ) REPRESENTATION_CONTEXT ( 'NONE', 'WORKASPACE' ) );
#17441=PRESENTATION_STYLE_ASSIGNMENT (( #65589 ) ) ;
#17443=ADVANCED_FACE ( 'NONE', ( #45756 ), #41507, .F. ) ;
#17459=AXIS2_PLACEMENT_3D ( 'NONE', #27332, #15789, #64654 ) ;
#17461=VECTOR ( 'NONE', #61169, 1000.000000000000000 ) ;
#17462=FILL_AREA_STYLE_COLOUR ( '', #21320 ) ;
#17467=LINE ( 'NONE', #50836, #27343 ) ;
#17475=FILL_AREA_STYLE ('',( #16452 ) ) ;
#17483=LINE ( 'NONE', #23088, #31662 ) ;
#17488=SURFACE_SIDE_STYLE ('',( #55784 ) ) ;
#17495=FILL_AREA_STYLE ('',( #65653 ) ) ;
#17504=DIRECTION ( 'NONE',  ( 1.300977106640434891E-16, 0.000000000000000000, 1.000000000000000000 ) ) ;
#17510=CARTESIAN_POINT ( 'NONE',  ( 22.99999999999995381, 5.000000000000000000, 32.00402776293825724 ) ) ;
#17516=PRESENTATION_STYLE_ASSIGNMENT (( #65670 ) ) ;
#17522=ORIENTED_EDGE ( 'NONE', *, *, #61752, .F. ) ;
#17539=( NAMED_UNIT ( * ) SI_UNIT ( $, .STERADIAN. ) SOLID_ANGLE_UNIT ( ) );
#17540=ORIENTED_EDGE ( 'NONE', *, *, #40533, .T. ) ;
#17554=VERTEX_POINT ( 'NONE', #62238 ) ;
#17556=( LENGTH_UNIT ( ) NAMED_UNIT ( * ) SI_UNIT ( .MILLI., .METRE. ) );
#17558=DIRECTION ( 'NONE',  ( 1.000000000000000000, 0.000000000000000000, -1.300977106640442040E-16 ) ) ;
#17565=CARTESIAN_POINT ( 'NONE',  ( 24.15983302833083712, 27.22897014610288480, -27.27767451507459029 ) ) ;
#17577=DIRECTION ( 'NONE',  ( 0.000000000000000000, 0.000000000000000000, -1.000000000000000000 ) ) ;
#17583=STYLED_ITEM ( 'NONE', ( #18767 ), #1461 ) ;
#17598=SURFACE_STYLE_FILL_AREA ( #22859 ) ;
#17609=DIRECTION ( 'NONE',  ( 0.000000000000000000, 1.000000000000000000, 0.000000000000000000 ) ) ;
#17611=SURFACE_STYLE_FILL_AREA ( #2744 ) ;
#17618=DIRECTION ( 'NONE',  ( 0.000000000000000000, 1.000000000000000000, 0.000000000000000000 ) ) ;
#17619=STYLED_ITEM ( 'NONE', ( #15936 ), #50144 ) ;
#17620=DIRECTION ( 'NONE',  ( 0.9418169057949938860, 0.000000000000000000, -0.3361263392814427542 ) ) ;
#17623=PRESENTATION_STYLE_ASSIGNMENT (( #23226 ) ) ;
#17632=ORIENTED_EDGE ( 'NONE', *, *, #62339, .T. ) ;
#17637=SURFACE_STYLE_FILL_AREA ( #13020 ) ;
#17639=CARTESIAN_POINT ( 'NONE',  ( 4.000000000000030198, 38.70020753820971748, 89.00000000000000000 ) ) ;
#17645=CARTESIAN_POINT ( 'NONE',  ( 3.000000000000030198, 42.00000000000000000, 80.00402776293826435 ) ) ;
#17651=EDGE_LOOP ( 'NONE', ( #19046, #11296, #34224, #46166 ) ) ;
#17653=CYLINDRICAL_SURFACE ( 'NONE', #11648, 1.000000000000001998 ) ;
#17659=CARTESIAN_POINT ( 'NONE',  ( 30.99999999999998579, 0.000000000000000000, 72.00402776293822171 ) ) ;
#17664=ADVANCED_FACE ( 'NONE', ( #37701 ), #58408, .F. ) ;
#17668=DIRECTION ( 'NONE',  ( 1.000000000000000000, -0.000000000000000000, -1.300977106640434891E-16 ) ) ;
#17672=CYLINDRICAL_SURFACE ( 'NONE', #51997, 5.000000000000004441 ) ;
#17680=EDGE_CURVE ( 'NONE', #9757, #2410, #30355, .T. ) ;
#17692=ADVANCED_FACE ( 'NONE', ( #21820 ), #11598, .F. ) ;
#17701=COLOUR_RGB ( '', 0.31764706, 0.68627451, 0.89019608) ;
#17710=CARTESIAN_POINT ( 'NONE',  ( 20.00000000000001776, 14.00000000000000000, 29.68999999999999417 ) ) ;
#17713=AXIS2_PLACEMENT_3D ( 'NONE', #18991, #52444, #51037 ) ;
#17726=( NAMED_UNIT ( * ) SI_UNIT ( $, .STERADIAN. ) SOLID_ANGLE_UNIT ( ) );
#17729=SURFACE_STYLE_FILL_AREA ( #28930 ) ;
#17731=EDGE_CURVE ( 'NONE', #40860, #13573, #39405, .T. ) ;
#17734=FILL_AREA_STYLE ('',( #18419 ) ) ;
#17735=ORIENTED_EDGE ( 'NONE', *, *, #54628, .F. ) ;
#17740=CARTESIAN_POINT ( 'NONE',  ( 11.00000000000001776, -0.1486183402614471571, 18.42691897641805099 ) ) ;
#17755=( GEOMETRIC_REPRESENTATION_CONTEXT ( 3 ) GLOBAL_UNCERTAINTY_ASSIGNED_CONTEXT ( ( #69309 ) ) GLOBAL_UNIT_ASSIGNED_CONTEXT ( ( #59714, #54764, #13598 ) ) REPRESENTATION_CONTEXT ( 'NONE', 'WORKASPACE' ) );
#17760=DIRECTION ( 'NONE',  ( -0.000000000000000000, -1.000000000000000000, 0.000000000000000000 ) ) ;
#17770=CYLINDRICAL_SURFACE ( 'NONE', #24155, 1.000000000000001998 ) ;
#17773=ADVANCED_FACE ( 'NONE', ( #11233 ), #42955, .T. ) ;
#17781=SURFACE_STYLE_USAGE ( .BOTH. , #11443 ) ;
#17793=ORIENTED_EDGE ( 'NONE', *, *, #55670, .F. ) ;
#17801=MECHANICAL_DESIGN_GEOMETRIC_PRESENTATION_REPRESENTATION('',(#36970),#69465);
#17814=DIRECTION ( 'NONE',  ( 0.000000000000000000, 0.000000000000000000, 1.000000000000000000 ) ) ;
#17817=ADVANCED_FACE ( 'NONE', ( #40767 ), #1667, .T. ) ;
#17819=ORIENTED_EDGE ( 'NONE', *, *, #21464, .F. ) ;
#17827=DIRECTION ( 'NONE',  ( 0.000000000000000000, 0.000000000000000000, 1.000000000000000000 ) ) ;
#17828=( LENGTH_UNIT ( ) NAMED_UNIT ( * ) SI_UNIT ( .MILLI., .METRE. ) );
#17833=AXIS2_PLACEMENT_3D ( 'NONE', #45229, #47600, #20087 ) ;
#17849=CARTESIAN_POINT ( 'NONE',  ( 23.85560559829669458, 24.60330559701304409, 27.21038588406899805 ) ) ;
#17865=ORIENTED_EDGE ( 'NONE', *, *, #52082, .T. ) ;
#17868=STYLED_ITEM ( 'NONE', ( #9004 ), #4500 ) ;
#17877=ORIENTED_EDGE ( 'NONE', *, *, #60811, .T. ) ;
#17878=( NAMED_UNIT ( * ) PLANE_ANGLE_UNIT ( ) SI_UNIT ( $, .RADIAN. ) );
#17880=DIRECTION ( 'NONE',  ( 1.300977106640434891E-16, -0.000000000000000000, 1.000000000000000000 ) ) ;
#17882=ORIENTED_EDGE ( 'NONE', *, *, #10386, .T. ) ;
#17912=VERTEX_POINT ( 'NONE', #20314 ) ;
#17921=CARTESIAN_POINT ( 'NONE',  ( 22.99999999999995026, 5.000000000000000000, -32.00402776293824303 ) ) ;
#17940=AXIS2_PLACEMENT_3D ( 'NONE', #61423, #3706, #56507 ) ;
#17942=ORIENTED_EDGE ( 'NONE', *, *, #61776, .T. ) ;
#17946=SURFACE_SIDE_STYLE ('',( #34803 ) ) ;
#17947=STYLED_ITEM ( 'NONE', ( #50635 ), #69178 ) ;
#17953=MECHANICAL_DESIGN_GEOMETRIC_PRESENTATION_REPRESENTATION('',(#22417),#20145);
#17957=EDGE_CURVE ( 'NONE', #50964, #37266, #46403, .T. ) ;
#17958=VECTOR ( 'NONE', #9573, 1000.000000000000000 ) ;
#17962=( NAMED_UNIT ( * ) SI_UNIT ( $, .STERADIAN. ) SOLID_ANGLE_UNIT ( ) );
#17967=DIRECTION ( 'NONE',  ( -0.000000000000000000, -1.000000000000000000, -0.000000000000000000 ) ) ;
#17969=EDGE_CURVE ( 'NONE', #53049, #46991, #55756, .T. ) ;
#17975=CARTESIAN_POINT ( 'NONE',  ( 23.50000000000001776, 14.00000000000000000, 29.68999999999999417 ) ) ;
#17978=EDGE_CURVE ( 'NONE', #1306, #22643, #3757, .T. ) ;
#17987=DIRECTION ( 'NONE',  ( 0.000000000000000000, 0.000000000000000000, -1.000000000000000000 ) ) ;
#18001=ORIENTED_EDGE ( 'NONE', *, *, #57141, .T. ) ;
#18006=EDGE_CURVE ( 'NONE', #34731, #59410, #37595, .T. ) ;
#18007=COLOUR_RGB ( '', 0.66274510, 0.83137255, 0.94901961) ;
#18008=FILL_AREA_STYLE_COLOUR ( '', #69575 ) ;
#18020=CIRCLE ( 'NONE', #5642, 1.000000000000000888 ) ;
#18028=CIRCLE ( 'NONE', #12383, 4.999999999999997335 ) ;
#18052=VERTEX_POINT ( 'NONE', #5857 ) ;
#18055=VECTOR ( 'NONE', #53493, 1000.000000000000000 ) ;
#18070=AXIS2_PLACEMENT_3D ( 'NONE', #41090, #7415, #67798 ) ;
#18073=PRESENTATION_STYLE_ASSIGNMENT (( #34942 ) ) ;
#18085=( GEOMETRIC_REPRESENTATION_CONTEXT ( 3 ) GLOBAL_UNCERTAINTY_ASSIGNED_CONTEXT ( ( #13615 ) ) GLOBAL_UNIT_ASSIGNED_CONTEXT ( ( #16571, #59417, #637 ) ) REPRESENTATION_CONTEXT ( 'NONE', 'WORKASPACE' ) );
#18093=CARTESIAN_POINT ( 'NONE',  ( 8.000000000000024869, 5.000000000000000000, 32.00402776293825724 ) ) ;
#18094=VERTEX_POINT ( 'NONE', #27986 ) ;
#18096=DIRECTION ( 'NONE',  ( 0.000000000000000000, -0.3420201433256630508, -0.9396926207859105373 ) ) ;
#18111=( GEOMETRIC_REPRESENTATION_CONTEXT ( 3 ) GLOBAL_UNCERTAINTY_ASSIGNED_CONTEXT ( ( #24300 ) ) GLOBAL_UNIT_ASSIGNED_CONTEXT ( ( #66822, #26304, #10837 ) ) REPRESENTATION_CONTEXT ( 'NONE', 'WORKASPACE' ) );
#18116=ADVANCED_FACE ( 'NONE', ( #42509 ), #63908, .T. ) ;
#18118=FILL_AREA_STYLE ('',( #54352 ) ) ;
#18127=DIRECTION ( 'NONE',  ( -0.000000000000000000, -1.000000000000000000, -0.000000000000000000 ) ) ;
#18133=CARTESIAN_POINT ( 'NONE',  ( 10.00000000000002132, 50.00000000000000000, 60.00000000000000711 ) ) ;
#18139=MECHANICAL_DESIGN_GEOMETRIC_PRESENTATION_REPRESENTATION('',(#22764),#54236);
#18144=CYLINDRICAL_SURFACE ( 'NONE', #4635, 1.000000000000000888 ) ;
#18149=ADVANCED_FACE ( 'NONE', ( #46602 ), #14840, .T. ) ;
#18152=AXIS2_PLACEMENT_3D ( 'NONE', #20209, #52606, #70 ) ;
#18174=ORIENTED_EDGE ( 'NONE', *, *, #46583, .T. ) ;
#18177=AXIS2_PLACEMENT_3D ( 'NONE', #20508, #21545, #36735 ) ;
#18192=DIRECTION ( 'NONE',  ( 0.000000000000000000, 0.000000000000000000, 1.000000000000000000 ) ) ;
#18206=ORIENTED_EDGE ( 'NONE', *, *, #57446, .T. ) ;
#18214=SURFACE_SIDE_STYLE ('',( #1957 ) ) ;
#18222=ORIENTED_EDGE ( 'NONE', *, *, #34227, .T. ) ;
#18231=( LENGTH_UNIT ( ) NAMED_UNIT ( * ) SI_UNIT ( .MILLI., .METRE. ) );
#18233=CARTESIAN_POINT ( 'NONE',  ( 24.29096171535645965, 27.11720862454939507, -27.31743315471676681 ) ) ;
#18238=( NAMED_UNIT ( * ) PLANE_ANGLE_UNIT ( ) SI_UNIT ( $, .RADIAN. ) );
#18241=VERTEX_POINT ( 'NONE', #64460 ) ;
#18247=MECHANICAL_DESIGN_GEOMETRIC_PRESENTATION_REPRESENTATION('',(#9279),#5880);
#18251=ORIENTED_EDGE ( 'NONE', *, *, #53319, .F. ) ;
#18252=MECHANICAL_DESIGN_GEOMETRIC_PRESENTATION_REPRESENTATION('',(#49744),#62068);
#18261=CARTESIAN_POINT ( 'NONE',  ( 0.000000000000000000, 13.00000000000000178, -80.00402776293826435 ) ) ;
#18266=( GEOMETRIC_REPRESENTATION_CONTEXT ( 3 ) GLOBAL_UNCERTAINTY_ASSIGNED_CONTEXT ( ( #11033 ) ) GLOBAL_UNIT_ASSIGNED_CONTEXT ( ( #49299, #11996, #61909 ) ) REPRESENTATION_CONTEXT ( 'NONE', 'WORKASPACE' ) );
#18276=DIRECTION ( 'NONE',  ( 0.000000000000000000, 0.000000000000000000, 1.000000000000000000 ) ) ;
#18280=FACE_OUTER_BOUND ( 'NONE', #13639, .T. ) ;
#18282=EDGE_CURVE ( 'NONE', #47636, #45878, #48552, .T. ) ;
#18285=EDGE_CURVE ( 'NONE', #67099, #60790, #41644, .T. ) ;
#18292=ADVANCED_FACE ( 'NONE', ( #37782 ), #48317, .T. ) ;
#18295=LINE ( 'NONE', #61194, #22452 ) ;
#18302=CARTESIAN_POINT ( 'NONE',  ( 57.00000000000000000, 13.00000000000000178, -60.00402776293827145 ) ) ;
#18314=DIRECTION ( 'NONE',  ( 0.000000000000000000, 1.000000000000000000, 0.000000000000000000 ) ) ;
#18326=AXIS2_PLACEMENT_3D ( 'NONE', #23953, #19361, #61245 ) ;
#18327=FACE_OUTER_BOUND ( 'NONE', #2167, .T. ) ;
#18332=ORIENTED_EDGE ( 'NONE', *, *, #55579, .F. ) ;
#18350=DIRECTION ( 'NONE',  ( 0.000000000000000000, 0.000000000000000000, 1.000000000000000000 ) ) ;
#18353=( GEOMETRIC_REPRESENTATION_CONTEXT ( 3 ) GLOBAL_UNCERTAINTY_ASSIGNED_CONTEXT ( ( #41284 ) ) GLOBAL_UNIT_ASSIGNED_CONTEXT ( ( #22159, #43658, #16227 ) ) REPRESENTATION_CONTEXT ( 'NONE', 'WORKASPACE' ) );
#18370=( GEOMETRIC_REPRESENTATION_CONTEXT ( 3 ) GLOBAL_UNCERTAINTY_ASSIGNED_CONTEXT ( ( #26230 ) ) GLOBAL_UNIT_ASSIGNED_CONTEXT ( ( #29303, #20132, #30332 ) ) REPRESENTATION_CONTEXT ( 'NONE', 'WORKASPACE' ) );
#18371=( NAMED_UNIT ( * ) SI_UNIT ( $, .STERADIAN. ) SOLID_ANGLE_UNIT ( ) );
#18373=LINE ( 'NONE', #54922, #64097 ) ;
#18393=ORIENTED_EDGE ( 'NONE', *, *, #66055, .T. ) ;
#18397=EDGE_LOOP ( 'NONE', ( #22267, #16310, #68659, #60128 ) ) ;
#18399=COLOUR_RGB ( '', 0.40784314, 0.44705882, 0.49803922) ;
#18413=EDGE_CURVE ( 'NONE', #51444, #13259, #50709, .T. ) ;
#18419=FILL_AREA_STYLE_COLOUR ( '', #26090 ) ;
#18424=VERTEX_POINT ( 'NONE', #55638 ) ;
#18425=CARTESIAN_POINT ( 'NONE',  ( 6.000000000000017764, 43.00000000000000000, 29.49447654986459710 ) ) ;
#18429=COLOUR_RGB ( '', 0.08235294, 0.09019608, 0.10196078) ;
#18450=LINE ( 'NONE', #39935, #57652 ) ;
#18452=CARTESIAN_POINT ( 'NONE',  ( 36.00000000000002132, 0.000000000000000000, -77.00402776293825013 ) ) ;
#18455=DIRECTION ( 'NONE',  ( 0.000000000000000000, 0.000000000000000000, 1.000000000000000000 ) ) ;
#18456=DIRECTION ( 'NONE',  ( -7.816271194327172234E-17, 0.000000000000000000, -1.000000000000000000 ) ) ;
#18460=( GEOMETRIC_REPRESENTATION_CONTEXT ( 3 ) GLOBAL_UNCERTAINTY_ASSIGNED_CONTEXT ( ( #52311 ) ) GLOBAL_UNIT_ASSIGNED_CONTEXT ( ( #21671, #32556, #43533 ) ) REPRESENTATION_CONTEXT ( 'NONE', 'WORKASPACE' ) );
#18473=CARTESIAN_POINT ( 'NONE',  ( 4.000000000000029310, 34.36176364315826248, 80.00402776293826435 ) ) ;
#18485=SURFACE_SIDE_STYLE ('',( #38935 ) ) ;
#18499=CARTESIAN_POINT ( 'NONE',  ( 6.000000000000017764, 43.00000000000000000, 28.38386403503541899 ) ) ;
#18505=EDGE_CURVE ( 'NONE', #17255, #11384, #68716, .T. ) ;
#18506=ORIENTED_EDGE ( 'NONE', *, *, #64312, .F. ) ;
#18519=STYLED_ITEM ( 'NONE', ( #44126 ), #37898 ) ;
#18521=PRESENTATION_STYLE_ASSIGNMENT (( #19546 ) ) ;
#18531=ADVANCED_FACE ( 'NONE', ( #45476 ), #46155, .F. ) ;
#18532=CARTESIAN_POINT ( 'NONE',  ( 27.00000000000001776, 43.00000000000000000, -36.50000000000000000 ) ) ;
#18533=SURFACE_SIDE_STYLE ('',( #66715 ) ) ;
#18540=EDGE_LOOP ( 'NONE', ( #47202, #8464, #23519, #43647 ) ) ;
#18541=MECHANICAL_DESIGN_GEOMETRIC_PRESENTATION_REPRESENTATION('',(#11798),#28602);
#18547=CARTESIAN_POINT ( 'NONE',  ( 1.000000000000000000, 43.00000000000000000, 35.50000000000000000 ) ) ;
#18553=( NAMED_UNIT ( * ) SI_UNIT ( $, .STERADIAN. ) SOLID_ANGLE_UNIT ( ) );
#18554=AXIS2_PLACEMENT_3D ( 'NONE', #64329, #20743, #20381 ) ;
#18559=CARTESIAN_POINT ( 'NONE',  ( 10.00000000000001954, 43.00000000000000000, 28.00000000000000355 ) ) ;
#18570=AXIS2_PLACEMENT_3D ( 'NONE', #46975, #51502, #19486 ) ;
#18573=DIRECTION ( 'NONE',  ( -0.000000000000000000, -1.000000000000000000, -0.000000000000000000 ) ) ;
#18585=ORIENTED_EDGE ( 'NONE', *, *, #49144, .F. ) ;
#18588=CARTESIAN_POINT ( 'NONE',  ( 3.000000000000030198, 35.42594141563417054, 80.00402776293826435 ) ) ;
#18592=EDGE_LOOP ( 'NONE', ( #20820, #56751, #58637, #26030 ) ) ;
#18596=CYLINDRICAL_SURFACE ( 'NONE', #55352, 3.499999999999999556 ) ;
#18602=SURFACE_STYLE_FILL_AREA ( #29109 ) ;
#18604=FILL_AREA_STYLE_COLOUR ( '', #43593 ) ;
#18610=DIRECTION ( 'NONE',  ( 1.000000000000000000, 0.000000000000000000, 0.000000000000000000 ) ) ;
#18616=VERTEX_POINT ( 'NONE', #57721 ) ;
#18628=COLOUR_RGB ( '', 0.31764706, 0.68627451, 0.89019608) ;
#18643=CARTESIAN_POINT ( 'NONE',  ( 6.000000000000017764, 43.00000000000000000, -29.49447654986460776 ) ) ;
#18647=DIRECTION ( 'NONE',  ( 0.000000000000000000, 0.000000000000000000, 1.000000000000000000 ) ) ;
#18655=FACE_OUTER_BOUND ( 'NONE', #16260, .T. ) ;
#18657=SURFACE_STYLE_USAGE ( .BOTH. , #12664 ) ;
#18665=CARTESIAN_POINT ( 'NONE',  ( 11.00000000000001776, 26.00000000000000355, -20.50000000000000355 ) ) ;
#18674=FACE_OUTER_BOUND ( 'NONE', #27324, .T. ) ;
#18678=ORIENTED_EDGE ( 'NONE', *, *, #36100, .T. ) ;
#18680=UNCERTAINTY_MEASURE_WITH_UNIT (LENGTH_MEASURE( 1.000000000000000082E-05 ), #52584, 'distance_accuracy_value', 'NONE');
#18682=EDGE_CURVE ( 'NONE', #15447, #4771, #51215, .T. ) ;
#18698=ORIENTED_EDGE ( 'NONE', *, *, #61318, .F. ) ;
#18701=CIRCLE ( 'NONE', #60220, 113.0000000000000142 ) ;
#18705=AXIS2_PLACEMENT_3D ( 'NONE', #23848, #45354, #67112 ) ;
#18709=CARTESIAN_POINT ( 'NONE',  ( 35.99999999999999289, 5.000000000000000000, 37.00402776293825724 ) ) ;
#18711=CARTESIAN_POINT ( 'NONE',  ( 32.00000000000000711, 43.00000000000000000, -36.50000000000000000 ) ) ;
#18722=EDGE_LOOP ( 'NONE', ( #16709, #45351, #39758, #33398 ) ) ;
#18727=CARTESIAN_POINT ( 'NONE',  ( 22.00000000000002132, 60.69879356856722552, 69.02971849933236115 ) ) ;
#18729=COLOUR_RGB ( '', 0.72549020, 0.75294118, 0.79215686) ;
#18746=( BOUNDED_CURVE ( )  B_SPLINE_CURVE ( 3, ( #28937, #50429, #45187, #18425 ),
 .UNSPECIFIED., .F., .F. ) 
 B_SPLINE_CURVE_WITH_KNOTS ( ( 4, 4 ),
 ( 3.874630939427412102, 4.712388980384682569 ),
 .UNSPECIFIED. ) 
 CURVE ( )  GEOMETRIC_REPRESENTATION_ITEM ( )  RATIONAL_B_SPLINE_CURVE ( ( 1.000000000000000000, 0.9423636384284016509, 0.9423636384284016509, 1.000000000000000000 ) ) 
 REPRESENTATION_ITEM ( '' )  );
#18749=CARTESIAN_POINT ( 'NONE',  ( 22.99999999999999289, 5.000000000000000000, -37.00402776293825013 ) ) ;
#18754=PRESENTATION_STYLE_ASSIGNMENT (( #45538 ) ) ;
#18763=DIRECTION ( 'NONE',  ( -0.000000000000000000, 1.000000000000000000, 0.000000000000000000 ) ) ;
#18767=PRESENTATION_STYLE_ASSIGNMENT (( #50785 ) ) ;
#18768=ORIENTED_EDGE ( 'NONE', *, *, #22695, .T. ) ;
#18781=PRESENTATION_STYLE_ASSIGNMENT (( #23036 ) ) ;
#18784=CARTESIAN_POINT ( 'NONE',  ( 24.16400019955192136, 24.76135179078163162, -27.27460947215016773 ) ) ;
#18803=DIRECTION ( 'NONE',  ( -1.000000000000000000, 0.000000000000000000, 1.300977106640434891E-16 ) ) ;
#18806=SURFACE_STYLE_FILL_AREA ( #8277 ) ;
#18817=EDGE_CURVE ( 'NONE', #55142, #59244, #37695, .T. ) ;
#18823=DIRECTION ( 'NONE',  ( 0.000000000000000000, -0.9984713486292863260, 0.05527174654752588928 ) ) ;
#18829=ORIENTED_EDGE ( 'NONE', *, *, #41490, .F. ) ;
#18843=ORIENTED_EDGE ( 'NONE', *, *, #59212, .F. ) ;
#18851=ORIENTED_EDGE ( 'NONE', *, *, #19194, .F. ) ;
#18866=( NAMED_UNIT ( * ) PLANE_ANGLE_UNIT ( ) SI_UNIT ( $, .RADIAN. ) );
#18878=PRESENTATION_STYLE_ASSIGNMENT (( #12922 ) ) ;
#18885=EDGE_LOOP ( 'NONE', ( #15605, #18001 ) ) ;
#18887=CARTESIAN_POINT ( 'NONE',  ( 36.00000000000002842, 5.000000000000000000, 77.00402776293825013 ) ) ;
#18888=ORIENTED_EDGE ( 'NONE', *, *, #41029, .F. ) ;
#18891=ORIENTED_EDGE ( 'NONE', *, *, #48167, .F. ) ;
#18895=ORIENTED_EDGE ( 'NONE', *, *, #3619, .F. ) ;
#18897=( NAMED_UNIT ( * ) SI_UNIT ( $, .STERADIAN. ) SOLID_ANGLE_UNIT ( ) );
#18903=AXIS2_PLACEMENT_3D ( 'NONE', #50430, #2156, #8572 ) ;
#18904=CIRCLE ( 'NONE', #7670, 1.000000000000000888 ) ;
#18910=CARTESIAN_POINT ( 'NONE',  ( 32.00000000000001421, 42.00000000000000000, 36.50000000000000000 ) ) ;
#18918=CARTESIAN_POINT ( 'NONE',  ( 36.00000000000002842, 5.000000000000000000, 32.00402776293825724 ) ) ;
#18921=STYLED_ITEM ( 'NONE', ( #63573 ), #1027 ) ;
#18924=ORIENTED_EDGE ( 'NONE', *, *, #381, .F. ) ;
#18925=ORIENTED_EDGE ( 'NONE', *, *, #17957, .T. ) ;
#18935=PLANE ( 'NONE',  #58800 ) ;
#18940=( LENGTH_UNIT ( ) NAMED_UNIT ( * ) SI_UNIT ( .MILLI., .METRE. ) );
#18943=CARTESIAN_POINT ( 'NONE',  ( 22.00000000000000355, 42.00000000000000000, -75.00000000000001421 ) ) ;
#18950=SURFACE_STYLE_USAGE ( .BOTH. , #2382 ) ;
#18960=EDGE_CURVE ( 'NONE', #6374, #8081, #47469, .T. ) ;
#18961=CYLINDRICAL_SURFACE ( 'NONE', #28020, 113.0000000000000142 ) ;
#18971=ORIENTED_EDGE ( 'NONE', *, *, #17731, .T. ) ;
#18974=( LENGTH_UNIT ( ) NAMED_UNIT ( * ) SI_UNIT ( .MILLI., .METRE. ) );
#18977=CARTESIAN_POINT ( 'NONE',  ( 57.00000000000000000, 0.000000000000000000, 60.00402776293825724 ) ) ;
#18983=SURFACE_SIDE_STYLE ('',( #45775 ) ) ;
#18985=SURFACE_STYLE_USAGE ( .BOTH. , #2060 ) ;
#18988=CIRCLE ( 'NONE', #47178, 25.00000000000001421 ) ;
#18991=CARTESIAN_POINT ( 'NONE',  ( 57.00000000000000000, 5.000000000000000000, -60.00402776293825724 ) ) ;
#18993=AXIS2_PLACEMENT_3D ( 'NONE', #26551, #48764, #10744 ) ;
#19006=AXIS2_PLACEMENT_3D ( 'NONE', #32143, #15641, #58528 ) ;
#19007=CARTESIAN_POINT ( 'NONE',  ( 8.000000000000000000, 5.000000000000000000, -72.00402776293825013 ) ) ;
#19024=FILL_AREA_STYLE ('',( #35589 ) ) ;
#19025=CARTESIAN_POINT ( 'NONE',  ( 28.00000000000000000, 38.70020753820971748, -89.00000000000000000 ) ) ;
#19026=DIRECTION ( 'NONE',  ( -0.000000000000000000, -1.000000000000000000, -0.000000000000000000 ) ) ;
#19030=FILL_AREA_STYLE ('',( #57036 ) ) ;
#19031=SURFACE_STYLE_USAGE ( .BOTH. , #6757 ) ;
#19046=ORIENTED_EDGE ( 'NONE', *, *, #44618, .T. ) ;
#19048=FILL_AREA_STYLE_COLOUR ( '', #33022 ) ;
#19065=DIRECTION ( 'NONE',  ( -0.000000000000000000, -0.000000000000000000, -1.000000000000000000 ) ) ;
#19069=DIRECTION ( 'NONE',  ( 0.000000000000000000, 0.000000000000000000, 1.000000000000000000 ) ) ;
#19073=ORIENTED_EDGE ( 'NONE', *, *, #11431, .F. ) ;
#19075=AXIS2_PLACEMENT_3D ( 'NONE', #13327, #2014, #66459 ) ;
#19089=DIRECTION ( 'NONE',  ( 0.000000000000000000, 0.000000000000000000, 1.000000000000000000 ) ) ;
#19107=AXIS2_PLACEMENT_3D ( 'NONE', #23067, #18127, #49797 ) ;
#19110=CARTESIAN_POINT ( 'NONE',  ( 24.50574400633172090, 25.15110077572983371, -27.39850243389338402 ) ) ;
#19114=EDGE_CURVE ( 'NONE', #31521, #330, #19638, .T. ) ;
#19126=VECTOR ( 'NONE', #13239, 1000.000000000000000 ) ;
#19127=CARTESIAN_POINT ( 'NONE',  ( 30.99999999999998579, 5.000000000000000000, -72.00402776293822171 ) ) ;
#19129=EDGE_CURVE ( 'NONE', #39359, #68708, #35089, .T. ) ;
#19133=ORIENTED_EDGE ( 'NONE', *, *, #25182, .T. ) ;
#19160=DIRECTION ( 'NONE',  ( 0.000000000000000000, 1.000000000000000000, 0.000000000000000000 ) ) ;
#19161=ORIENTED_EDGE ( 'NONE', *, *, #38326, .T. ) ;
#19171=FACE_OUTER_BOUND ( 'NONE', #12014, .T. ) ;
#19172=( GEOMETRIC_REPRESENTATION_CONTEXT ( 3 ) GLOBAL_UNCERTAINTY_ASSIGNED_CONTEXT ( ( #45319 ) ) GLOBAL_UNIT_ASSIGNED_CONTEXT ( ( #61008, #34291, #7894 ) ) REPRESENTATION_CONTEXT ( 'NONE', 'WORKASPACE' ) );
#19179=( NAMED_UNIT ( * ) SI_UNIT ( $, .STERADIAN. ) SOLID_ANGLE_UNIT ( ) );
#19181=COLOUR_RGB ( '', 0.31764706, 0.68627451, 0.89019608) ;
#19182=FACE_OUTER_BOUND ( 'NONE', #51383, .T. ) ;
#19188=DIRECTION ( 'NONE',  ( 1.000000000000000000, -0.000000000000000000, -1.300977106640434891E-16 ) ) ;
#19191=AXIS2_PLACEMENT_3D ( 'NONE', #47859, #53426, #15463 ) ;
#19192=CYLINDRICAL_SURFACE ( 'NONE', #61299, 5.000000000000004441 ) ;
#19194=EDGE_CURVE ( 'NONE', #53011, #24720, #8328, .T. ) ;
#19201=EDGE_CURVE ( 'NONE', #48456, #37266, #5905, .T. ) ;
#19212=MECHANICAL_DESIGN_GEOMETRIC_PRESENTATION_REPRESENTATION('',(#10263),#37262);
#19216=CARTESIAN_POINT ( 'NONE',  ( 0.000000000000000000, 42.00000000000000000, -44.99999999999999289 ) ) ;
#19228=VECTOR ( 'NONE', #34827, 1000.000000000000000 ) ;
#19230=CARTESIAN_POINT ( 'NONE',  ( 22.00000000000002132, 42.47058823529412308, 74.11764705882352189 ) ) ;
#19231=( NAMED_UNIT ( * ) SI_UNIT ( $, .STERADIAN. ) SOLID_ANGLE_UNIT ( ) );
#19235=SURFACE_STYLE_FILL_AREA ( #9419 ) ;
#19247=( NAMED_UNIT ( * ) PLANE_ANGLE_UNIT ( ) SI_UNIT ( $, .RADIAN. ) );
#19255=CARTESIAN_POINT ( 'NONE',  ( 2.000000000000008882, 26.00000000000000355, -24.00000000000000355 ) ) ;
#19257=AXIS2_PLACEMENT_3D ( 'NONE', #14120, #3145, #35579 ) ;
#19264=LINE ( 'NONE', #4115, #5814 ) ;
#19282=( NAMED_UNIT ( * ) PLANE_ANGLE_UNIT ( ) SI_UNIT ( $, .RADIAN. ) );
#19296=FACE_OUTER_BOUND ( 'NONE', #57403, .T. ) ;
#19303=STYLED_ITEM ( 'NONE', ( #31878 ), #22304 ) ;
#19304=SURFACE_STYLE_FILL_AREA ( #35153 ) ;
#19305=EDGE_CURVE ( 'NONE', #56838, #68708, #44400, .T. ) ;
#19312=EDGE_CURVE ( 'NONE', #14021, #41380, #50540, .T. ) ;
#19314=TOROIDAL_SURFACE ( 'NONE', #63114, 18.99999999999998934, 1.000000000000000000 ) ;
#19320=DIRECTION ( 'NONE',  ( -0.000000000000000000, -1.000000000000000000, -0.000000000000000000 ) ) ;
#19340=CARTESIAN_POINT ( 'NONE',  ( 31.00000000000000711, 15.00000000000000000, -35.50000000000000000 ) ) ;
#19356=STYLED_ITEM ( 'NONE', ( #55945 ), #22725 ) ;
#19359=CARTESIAN_POINT ( 'NONE',  ( 23.50000000000001776, 15.00000000000000000, 29.68999999999999417 ) ) ;
#19361=DIRECTION ( 'NONE',  ( 0.000000000000000000, 0.000000000000000000, 1.000000000000000000 ) ) ;
#19365=UNCERTAINTY_MEASURE_WITH_UNIT (LENGTH_MEASURE( 1.000000000000000082E-05 ), #36821, 'distance_accuracy_value', 'NONE');
#19372=ORIENTED_EDGE ( 'NONE', *, *, #27603, .T. ) ;
#19378=EDGE_CURVE ( 'NONE', #62177, #59244, #25011, .T. ) ;
#19387=CYLINDRICAL_SURFACE ( 'NONE', #57117, 4.999999999999997335 ) ;
#19389=CARTESIAN_POINT ( 'NONE',  ( 23.50000000000001776, 27.44010416289936316, -27.18999999999999417 ) ) ;
#19396=FACE_OUTER_BOUND ( 'NONE', #46735, .T. ) ;
#19397=AXIS2_PLACEMENT_3D ( 'NONE', #3405, #61830, #13302 ) ;
#19402=COLOUR_RGB ( '', 0.72549020, 0.75294118, 0.79215686) ;
#19411=ORIENTED_EDGE ( 'NONE', *, *, #42173, .F. ) ;
#19427=ORIENTED_EDGE ( 'NONE', *, *, #9760, .F. ) ;
#19428=DIRECTION ( 'NONE',  ( 0.000000000000000000, 0.000000000000000000, -1.000000000000000000 ) ) ;
#19429=CARTESIAN_POINT ( 'NONE',  ( 57.00000000000000000, 0.9999999999999991118, -80.00402776293826435 ) ) ;
#19431=AXIS2_PLACEMENT_3D ( 'NONE', #60137, #64379, #638 ) ;
#19441=( LENGTH_UNIT ( ) NAMED_UNIT ( * ) SI_UNIT ( .MILLI., .METRE. ) );
#19448=CARTESIAN_POINT ( 'NONE',  ( 31.53557424407129517, 42.85561152959481035, 45.52242327283500600 ) ) ;
#19459=ORIENTED_EDGE ( 'NONE', *, *, #7955, .F. ) ;
#19469=STYLED_ITEM ( 'NONE', ( #12929 ), #31034 ) ;
#19481=PRESENTATION_STYLE_ASSIGNMENT (( #30361 ) ) ;
#19482=DIRECTION ( 'NONE',  ( -1.000000000000000000, 0.000000000000000000, -4.625929269271509580E-16 ) ) ;
#19486=DIRECTION ( 'NONE',  ( 0.000000000000000000, 0.000000000000000000, -1.000000000000000000 ) ) ;
#19487=AXIS2_PLACEMENT_3D ( 'NONE', #30833, #63204, #31872 ) ;
#19496=VECTOR ( 'NONE', #55271, 1000.000000000000000 ) ;
#19498=DIRECTION ( 'NONE',  ( -1.000000000000000000, 0.000000000000000000, 1.300977106640434891E-16 ) ) ;
#19499=( NAMED_UNIT ( * ) PLANE_ANGLE_UNIT ( ) SI_UNIT ( $, .RADIAN. ) );
#19509=PRESENTATION_STYLE_ASSIGNMENT (( #46293 ) ) ;
#19511=DIRECTION ( 'NONE',  ( 0.000000000000000000, 0.000000000000000000, -1.000000000000000000 ) ) ;
#19525=CIRCLE ( 'NONE', #58863, 111.0000000000000142 ) ;
#19527=FILL_AREA_STYLE ('',( #46674 ) ) ;
#19538=ADVANCED_FACE ( 'NONE', ( #32896 ), #10746, .T. ) ;
#19539=VERTEX_POINT ( 'NONE', #61337 ) ;
#19542=MECHANICAL_DESIGN_GEOMETRIC_PRESENTATION_REPRESENTATION('',(#48818),#18460);
#19546=SURFACE_STYLE_USAGE ( .BOTH. , #67746 ) ;
#19549=EDGE_CURVE ( 'NONE', #4398, #56593, #18450, .T. ) ;
#19556=SURFACE_SIDE_STYLE ('',( #35750 ) ) ;
#19577=AXIS2_PLACEMENT_3D ( 'NONE', #67998, #19783, #41277 ) ;
#19591=DIRECTION ( 'NONE',  ( -1.000000000000000000, 0.000000000000000000, 1.300977106640434891E-16 ) ) ;
#19595=SURFACE_STYLE_USAGE ( .BOTH. , #63210 ) ;
#19599=VECTOR ( 'NONE', #40825, 1000.000000000000000 ) ;
#19602=DIRECTION ( 'NONE',  ( 0.000000000000000000, -1.000000000000000000, 0.000000000000000000 ) ) ;
#19603=EDGE_LOOP ( 'NONE', ( #33492, #11375, #30891, #16036 ) ) ;
#19606=SURFACE_STYLE_FILL_AREA ( #46751 ) ;
#19612=FILL_AREA_STYLE ('',( #36173 ) ) ;
#19614=ORIENTED_EDGE ( 'NONE', *, *, #60940, .T. ) ;
#19621=EDGE_CURVE ( 'NONE', #44068, #44052, #10020, .T. ) ;
#19623=DIRECTION ( 'NONE',  ( 0.000000000000000000, 1.000000000000000000, 0.000000000000000000 ) ) ;
#19632=( GEOMETRIC_REPRESENTATION_CONTEXT ( 3 ) GLOBAL_UNCERTAINTY_ASSIGNED_CONTEXT ( ( #29218 ) ) GLOBAL_UNIT_ASSIGNED_CONTEXT ( ( #64266, #5495, #21709 ) ) REPRESENTATION_CONTEXT ( 'NONE', 'WORKASPACE' ) );
#19634=EDGE_CURVE ( 'NONE', #6374, #2941, #40258, .T. ) ;
#19637=EDGE_LOOP ( 'NONE', ( #24978, #58753, #1824, #54798 ) ) ;
#19638=LINE ( 'NONE', #14355, #54222 ) ;
#19654=FILL_AREA_STYLE_COLOUR ( '', #56034 ) ;
#19655=PRESENTATION_STYLE_ASSIGNMENT (( #67862 ) ) ;
#19659=CARTESIAN_POINT ( 'NONE',  ( 98.00000000000000000, 5.000000000000000000, -5.000000000000004441 ) ) ;
#19674=FILL_AREA_STYLE ('',( #7729 ) ) ;
#19689=EDGE_CURVE ( 'NONE', #62580, #3143, #28260, .T. ) ;
#19690=COLOUR_RGB ( '', 0.09019608, 0.27058824, 0.51372549) ;
#19692=ADVANCED_FACE ( 'NONE', ( #65583 ), #6837, .F. ) ;
#19700=SURFACE_STYLE_FILL_AREA ( #46843 ) ;
#19701=ORIENTED_EDGE ( 'NONE', *, *, #12980, .T. ) ;
#19702=DIRECTION ( 'NONE',  ( 0.000000000000000000, 0.000000000000000000, -1.000000000000000000 ) ) ;
#19711=FILL_AREA_STYLE ('',( #46494 ) ) ;
#19714=EDGE_LOOP ( 'NONE', ( #1969, #45870, #45114, #16720, #9242, #8654 ) ) ;
#19726=CARTESIAN_POINT ( 'NONE',  ( 30.99999999999998579, 0.000000000000000000, -72.00402776293822171 ) ) ;
#19738=STYLED_ITEM ( 'NONE', ( #8671 ), #8539 ) ;
#19742=DIRECTION ( 'NONE',  ( -4.625929269271509580E-16, 0.000000000000000000, 1.000000000000000000 ) ) ;
#19769=SURFACE_STYLE_USAGE ( .BOTH. , #9928 ) ;
#19773=EDGE_CURVE ( 'NONE', #12357, #42679, #55557, .T. ) ;
#19776=DIRECTION ( 'NONE',  ( -0.000000000000000000, -1.000000000000000000, -0.000000000000000000 ) ) ;
#19778=( NAMED_UNIT ( * ) SI_UNIT ( $, .STERADIAN. ) SOLID_ANGLE_UNIT ( ) );
#19779=CARTESIAN_POINT ( 'NONE',  ( 57.00000000000000000, 5.000000000000000000, -77.00402776293825013 ) ) ;
#19783=DIRECTION ( 'NONE',  ( -0.000000000000000000, -1.000000000000000000, 0.000000000000000000 ) ) ;
#19793=ADVANCED_FACE ( 'NONE', ( #10998 ), #58503, .F. ) ;
#19805=PRESENTATION_STYLE_ASSIGNMENT (( #40595 ) ) ;
#19810=AXIS2_PLACEMENT_3D ( 'NONE', #38341, #64691, #22122 ) ;
#19815=( GEOMETRIC_REPRESENTATION_CONTEXT ( 3 ) GLOBAL_UNCERTAINTY_ASSIGNED_CONTEXT ( ( #65127 ) ) GLOBAL_UNIT_ASSIGNED_CONTEXT ( ( #45550, #24046, #3228 ) ) REPRESENTATION_CONTEXT ( 'NONE', 'WORKASPACE' ) );
#19833=FILL_AREA_STYLE ('',( #55743 ) ) ;
#19837=SURFACE_STYLE_FILL_AREA ( #69422 ) ;
#19838=EDGE_CURVE ( 'NONE', #55848, #33948, #55192, .T. ) ;
#19839=AXIS2_PLACEMENT_3D ( 'NONE', #27807, #49311, #61235 ) ;
#19845=SURFACE_SIDE_STYLE ('',( #8956 ) ) ;
#19847=CARTESIAN_POINT ( 'NONE',  ( 27.00000000000001776, 15.00000000000000000, 34.49999999999998579 ) ) ;
#19852=ADVANCED_FACE ( 'NONE', ( #67859 ), #24572, .T. ) ;
#19853=VERTEX_POINT ( 'NONE', #35838 ) ;
#19854=DIRECTION ( 'NONE',  ( -0.000000000000000000, -1.000000000000000000, 0.000000000000000000 ) ) ;
#19857=CARTESIAN_POINT ( 'NONE',  ( 8.000000000000000000, 0.000000000000000000, 72.00402776293825013 ) ) ;
#19861=SURFACE_STYLE_USAGE ( .BOTH. , #55770 ) ;
#19867=( LENGTH_UNIT ( ) NAMED_UNIT ( * ) SI_UNIT ( .MILLI., .METRE. ) );
#19877=( GEOMETRIC_REPRESENTATION_CONTEXT ( 3 ) GLOBAL_UNCERTAINTY_ASSIGNED_CONTEXT ( ( #60066 ) ) GLOBAL_UNIT_ASSIGNED_CONTEXT ( ( #42293, #4934, #26033 ) ) REPRESENTATION_CONTEXT ( 'NONE', 'WORKASPACE' ) );
#19900=( NAMED_UNIT ( * ) SI_UNIT ( $, .STERADIAN. ) SOLID_ANGLE_UNIT ( ) );
#19907=UNCERTAINTY_MEASURE_WITH_UNIT (LENGTH_MEASURE( 1.000000000000000082E-05 ), #5522, 'distance_accuracy_value', 'NONE');
#19915=SURFACE_STYLE_FILL_AREA ( #9036 ) ;
#19919=FILL_AREA_STYLE ('',( #46727 ) ) ;
#19920=CARTESIAN_POINT ( 'NONE',  ( 22.00000000000002132, 42.47058823529412308, 74.11764705882352189 ) ) ;
#19921=VECTOR ( 'NONE', #67121, 1000.000000000000000 ) ;
#19926=CARTESIAN_POINT ( 'NONE',  ( 36.00000000000002132, 5.000000000000000000, -77.00402776293825013 ) ) ;
#19928=VERTEX_POINT ( 'NONE', #56943 ) ;
#19929=ORIENTED_EDGE ( 'NONE', *, *, #61932, .F. ) ;
#19940=AXIS2_PLACEMENT_3D ( 'NONE', #38704, #39721, #28411 ) ;
#19948=SURFACE_STYLE_USAGE ( .BOTH. , #41808 ) ;
#19955=ORIENTED_EDGE ( 'NONE', *, *, #52459, .T. ) ;
#19990=ADVANCED_FACE ( 'NONE', ( #42537 ), #48159, .T. ) ;
#19992=( LENGTH_UNIT ( ) NAMED_UNIT ( * ) SI_UNIT ( .MILLI., .METRE. ) );
#20003=SURFACE_STYLE_USAGE ( .BOTH. , #52412 ) ;
#20007=SURFACE_STYLE_USAGE ( .BOTH. , #24950 ) ;
#20008=ORIENTED_EDGE ( 'NONE', *, *, #10985, .F. ) ;
#20009=CIRCLE ( 'NONE', #23382, 1.000000000000000888 ) ;
#20012=CARTESIAN_POINT ( 'NONE',  ( 31.00000000000002132, 42.00000000000000711, 75.00000000000000000 ) ) ;
#20013=UNCERTAINTY_MEASURE_WITH_UNIT (LENGTH_MEASURE( 1.000000000000000082E-05 ), #7308, 'distance_accuracy_value', 'NONE');
#20016=CARTESIAN_POINT ( 'NONE',  ( 3.000000000000030198, 34.36176364315826248, 80.00402776293826435 ) ) ;
#20019=ORIENTED_EDGE ( 'NONE', *, *, #60264, .F. ) ;
#20022=( NAMED_UNIT ( * ) SI_UNIT ( $, .STERADIAN. ) SOLID_ANGLE_UNIT ( ) );
#20026=VERTEX_POINT ( 'NONE', #54076 ) ;
#20027=COLOUR_RGB ( '', 0.66274510, 0.83137255, 0.94901961) ;
#20031=ORIENTED_EDGE ( 'NONE', *, *, #47050, .T. ) ;
#20043=CARTESIAN_POINT ( 'NONE',  ( 28.58578643762692550, 34.36176364315826248, 80.00402776293826435 ) ) ;
#20059=CARTESIAN_POINT ( 'NONE',  ( 22.84125995469108972, 24.77021312349235771, 27.27736960510218367 ) ) ;
#20064=( NAMED_UNIT ( * ) PLANE_ANGLE_UNIT ( ) SI_UNIT ( $, .RADIAN. ) );
#20065=DIRECTION ( 'NONE',  ( 1.000000000000000000, 0.000000000000000000, -1.300977106640434891E-16 ) ) ;
#20073=DIRECTION ( 'NONE',  ( 0.000000000000000000, -1.000000000000000000, 0.000000000000000000 ) ) ;
#20078=DIRECTION ( 'NONE',  ( -0.000000000000000000, -1.000000000000000000, 0.000000000000000000 ) ) ;
#20082=ORIENTED_EDGE ( 'NONE', *, *, #62254, .F. ) ;
#20085=CARTESIAN_POINT ( 'NONE',  ( 36.00000000000002842, 5.000000000000000000, 29.00402776293825724 ) ) ;
#20087=DIRECTION ( 'NONE',  ( -1.239088197126289584E-16, 0.000000000000000000, -1.000000000000000000 ) ) ;
#20096=( LENGTH_UNIT ( ) NAMED_UNIT ( * ) SI_UNIT ( .MILLI., .METRE. ) );
#20101=CARTESIAN_POINT ( 'NONE',  ( 0.000000000000000000, 42.00000000000000000, -44.99999999999999289 ) ) ;
#20105=CIRCLE ( 'NONE', #44916, 5.000000000000004441 ) ;
#20107=CARTESIAN_POINT ( 'NONE',  ( 22.00000000000002132, 50.00000000000000000, 46.00000000000000000 ) ) ;
#20110=ORIENTED_EDGE ( 'NONE', *, *, #41018, .F. ) ;
#20119=CARTESIAN_POINT ( 'NONE',  ( 6.000000000000017764, 43.00000000000000000, 29.49447654986459710 ) ) ;
#20121=CARTESIAN_POINT ( 'NONE',  ( 3.414213562373098032, 42.99999999999999289, -79.58981420056515788 ) ) ;
#20132=( NAMED_UNIT ( * ) PLANE_ANGLE_UNIT ( ) SI_UNIT ( $, .RADIAN. ) );
#20145=( GEOMETRIC_REPRESENTATION_CONTEXT ( 3 ) GLOBAL_UNCERTAINTY_ASSIGNED_CONTEXT ( ( #53028 ) ) GLOBAL_UNIT_ASSIGNED_CONTEXT ( ( #57161, #3670, #2243 ) ) REPRESENTATION_CONTEXT ( 'NONE', 'WORKASPACE' ) );
#20146=TOROIDAL_SURFACE ( 'NONE', #59453, 17.00000000000000355, 1.000000000000000000 ) ;
#20150=EDGE_CURVE ( 'NONE', #61901, #7256, #40710, .T. ) ;
#20177=DIRECTION ( 'NONE',  ( 0.000000000000000000, 1.000000000000000000, 0.000000000000000000 ) ) ;
#20188=( NAMED_UNIT ( * ) SI_UNIT ( $, .STERADIAN. ) SOLID_ANGLE_UNIT ( ) );
#20199=CARTESIAN_POINT ( 'NONE',  ( 23.50000000000001776, 15.00000000000000000, 29.68999999999999417 ) ) ;
#20208=CARTESIAN_POINT ( 'NONE',  ( 35.99999999999999289, 5.000000000000000000, -37.00402776293825724 ) ) ;
#20209=CARTESIAN_POINT ( 'NONE',  ( 12.00000000000001776, 15.00000000000000000, -60.00402776293827145 ) ) ;
#20213=ORIENTED_EDGE ( 'NONE', *, *, #66636, .T. ) ;
#20222=ORIENTED_EDGE ( 'NONE', *, *, #6663, .T. ) ;
#20224=DIRECTION ( 'NONE',  ( 0.000000000000000000, 1.000000000000000000, -0.000000000000000000 ) ) ;
#20236=( GEOMETRIC_REPRESENTATION_CONTEXT ( 3 ) GLOBAL_UNCERTAINTY_ASSIGNED_CONTEXT ( ( #41179 ) ) GLOBAL_UNIT_ASSIGNED_CONTEXT ( ( #12292, #44719, #16924 ) ) REPRESENTATION_CONTEXT ( 'NONE', 'WORKASPACE' ) );
#20247=( NAMED_UNIT ( * ) PLANE_ANGLE_UNIT ( ) SI_UNIT ( $, .RADIAN. ) );
#20248=EDGE_CURVE ( 'NONE', #18094, #40178, #25528, .T. ) ;
#20263=CARTESIAN_POINT ( 'NONE',  ( 3.414213562373125121, 34.36176364315826248, 80.00402776293826435 ) ) ;
#20270=MECHANICAL_DESIGN_GEOMETRIC_PRESENTATION_REPRESENTATION('',(#41660),#62948);
#20271=FACE_OUTER_BOUND ( 'NONE', #46459, .T. ) ;
#20278=DIRECTION ( 'NONE',  ( 0.000000000000000000, 0.000000000000000000, -1.000000000000000000 ) ) ;
#20282=FILL_AREA_STYLE_COLOUR ( '', #58824 ) ;
#20286=FACE_OUTER_BOUND ( 'NONE', #45062, .T. ) ;
#20289=DIRECTION ( 'NONE',  ( 0.000000000000000000, 0.000000000000000000, -1.000000000000000000 ) ) ;
#20290=SURFACE_STYLE_USAGE ( .BOTH. , #57953 ) ;
#20302=CIRCLE ( 'NONE', #22583, 18.99999999999998934 ) ;
#20309=ORIENTED_EDGE ( 'NONE', *, *, #50376, .T. ) ;
#20314=CARTESIAN_POINT ( 'NONE',  ( 10.00000000000001776, 42.74314482547740113, 27.71473342867655987 ) ) ;
#20327=( GEOMETRIC_REPRESENTATION_CONTEXT ( 3 ) GLOBAL_UNCERTAINTY_ASSIGNED_CONTEXT ( ( #309 ) ) GLOBAL_UNIT_ASSIGNED_CONTEXT ( ( #35446, #35079, #30125 ) ) REPRESENTATION_CONTEXT ( 'NONE', 'WORKASPACE' ) );
#20328=VERTEX_POINT ( 'NONE', #42461 ) ;
#20329=DIRECTION ( 'NONE',  ( -1.982541115402069054E-16, -0.000000000000000000, -1.000000000000000000 ) ) ;
#20335=EDGE_CURVE ( 'NONE', #21181, #40347, #26565, .T. ) ;
#20338=PLANE ( 'NONE',  #60496 ) ;
#20347=( LENGTH_UNIT ( ) NAMED_UNIT ( * ) SI_UNIT ( .MILLI., .METRE. ) );
#20353=AXIS2_PLACEMENT_3D ( 'NONE', #1793, #51095, #66926 ) ;
#20357=ORIENTED_EDGE ( 'NONE', *, *, #46346, .T. ) ;
#20363=CARTESIAN_POINT ( 'NONE',  ( 31.00000000000002132, 43.00000000000000000, 79.00402776293823592 ) ) ;
#20364=AXIS2_PLACEMENT_3D ( 'NONE', #24007, #45516, #40915 ) ;
#20378=VERTEX_POINT ( 'NONE', #62474 ) ;
#20381=DIRECTION ( 'NONE',  ( 0.000000000000000000, -0.000000000000000000, -1.000000000000000000 ) ) ;
#20391=VERTEX_POINT ( 'NONE', #31146 ) ;
#20396=ORIENTED_EDGE ( 'NONE', *, *, #40370, .T. ) ;
#20398=CARTESIAN_POINT ( 'NONE',  ( 4.000000000000002665, 43.00000000000000000, -90.00000000000000000 ) ) ;
#20402=DIRECTION ( 'NONE',  ( -1.300977106640434891E-16, 0.000000000000000000, -1.000000000000000000 ) ) ;
#20414=ADVANCED_FACE ( 'NONE', ( #25874 ), #41761, .F. ) ;
#20417=DIRECTION ( 'NONE',  ( 1.000000000000000000, 0.000000000000000000, -1.300977106640434891E-16 ) ) ;
#20422=AXIS2_PLACEMENT_3D ( 'NONE', #41804, #62852, #63223 ) ;
#20427=SURFACE_SIDE_STYLE ('',( #5964 ) ) ;
#20441=FILL_AREA_STYLE_COLOUR ( '', #49937 ) ;
#20442=CARTESIAN_POINT ( 'NONE',  ( 22.00000000000002132, 50.00000000000000000, 59.99999999999999289 ) ) ;
#20447=( LENGTH_UNIT ( ) NAMED_UNIT ( * ) SI_UNIT ( .MILLI., .METRE. ) );
#20448=COLOUR_RGB ( '', 0.40784314, 0.44705882, 0.49803922) ;
#20454=( LENGTH_UNIT ( ) NAMED_UNIT ( * ) SI_UNIT ( .MILLI., .METRE. ) );
#20463=VECTOR ( 'NONE', #44381, 1000.000000000000000 ) ;
#20466=MECHANICAL_DESIGN_GEOMETRIC_PRESENTATION_REPRESENTATION('',(#49701),#43013);
#20475=FILL_AREA_STYLE_COLOUR ( '', #40573 ) ;
#20478=CARTESIAN_POINT ( 'NONE',  ( 0.8561458320465511473, 42.99999999999999289, -74.38749456993816978 ) ) ;
#20488=MECHANICAL_DESIGN_GEOMETRIC_PRESENTATION_REPRESENTATION('',(#30555),#171);
#20491=DIRECTION ( 'NONE',  ( 0.000000000000000000, 0.000000000000000000, 1.000000000000000000 ) ) ;
#20494=FILL_AREA_STYLE_COLOUR ( '', #21000 ) ;
#20501=( GEOMETRIC_REPRESENTATION_CONTEXT ( 3 ) GLOBAL_UNCERTAINTY_ASSIGNED_CONTEXT ( ( #49731 ) ) GLOBAL_UNIT_ASSIGNED_CONTEXT ( ( #25437, #54915, #10654 ) ) REPRESENTATION_CONTEXT ( 'NONE', 'WORKASPACE' ) );
#20508=CARTESIAN_POINT ( 'NONE',  ( 10.00000000000000533, 50.00000000000000000, -60.00000000000000000 ) ) ;
#20511=FACE_OUTER_BOUND ( 'NONE', #54132, .T. ) ;
#20519=EDGE_CURVE ( 'NONE', #38534, #1374, #67330, .T. ) ;
#20525=CARTESIAN_POINT ( 'NONE',  ( 1.000000000000000000, 42.00000000000000000, 79.00402776293826435 ) ) ;
#20527=CARTESIAN_POINT ( 'NONE',  ( 22.00000000000002132, 43.00000000000000000, -29.68999999999999417 ) ) ;
#20529=AXIS2_PLACEMENT_3D ( 'NONE', #29191, #2420, #52086 ) ;
#20532=CARTESIAN_POINT ( 'NONE',  ( 28.00000000000000000, 43.00000000000000000, -79.00402776293826435 ) ) ;
#20559=PRESENTATION_STYLE_ASSIGNMENT (( #68406 ) ) ;
#20561=ORIENTED_EDGE ( 'NONE', *, *, #24101, .T. ) ;
#20562=DIRECTION ( 'NONE',  ( -0.000000000000000000, -1.000000000000000000, -0.000000000000000000 ) ) ;
#20567=EDGE_CURVE ( 'NONE', #51461, #31418, #24619, .T. ) ;
#20580=EDGE_CURVE ( 'NONE', #45878, #66425, #1521, .T. ) ;
#20585=CARTESIAN_POINT ( 'NONE',  ( 57.00000000000000000, 5.000000000000000000, -65.00402776293825013 ) ) ;
#20622=CARTESIAN_POINT ( 'NONE',  ( 3.000000000000030198, 35.42594141563417054, 80.00402776293826435 ) ) ;
#20628=( NAMED_UNIT ( * ) PLANE_ANGLE_UNIT ( ) SI_UNIT ( $, .RADIAN. ) );
#20632=CARTESIAN_POINT ( 'NONE',  ( 92.41620014002536720, 5.000000000000000000, 29.00402776293826079 ) ) ;
#20637=DIRECTION ( 'NONE',  ( 0.000000000000000000, 1.000000000000000000, -0.000000000000000000 ) ) ;
#20639=ORIENTED_EDGE ( 'NONE', *, *, #47063, .F. ) ;
#20641=PLANE ( 'NONE',  #19487 ) ;
#20644=CIRCLE ( 'NONE', #2616, 1.000000000000000888 ) ;
#20645=CIRCLE ( 'NONE', #59956, 5.000000000000000888 ) ;
#20648=CARTESIAN_POINT ( 'NONE',  ( 22.91454444302602411, 24.72107417156074760, -27.25824408850648695 ) ) ;
#20649=ORIENTED_EDGE ( 'NONE', *, *, #68891, .F. ) ;
#20668=ADVANCED_FACE ( 'NONE', ( #30717 ), #49414, .F. ) ;
#20674=DIRECTION ( 'NONE',  ( -4.516179008354028246E-16, 0.000000000000000000, 1.000000000000000000 ) ) ;
#20704=CIRCLE ( 'NONE', #21808, 1.000000000000000888 ) ;
#20705=FILL_AREA_STYLE ('',( #4489 ) ) ;
#20713=CIRCLE ( 'NONE', #44360, 22.00000000000001421 ) ;
#20717=UNCERTAINTY_MEASURE_WITH_UNIT (LENGTH_MEASURE( 1.000000000000000082E-05 ), #1473, 'distance_accuracy_value', 'NONE');
#20722=AXIS2_PLACEMENT_3D ( 'NONE', #8784, #35169, #40470 ) ;
#20731=AXIS2_PLACEMENT_3D ( 'NONE', #16605, #38067, #59461 ) ;
#20739=SURFACE_STYLE_USAGE ( .BOTH. , #36253 ) ;
#20743=DIRECTION ( 'NONE',  ( 0.000000000000000000, -1.000000000000000000, 0.000000000000000000 ) ) ;
#20750=DIRECTION ( 'NONE',  ( 0.000000000000000000, 0.000000000000000000, -1.000000000000000000 ) ) ;
#20752=FACE_OUTER_BOUND ( 'NONE', #31719, .T. ) ;
#20753=STYLED_ITEM ( 'NONE', ( #46886 ), #27294 ) ;
#20767=ORIENTED_EDGE ( 'NONE', *, *, #38509, .F. ) ;
#20771=AXIS2_PLACEMENT_3D ( 'NONE', #24269, #33862, #61899 ) ;
#20776=SURFACE_SIDE_STYLE ('',( #49236 ) ) ;
#20783=ORIENTED_EDGE ( 'NONE', *, *, #1587, .F. ) ;
#20784=DIRECTION ( 'NONE',  ( 0.000000000000000000, 0.000000000000000000, -1.000000000000000000 ) ) ;
#20792=FILL_AREA_STYLE_COLOUR ( '', #36302 ) ;
#20795=DIRECTION ( 'NONE',  ( -0.000000000000000000, -1.000000000000000000, -0.000000000000000000 ) ) ;
#20806=DIRECTION ( 'NONE',  ( 0.000000000000000000, 0.000000000000000000, 1.000000000000000000 ) ) ;
#20813=PRESENTATION_STYLE_ASSIGNMENT (( #36327 ) ) ;
#20820=ORIENTED_EDGE ( 'NONE', *, *, #30147, .F. ) ;
#20827=EDGE_CURVE ( 'NONE', #5819, #13735, #29924, .T. ) ;
#20829=CARTESIAN_POINT ( 'NONE',  ( 27.00000000000001776, -60.04052944165106709, -35.50000000000000000 ) ) ;
#20830=CARTESIAN_POINT ( 'NONE',  ( 10.00000000000001954, 43.00000000000000000, -29.68999999999999417 ) ) ;
#20848=UNCERTAINTY_MEASURE_WITH_UNIT (LENGTH_MEASURE( 1.000000000000000082E-05 ), #64198, 'distance_accuracy_value', 'NONE');
#20849=CARTESIAN_POINT ( 'NONE',  ( 22.00000000000000355, 43.00000000000000000, -75.00000000000001421 ) ) ;
#20856=VERTEX_POINT ( 'NONE', #29165 ) ;
#20858=COLOUR_RGB ( '', 0.66274510, 0.83137255, 0.94901961) ;
#20868=FACE_OUTER_BOUND ( 'NONE', #43404, .T. ) ;
#20876=FACE_OUTER_BOUND ( 'NONE', #11671, .T. ) ;
#20877=PRESENTATION_STYLE_ASSIGNMENT (( #52212 ) ) ;
#20887=CIRCLE ( 'NONE', #55671, 0.9999999999999986677 ) ;
#20892=SURFACE_STYLE_FILL_AREA ( #25807 ) ;
#20899=COLOUR_RGB ( '', 0.08235294, 0.09019608, 0.10196078) ;
#20903=ADVANCED_FACE ( 'NONE', ( #51347 ), #18961, .T. ) ;
#20907=FACE_OUTER_BOUND ( 'NONE', #11485, .T. ) ;
#20913=AXIS2_PLACEMENT_3D ( 'NONE', #41902, #5245, #68954 ) ;
#20918=VERTEX_POINT ( 'NONE', #67170 ) ;
#20923=DIRECTION ( 'NONE',  ( 0.000000000000000000, -0.6691306063588592368, -0.7431448254773934670 ) ) ;
#20927=DIRECTION ( 'NONE',  ( 0.6402681315062923595, 0.000000000000000000, 0.7681514953298217430 ) ) ;
#20929=CARTESIAN_POINT ( 'NONE',  ( 10.00000000000002132, 43.00000000000000000, 90.00000000000000000 ) ) ;
#20940=PRESENTATION_STYLE_ASSIGNMENT (( #68794 ) ) ;
#20953=ORIENTED_EDGE ( 'NONE', *, *, #32512, .T. ) ;
#20960=FACE_OUTER_BOUND ( 'NONE', #51442, .T. ) ;
#20977=ADVANCED_FACE ( 'NONE', ( #26321 ), #31957, .T. ) ;
#20979=LINE ( 'NONE', #19920, #9041 ) ;
#20983=EDGE_CURVE ( 'NONE', #59410, #41519, #61768, .T. ) ;
#20984=LINE ( 'NONE', #16082, #38536 ) ;
#20989=CARTESIAN_POINT ( 'NONE',  ( 22.49408850561247775, 25.15120473151022296, -27.39855116598959128 ) ) ;
#20991=EDGE_LOOP ( 'NONE', ( #54591, #1771, #27409, #35582 ) ) ;
#20992=ORIENTED_EDGE ( 'NONE', *, *, #18282, .F. ) ;
#20996=FACE_BOUND ( 'NONE', #44565, .T. ) ;
#21000=COLOUR_RGB ( '', 0.72549020, 0.75294118, 0.79215686) ;
#21017=DIRECTION ( 'NONE',  ( -1.000000000000000000, -0.000000000000000000, -0.000000000000000000 ) ) ;
#21029=VERTEX_POINT ( 'NONE', #9832 ) ;
#21036=ORIENTED_EDGE ( 'NONE', *, *, #51331, .T. ) ;
#21041=ADVANCED_FACE ( 'NONE', ( #52742 ), #36237, .F. ) ;
#21058=SURFACE_STYLE_USAGE ( .BOTH. , #3442 ) ;
#21067=( LENGTH_UNIT ( ) NAMED_UNIT ( * ) SI_UNIT ( .MILLI., .METRE. ) );
#21068=( LENGTH_UNIT ( ) NAMED_UNIT ( * ) SI_UNIT ( .MILLI., .METRE. ) );
#21069=DIRECTION ( 'NONE',  ( 0.000000000000000000, 0.000000000000000000, -1.000000000000000000 ) ) ;
#21074=LINE ( 'NONE', #241, #65687 ) ;
#21093=( NAMED_UNIT ( * ) PLANE_ANGLE_UNIT ( ) SI_UNIT ( $, .RADIAN. ) );
#21096=DIRECTION ( 'NONE',  ( 0.000000000000000000, 0.000000000000000000, -1.000000000000000000 ) ) ;
#21105=SURFACE_SIDE_STYLE ('',( #4926 ) ) ;
#21107=PRESENTATION_STYLE_ASSIGNMENT (( #37341 ) ) ;
#21109=VERTEX_POINT ( 'NONE', #44562 ) ;
#21116=FILL_AREA_STYLE ('',( #43333 ) ) ;
#21119=CARTESIAN_POINT ( 'NONE',  ( 11.00000000000001776, 26.00000000000000355, -27.50000000000000355 ) ) ;
#21142=VECTOR ( 'NONE', #68748, 1000.000000000000000 ) ;
#21143=ORIENTED_EDGE ( 'NONE', *, *, #29790, .F. ) ;
#21144=LINE ( 'NONE', #52501, #26276 ) ;
#21153=EDGE_LOOP ( 'NONE', ( #60619, #4897, #842, #18678 ) ) ;
#21174=DIRECTION ( 'NONE',  ( -1.000000000000000000, 0.000000000000000000, 0.000000000000000000 ) ) ;
#21181=VERTEX_POINT ( 'NONE', #57855 ) ;
#21188=ADVANCED_FACE ( 'NONE', ( #68394 ), #25470, .T. ) ;
#21195=( NAMED_UNIT ( * ) SI_UNIT ( $, .STERADIAN. ) SOLID_ANGLE_UNIT ( ) );
#21196=COLOUR_RGB ( '', 0.09019608, 0.27058824, 0.51372549) ;
#21197=FACE_OUTER_BOUND ( 'NONE', #30847, .T. ) ;
#21205=DIRECTION ( 'NONE',  ( 1.000000000000000000, 0.000000000000000000, -1.300977106640434891E-16 ) ) ;
#21207=EDGE_LOOP ( 'NONE', ( #9713, #8389, #14864, #24559 ) ) ;
#21215=AXIS2_PLACEMENT_3D ( 'NONE', #41522, #62935, #42936 ) ;
#21217=CARTESIAN_POINT ( 'NONE',  ( 33.00000000000002132, 13.00000000000000178, 79.00402776293826435 ) ) ;
#21237=ORIENTED_EDGE ( 'NONE', *, *, #55188, .F. ) ;
#21240=FILL_AREA_STYLE_COLOUR ( '', #60074 ) ;
#21250=EDGE_LOOP ( 'NONE', ( #15499, #57146, #59399, #63516 ) ) ;
#21257=AXIS2_PLACEMENT_3D ( 'NONE', #68125, #30443, #51943 ) ;
#21264=EDGE_CURVE ( 'NONE', #39120, #33963, #41697, .T. ) ;
#21266=AXIS2_PLACEMENT_3D ( 'NONE', #11378, #64147, #31431 ) ;
#21271=( GEOMETRIC_REPRESENTATION_CONTEXT ( 3 ) GLOBAL_UNCERTAINTY_ASSIGNED_CONTEXT ( ( #53828 ) ) GLOBAL_UNIT_ASSIGNED_CONTEXT ( ( #15468, #69590, #54095 ) ) REPRESENTATION_CONTEXT ( 'NONE', 'WORKASPACE' ) );
#21275=DIRECTION ( 'NONE',  ( 0.000000000000000000, -1.000000000000000000, 0.000000000000000000 ) ) ;
#21289=FILL_AREA_STYLE_COLOUR ( '', #69379 ) ;
#21300=AXIS2_PLACEMENT_3D ( 'NONE', #25849, #15348, #47734 ) ;
#21304=CARTESIAN_POINT ( 'NONE',  ( -2.081668171172168513E-14, 43.00000000000000000, -28.00000000000000000 ) ) ;
#21309=VECTOR ( 'NONE', #51384, 1000.000000000000000 ) ;
#21310=CARTESIAN_POINT ( 'NONE',  ( 26.00000000000001776, -3.148064030671221758, 29.68999999999999417 ) ) ;
#21312=CARTESIAN_POINT ( 'NONE',  ( 16.00000000000001776, -3.148064030671221758, 29.68999999999999417 ) ) ;
#21316=ADVANCED_FACE ( 'NONE', ( #49368 ), #66357, .T. ) ;
#21318=AXIS2_PLACEMENT_3D ( 'NONE', #5901, #22796, #576 ) ;
#21319=SURFACE_STYLE_USAGE ( .BOTH. , #15398 ) ;
#21320=COLOUR_RGB ( '', 0.31764706, 0.68627451, 0.89019608) ;
#21321=CARTESIAN_POINT ( 'NONE',  ( 27.99999999999999645, 0.000000000000000000, -24.00402776293821816 ) ) ;
#21328=FILL_AREA_STYLE ('',( #69524 ) ) ;
#21345=DIRECTION ( 'NONE',  ( 0.000000000000000000, 0.000000000000000000, -1.000000000000000000 ) ) ;
#21346=CARTESIAN_POINT ( 'NONE',  ( 2.999999999999998668, 0.000000000000000000, -37.00402776293829277 ) ) ;
#21349=FACE_OUTER_BOUND ( 'NONE', #21843, .T. ) ;
#21366=MECHANICAL_DESIGN_GEOMETRIC_PRESENTATION_REPRESENTATION('',(#53905),#52835);
#21368=EDGE_CURVE ( 'NONE', #56593, #39359, #7344, .T. ) ;
#21384=MECHANICAL_DESIGN_GEOMETRIC_PRESENTATION_REPRESENTATION('',(#30356),#66324);
#21387=UNCERTAINTY_MEASURE_WITH_UNIT (LENGTH_MEASURE( 1.000000000000000082E-05 ), #45938, 'distance_accuracy_value', 'NONE');
#21395=SURFACE_STYLE_FILL_AREA ( #47147 ) ;
#21405=DIRECTION ( 'NONE',  ( 0.000000000000000000, 0.000000000000000000, -1.000000000000000000 ) ) ;
#21413=FILL_AREA_STYLE_COLOUR ( '', #3856 ) ;
#21415=( NAMED_UNIT ( * ) PLANE_ANGLE_UNIT ( ) SI_UNIT ( $, .RADIAN. ) );
#21421=SURFACE_SIDE_STYLE ('',( #58722 ) ) ;
#21431=VECTOR ( 'NONE', #38846, 1000.000000000000000 ) ;
#21447=AXIS2_PLACEMENT_3D ( 'NONE', #24925, #41483, #3793 ) ;
#21451=SURFACE_STYLE_FILL_AREA ( #10222 ) ;
#21452=ORIENTED_EDGE ( 'NONE', *, *, #63261, .F. ) ;
#21459=ORIENTED_EDGE ( 'NONE', *, *, #3368, .T. ) ;
#21461=DIRECTION ( 'NONE',  ( 0.000000000000000000, -1.000000000000000000, 0.000000000000000000 ) ) ;
#21464=EDGE_CURVE ( 'NONE', #46026, #47623, #57407, .T. ) ;
#21470=COLOUR_RGB ( '', 0.08235294, 0.09019608, 0.10196078) ;
#21471=CARTESIAN_POINT ( 'NONE',  ( 22.99999999999998934, 5.000000000000000000, 37.00402776293825724 ) ) ;
#21472=EDGE_CURVE ( 'NONE', #51817, #1374, #23679, .T. ) ;
#21475=MECHANICAL_DESIGN_GEOMETRIC_PRESENTATION_REPRESENTATION('',(#15879),#50710);
#21481=CARTESIAN_POINT ( 'NONE',  ( 3.000000000000002665, 42.00000000000000000, -89.00000000000000000 ) ) ;
#21483=STYLED_ITEM ( 'NONE', ( #57214 ), #53990 ) ;
#21487=CARTESIAN_POINT ( 'NONE',  ( 16.00000000000001776, -3.148064030671221758, 34.68999999999999062 ) ) ;
#21488=COLOUR_RGB ( '', 0.31764706, 0.68627451, 0.89019608) ;
#21490=PRESENTATION_STYLE_ASSIGNMENT (( #26742 ) ) ;
#21500=EDGE_LOOP ( 'NONE', ( #15399, #448, #63056, #44263 ) ) ;
#21502=ORIENTED_EDGE ( 'NONE', *, *, #49110, .T. ) ;
#21505=ORIENTED_EDGE ( 'NONE', *, *, #42180, .F. ) ;
#21523=EDGE_CURVE ( 'NONE', #9623, #26861, #63048, .T. ) ;
#21527=LINE ( 'NONE', #53211, #2422 ) ;
#21535=ORIENTED_EDGE ( 'NONE', *, *, #52845, .F. ) ;
#21537=UNCERTAINTY_MEASURE_WITH_UNIT (LENGTH_MEASURE( 1.000000000000000082E-05 ), #31389, 'distance_accuracy_value', 'NONE');
#21545=DIRECTION ( 'NONE',  ( 1.000000000000000000, 0.000000000000000000, -1.300977106640434891E-16 ) ) ;
#21546=FILL_AREA_STYLE ('',( #36737 ) ) ;
#21548=ORIENTED_EDGE ( 'NONE', *, *, #4270, .T. ) ;
#21554=( GEOMETRIC_REPRESENTATION_CONTEXT ( 3 ) GLOBAL_UNCERTAINTY_ASSIGNED_CONTEXT ( ( #43468 ) ) GLOBAL_UNIT_ASSIGNED_CONTEXT ( ( #10217, #59404, #61477 ) ) REPRESENTATION_CONTEXT ( 'NONE', 'WORKASPACE' ) );
#21557=DIRECTION ( 'NONE',  ( -0.000000000000000000, -1.000000000000000000, -0.000000000000000000 ) ) ;
#21569=MECHANICAL_DESIGN_GEOMETRIC_PRESENTATION_REPRESENTATION('',(#41789),#56347);
#21572=AXIS2_PLACEMENT_3D ( 'NONE', #47801, #48122, #10795 ) ;
#21588=FILL_AREA_STYLE_COLOUR ( '', #61677 ) ;
#21599=UNCERTAINTY_MEASURE_WITH_UNIT (LENGTH_MEASURE( 1.000000000000000082E-05 ), #8570, 'distance_accuracy_value', 'NONE');
#21602=SURFACE_STYLE_FILL_AREA ( #16021 ) ;
#21609=ORIENTED_EDGE ( 'NONE', *, *, #19689, .F. ) ;
#21617=DIRECTION ( 'NONE',  ( -1.000000000000000000, 0.000000000000000000, 1.300977106640434891E-16 ) ) ;
#21634=FILL_AREA_STYLE ('',( #55379 ) ) ;
#21635=( NAMED_UNIT ( * ) PLANE_ANGLE_UNIT ( ) SI_UNIT ( $, .RADIAN. ) );
#21636=CARTESIAN_POINT ( 'NONE',  ( 11.00000000000001599, 43.00000000000000000, -28.38386403503541899 ) ) ;
#21647=DIRECTION ( 'NONE',  ( 0.000000000000000000, 0.000000000000000000, -1.000000000000000000 ) ) ;
#21660=SURFACE_STYLE_USAGE ( .BOTH. , #47407 ) ;
#21669=DIRECTION ( 'NONE',  ( 0.000000000000000000, 0.000000000000000000, -1.000000000000000000 ) ) ;
#21671=( LENGTH_UNIT ( ) NAMED_UNIT ( * ) SI_UNIT ( .MILLI., .METRE. ) );
#21680=STYLED_ITEM ( 'NONE', ( #60358 ), #7177 ) ;
#21687=SURFACE_SIDE_STYLE ('',( #48463 ) ) ;
#21689=MECHANICAL_DESIGN_GEOMETRIC_PRESENTATION_REPRESENTATION('',(#28378),#25055);
#21709=( NAMED_UNIT ( * ) SI_UNIT ( $, .STERADIAN. ) SOLID_ANGLE_UNIT ( ) );
#21716=EDGE_LOOP ( 'NONE', ( #33982, #21884, #3315, #48004 ) ) ;
#21721=ORIENTED_EDGE ( 'NONE', *, *, #59099, .F. ) ;
#21737=CARTESIAN_POINT ( 'NONE',  ( 0.4142135623730951455, 42.99999999999999289, -35.49999999999999289 ) ) ;
#21740=AXIS2_PLACEMENT_3D ( 'NONE', #27801, #53538, #49307 ) ;
#21749=FACE_OUTER_BOUND ( 'NONE', #609, .T. ) ;
#21750=STYLED_ITEM ( 'NONE', ( #5458 ), #8923 ) ;
#21753=MECHANICAL_DESIGN_GEOMETRIC_PRESENTATION_REPRESENTATION('',(#26369),#1616);
#21760=AXIS2_PLACEMENT_3D ( 'NONE', #14318, #19591, #35077 ) ;
#21762=MECHANICAL_DESIGN_GEOMETRIC_PRESENTATION_REPRESENTATION('',(#34109),#63343);
#21763=CARTESIAN_POINT ( 'NONE',  ( 5.429140806177446840E-16, 13.58578643762690419, -35.91421356237308515 ) ) ;
#21777=EDGE_LOOP ( 'NONE', ( #36801, #67462, #6034, #52017 ) ) ;
#21778=CYLINDRICAL_SURFACE ( 'NONE', #54898, 0.9999999999999974465 ) ;
#21786=ORIENTED_EDGE ( 'NONE', *, *, #36008, .F. ) ;
#21803=PRESENTATION_STYLE_ASSIGNMENT (( #54816 ) ) ;
#21804=COLOUR_RGB ( '', 0.40784314, 0.44705882, 0.49803922) ;
#21806=DIRECTION ( 'NONE',  ( -1.000000000000000000, -0.000000000000000000, 0.000000000000000000 ) ) ;
#21807=SURFACE_STYLE_USAGE ( .BOTH. , #20776 ) ;
#21808=AXIS2_PLACEMENT_3D ( 'NONE', #7287, #44949, #40023 ) ;
#21813=ORIENTED_EDGE ( 'NONE', *, *, #46346, .F. ) ;
#21820=FACE_OUTER_BOUND ( 'NONE', #42837, .T. ) ;
#21837=LINE ( 'NONE', #64393, #17397 ) ;
#21843=EDGE_LOOP ( 'NONE', ( #48377, #30918, #22805, #25032 ) ) ;
#21869=DIRECTION ( 'NONE',  ( 0.000000000000000000, -0.000000000000000000, -1.000000000000000000 ) ) ;
#21870=ORIENTED_EDGE ( 'NONE', *, *, #30307, .T. ) ;
#21872=( GEOMETRIC_REPRESENTATION_CONTEXT ( 3 ) GLOBAL_UNCERTAINTY_ASSIGNED_CONTEXT ( ( #48779 ) ) GLOBAL_UNIT_ASSIGNED_CONTEXT ( ( #26672, #16527, #11209 ) ) REPRESENTATION_CONTEXT ( 'NONE', 'WORKASPACE' ) );
#21884=ORIENTED_EDGE ( 'NONE', *, *, #9795, .F. ) ;
#21886=TOROIDAL_SURFACE ( 'NONE', #57837, 111.0000000000000142, 1.000000000000000000 ) ;
#21897=DIRECTION ( 'NONE',  ( 0.000000000000000000, 1.000000000000000000, 0.000000000000000000 ) ) ;
#21898=MECHANICAL_DESIGN_GEOMETRIC_PRESENTATION_REPRESENTATION('',(#27488),#28644);
#21905=ORIENTED_EDGE ( 'NONE', *, *, #13091, .T. ) ;
#21912=EDGE_CURVE ( 'NONE', #36332, #27365, #9139, .T. ) ;
#21914=LINE ( 'NONE', #54246, #65085 ) ;
#21918=( LENGTH_UNIT ( ) NAMED_UNIT ( * ) SI_UNIT ( .MILLI., .METRE. ) );
#21919=DIRECTION ( 'NONE',  ( 0.000000000000000000, 0.000000000000000000, -1.000000000000000000 ) ) ;
#21938=ORIENTED_EDGE ( 'NONE', *, *, #17680, .F. ) ;
#21941=MECHANICAL_DESIGN_GEOMETRIC_PRESENTATION_REPRESENTATION('',(#39946),#29763);
#21944=EDGE_CURVE ( 'NONE', #9217, #27703, #54048, .T. ) ;
#21950=VERTEX_POINT ( 'NONE', #31251 ) ;
#21959=AXIS2_PLACEMENT_3D ( 'NONE', #51471, #51835, #47648 ) ;
#21961=DIRECTION ( 'NONE',  ( 1.000000000000000000, 0.000000000000000000, -1.300977106640434891E-16 ) ) ;
#21963=CARTESIAN_POINT ( 'NONE',  ( 21.00000000000001776, -3.148064030671221758, -29.68999999999999417 ) ) ;
#21968=PRESENTATION_STYLE_ASSIGNMENT (( #17053 ) ) ;
#21972=SURFACE_STYLE_USAGE ( .BOTH. , #75 ) ;
#21980=SURFACE_STYLE_USAGE ( .BOTH. , #38183 ) ;
#21983=VECTOR ( 'NONE', #21869, 1000.000000000000000 ) ;
#21984=LINE ( 'NONE', #59228, #4429 ) ;
#21987=FACE_OUTER_BOUND ( 'NONE', #22506, .T. ) ;
#21988=CARTESIAN_POINT ( 'NONE',  ( 31.91038605531459993, 42.48853604202995626, -45.29557250688775838 ) ) ;
#21990=DIRECTION ( 'NONE',  ( 0.000000000000000000, 1.000000000000000000, 0.000000000000000000 ) ) ;
#21999=DIRECTION ( 'NONE',  ( -0.000000000000000000, -1.000000000000000000, -0.000000000000000000 ) ) ;
#22003=ADVANCED_FACE ( 'NONE', ( #58033 ), #63294, .F. ) ;
#22010=UNCERTAINTY_MEASURE_WITH_UNIT (LENGTH_MEASURE( 1.000000000000000082E-05 ), #38946, 'distance_accuracy_value', 'NONE');
#22015=ADVANCED_FACE ( 'NONE', ( #41515 ), #15478, .T. ) ;
#22034=DIRECTION ( 'NONE',  ( 0.000000000000000000, -0.9396926207859082059, 0.3420201433256693790 ) ) ;
#22055=COLOUR_RGB ( '', 0.66274510, 0.83137255, 0.94901961) ;
#22062=( LENGTH_UNIT ( ) NAMED_UNIT ( * ) SI_UNIT ( .MILLI., .METRE. ) );
#22085=CARTESIAN_POINT ( 'NONE',  ( 1.092332116235429474E-16, 42.58578643762690774, -35.91421356237308515 ) ) ;
#22086=CARTESIAN_POINT ( 'NONE',  ( 24.68182447752072406, 26.35395679099813293, 27.48625690893775797 ) ) ;
#22095=( NAMED_UNIT ( * ) SI_UNIT ( $, .STERADIAN. ) SOLID_ANGLE_UNIT ( ) );
#22103=VECTOR ( 'NONE', #5336, 1000.000000000000000 ) ;
#22110=FILL_AREA_STYLE ('',( #43946 ) ) ;
#22114=ORIENTED_EDGE ( 'NONE', *, *, #47785, .T. ) ;
#22122=DIRECTION ( 'NONE',  ( 0.000000000000000000, 0.000000000000000000, -1.000000000000000000 ) ) ;
#22124=LINE ( 'NONE', #28764, #62446 ) ;
#22132=ORIENTED_EDGE ( 'NONE', *, *, #51736, .T. ) ;
#22147=VERTEX_POINT ( 'NONE', #19230 ) ;
#22159=( LENGTH_UNIT ( ) NAMED_UNIT ( * ) SI_UNIT ( .MILLI., .METRE. ) );
#22170=DIRECTION ( 'NONE',  ( 0.000000000000000000, 0.000000000000000000, -1.000000000000000000 ) ) ;
#22198=MECHANICAL_DESIGN_GEOMETRIC_PRESENTATION_REPRESENTATION('',(#10945),#43589);
#22223=COLOUR_RGB ( '', 0.72549020, 0.75294118, 0.79215686) ;
#22227=ORIENTED_EDGE ( 'NONE', *, *, #66552, .T. ) ;
#22233=LINE ( 'NONE', #22940, #19496 ) ;
#22238=CARTESIAN_POINT ( 'NONE',  ( 57.00000000000000000, 0.9999999999999991118, 60.00402776293827145 ) ) ;
#22252=PRESENTATION_STYLE_ASSIGNMENT (( #718 ) ) ;
#22258=AXIS2_PLACEMENT_3D ( 'NONE', #46358, #46723, #45992 ) ;
#22260=CARTESIAN_POINT ( 'NONE',  ( 29.00000000000002842, 42.00000000000000000, 89.00000000000000000 ) ) ;
#22264=MECHANICAL_DESIGN_GEOMETRIC_PRESENTATION_REPRESENTATION('',(#31230),#16671);
#22266=CARTESIAN_POINT ( 'NONE',  ( 57.00000000000000000, 0.000000000000000000, 55.00402776293825724 ) ) ;
#22267=ORIENTED_EDGE ( 'NONE', *, *, #25332, .T. ) ;
#22271=CARTESIAN_POINT ( 'NONE',  ( 16.00000000000001776, -3.148064030671221758, 29.68999999999999417 ) ) ;
#22297=AXIS2_PLACEMENT_3D ( 'NONE', #13876, #35342, #13514 ) ;
#22298=( LENGTH_UNIT ( ) NAMED_UNIT ( * ) SI_UNIT ( .MILLI., .METRE. ) );
#22303=COLOUR_RGB ( '', 0.09019608, 0.27058824, 0.51372549) ;
#22304=ADVANCED_FACE ( 'NONE', ( #68493 ), #41430, .F. ) ;
#22308=SPHERICAL_SURFACE ( 'NONE', #23579, 1.000000000000000000 ) ;
#22312=EDGE_CURVE ( 'NONE', #22382, #63620, #17343, .T. ) ;
#22314=LINE ( 'NONE', #31820, #23536 ) ;
#22329=CARTESIAN_POINT ( 'NONE',  ( 23.00000000000000000, 0.000000000000000000, -24.00402776293825013 ) ) ;
#22331=( NAMED_UNIT ( * ) PLANE_ANGLE_UNIT ( ) SI_UNIT ( $, .RADIAN. ) );
#22333=SURFACE_SIDE_STYLE ('',( #5429 ) ) ;
#22337=CARTESIAN_POINT ( 'NONE',  ( 32.00000000000000000, 15.00000000000000000, -80.00402776293826435 ) ) ;
#22346=CARTESIAN_POINT ( 'NONE',  ( 24.70577775730027881, 26.00000000000004619, -27.50000000000000711 ) ) ;
#22351=MECHANICAL_DESIGN_GEOMETRIC_PRESENTATION_REPRESENTATION('',(#52689),#47087);
#22358=VECTOR ( 'NONE', #7875, 1000.000000000000000 ) ;
#22364=CARTESIAN_POINT ( 'NONE',  ( 27.00000000000001776, 42.00000000000000000, -34.49999999999999289 ) ) ;
#22365=ORIENTED_EDGE ( 'NONE', *, *, #61369, .T. ) ;
#22382=VERTEX_POINT ( 'NONE', #53679 ) ;
#22383=CIRCLE ( 'NONE', #48288, 5.000000000000004441 ) ;
#22388=ORIENTED_EDGE ( 'NONE', *, *, #29743, .F. ) ;
#22391=TOROIDAL_SURFACE ( 'NONE', #56084, 18.99999999999998934, 1.000000000000000000 ) ;
#22402=PLANE ( 'NONE',  #24012 ) ;
#22405=VERTEX_POINT ( 'NONE', #50499 ) ;
#22407=CARTESIAN_POINT ( 'NONE',  ( 3.000000000000002665, 42.00000000000000000, -80.00402776293826435 ) ) ;
#22410=DIRECTION ( 'NONE',  ( 0.000000000000000000, 0.000000000000000000, 1.000000000000000000 ) ) ;
#22411=VERTEX_POINT ( 'NONE', #7243 ) ;
#22417=STYLED_ITEM ( 'NONE', ( #14264 ), #1191 ) ;
#22426=SURFACE_STYLE_FILL_AREA ( #6570 ) ;
#22438=DIRECTION ( 'NONE',  ( 0.000000000000000000, 0.000000000000000000, -1.000000000000000000 ) ) ;
#22449=ORIENTED_EDGE ( 'NONE', *, *, #57573, .T. ) ;
#22452=VECTOR ( 'NONE', #68218, 1000.000000000000000 ) ;
#22461=DIRECTION ( 'NONE',  ( -0.000000000000000000, -1.000000000000000000, 0.000000000000000000 ) ) ;
#22463=FILL_AREA_STYLE ('',( #16866 ) ) ;
#22467=STYLED_ITEM ( 'NONE', ( #64540 ), #1385 ) ;
#22480=PRESENTATION_STYLE_ASSIGNMENT (( #27384 ) ) ;
#22484=AXIS2_PLACEMENT_3D ( 'NONE', #20363, #63959, #53431 ) ;
#22494=AXIS2_PLACEMENT_3D ( 'NONE', #68317, #31011, #46197 ) ;
#22498=DIRECTION ( 'NONE',  ( 0.000000000000000000, -1.000000000000000000, 0.000000000000000000 ) ) ;
#22506=EDGE_LOOP ( 'NONE', ( #9368, #22449, #26622, #26014, #9921, #7173 ) ) ;
#22514=( GEOMETRIC_REPRESENTATION_CONTEXT ( 3 ) GLOBAL_UNCERTAINTY_ASSIGNED_CONTEXT ( ( #20013 ) ) GLOBAL_UNIT_ASSIGNED_CONTEXT ( ( #7308, #6256, #22095 ) ) REPRESENTATION_CONTEXT ( 'NONE', 'WORKASPACE' ) );
#22519=PRESENTATION_STYLE_ASSIGNMENT (( #53494 ) ) ;
#22537=EDGE_LOOP ( 'NONE', ( #15101, #21870, #14684 ) ) ;
#22553=EDGE_CURVE ( 'NONE', #582, #46401, #26088, .T. ) ;
#22555=FILL_AREA_STYLE_COLOUR ( '', #53428 ) ;
#22568=DIRECTION ( 'NONE',  ( 0.000000000000000000, 0.000000000000000000, -1.000000000000000000 ) ) ;
#22573=EDGE_CURVE ( 'NONE', #26861, #53011, #44262, .T. ) ;
#22583=AXIS2_PLACEMENT_3D ( 'NONE', #55681, #2132, #19428 ) ;
#22586=LINE ( 'NONE', #7453, #53220 ) ;
#22591=COLOUR_RGB ( '', 0.72549020, 0.75294118, 0.79215686) ;
#22592=DIRECTION ( 'NONE',  ( 0.000000000000000000, 0.000000000000000000, -1.000000000000000000 ) ) ;
#22594=VERTEX_POINT ( 'NONE', #42339 ) ;
#22595=FACE_OUTER_BOUND ( 'NONE', #22656, .T. ) ;
#22600=SURFACE_SIDE_STYLE ('',( #60548 ) ) ;
#22620=ORIENTED_EDGE ( 'NONE', *, *, #34620, .T. ) ;
#22627=LINE ( 'NONE', #65176, #42830 ) ;
#22628=SURFACE_SIDE_STYLE ('',( #12394 ) ) ;
#22630=SURFACE_STYLE_FILL_AREA ( #1091 ) ;
#22643=VERTEX_POINT ( 'NONE', #28498 ) ;
#22656=EDGE_LOOP ( 'NONE', ( #42300, #30368, #59577, #2884 ) ) ;
#22670=PRESENTATION_STYLE_ASSIGNMENT (( #31203 ) ) ;
#22683=( NAMED_UNIT ( * ) SI_UNIT ( $, .STERADIAN. ) SOLID_ANGLE_UNIT ( ) );
#22690=DIRECTION ( 'NONE',  ( -0.000000000000000000, -1.000000000000000000, -0.000000000000000000 ) ) ;
#22695=EDGE_CURVE ( 'NONE', #62632, #61113, #55243, .T. ) ;
#22698=UNCERTAINTY_MEASURE_WITH_UNIT (LENGTH_MEASURE( 1.000000000000000082E-05 ), #16278, 'distance_accuracy_value', 'NONE');
#22710=DIRECTION ( 'NONE',  ( 1.000000000000000000, 0.000000000000000000, -1.300977106640442040E-16 ) ) ;
#22712=FACE_OUTER_BOUND ( 'NONE', #7395, .T. ) ;
#22715=AXIS2_PLACEMENT_3D ( 'NONE', #65485, #5006, #43726 ) ;
#22720=ORIENTED_EDGE ( 'NONE', *, *, #15928, .F. ) ;
#22721=DIRECTION ( 'NONE',  ( 1.000000000000000000, 0.000000000000000000, -0.000000000000000000 ) ) ;
#22725=ADVANCED_FACE ( 'NONE', ( #43707 ), #44060, .F. ) ;
#22729=SURFACE_STYLE_FILL_AREA ( #1197 ) ;
#22734=CARTESIAN_POINT ( 'NONE',  ( 57.00000000000000000, 16.00000000000000000, -60.00402776293825724 ) ) ;
#22737=AXIS2_PLACEMENT_3D ( 'NONE', #54651, #49390, #12078 ) ;
#22741=COLOUR_RGB ( '', 0.09019608, 0.27058824, 0.51372549) ;
#22745=ADVANCED_FACE ( 'NONE', ( #8114 ), #14089, .F. ) ;
#22748=FILL_AREA_STYLE ('',( #27641 ) ) ;
#22753=ORIENTED_EDGE ( 'NONE', *, *, #2368, .T. ) ;
#22754=CARTESIAN_POINT ( 'NONE',  ( 1.000000000000000000, 0.9999999999999991118, 80.00402776293826435 ) ) ;
#22759=CARTESIAN_POINT ( 'NONE',  ( 10.00000000000000711, 50.00000000000000000, -60.00000000000000000 ) ) ;
#22764=STYLED_ITEM ( 'NONE', ( #6730 ), #24852 ) ;
#22767=DIRECTION ( 'NONE',  ( 0.000000000000000000, 1.000000000000000000, -0.000000000000000000 ) ) ;
#22791=UNCERTAINTY_MEASURE_WITH_UNIT (LENGTH_MEASURE( 1.000000000000000082E-05 ), #6639, 'distance_accuracy_value', 'NONE');
#22796=DIRECTION ( 'NONE',  ( -0.000000000000000000, -0.000000000000000000, -1.000000000000000000 ) ) ;
#22800=ADVANCED_FACE ( 'NONE', ( #2789 ), #3471, .F. ) ;
#22803=SURFACE_STYLE_FILL_AREA ( #2675 ) ;
#22805=ORIENTED_EDGE ( 'NONE', *, *, #1447, .F. ) ;
#22812=CARTESIAN_POINT ( 'NONE',  ( 6.000000000000017764, 14.00000000000000533, -35.50000000000000000 ) ) ;
#22826=CARTESIAN_POINT ( 'NONE',  ( 57.00000000000000000, 0.000000000000000000, 60.00402776293827145 ) ) ;
#22829=PRESENTATION_STYLE_ASSIGNMENT (( #34059 ) ) ;
#22831=EDGE_LOOP ( 'NONE', ( #47429, #777 ) ) ;
#22834=FILL_AREA_STYLE_COLOUR ( '', #63578 ) ;
#22852=MECHANICAL_DESIGN_GEOMETRIC_PRESENTATION_REPRESENTATION('',(#56516),#41967);
#22859=FILL_AREA_STYLE ('',( #65757 ) ) ;
#22861=ORIENTED_EDGE ( 'NONE', *, *, #15928, .T. ) ;
#22877=DIRECTION ( 'NONE',  ( -1.000000000000000000, 3.011817513800517074E-33, 1.300977106640435384E-16 ) ) ;
#22880=COLOUR_RGB ( '', 0.72549020, 0.75294118, 0.79215686) ;
#22897=VERTEX_POINT ( 'NONE', #26001 ) ;
#22905=DIRECTION ( 'NONE',  ( 0.000000000000000000, -0.000000000000000000, -1.000000000000000000 ) ) ;
#22907=ADVANCED_FACE ( 'NONE', ( #20752 ), #37314, .T. ) ;
#22911=VECTOR ( 'NONE', #48183, 1000.000000000000000 ) ;
#22917=DIRECTION ( 'NONE',  ( 0.000000000000000000, -0.000000000000000000, -1.000000000000000000 ) ) ;
#22938=CARTESIAN_POINT ( 'NONE',  ( 22.00000000000002132, 50.00000000000000000, 60.00000000000000000 ) ) ;
#22940=CARTESIAN_POINT ( 'NONE',  ( 1.000000000000000000, 43.00000000000000000, -35.50000000000000000 ) ) ;
#22950=DIRECTION ( 'NONE',  ( -0.000000000000000000, -1.000000000000000000, -0.000000000000000000 ) ) ;
#22951=AXIS2_PLACEMENT_3D ( 'NONE', #30631, #10591, #63698 ) ;
#22960=VECTOR ( 'NONE', #31360, 1000.000000000000000 ) ;
#22975=EDGE_CURVE ( 'NONE', #44696, #48050, #65381, .T. ) ;
#22981=CARTESIAN_POINT ( 'NONE',  ( 0.7152604538204458962, 42.96841842781390852, 74.40727953928171701 ) ) ;
#22984=EDGE_CURVE ( 'NONE', #35304, #34116, #50900, .T. ) ;
#22991=PRESENTATION_STYLE_ASSIGNMENT (( #17387 ) ) ;
#23002=DIRECTION ( 'NONE',  ( -1.000000000000000000, 0.000000000000000000, -4.625929269271505635E-16 ) ) ;
#23005=( NAMED_UNIT ( * ) SI_UNIT ( $, .STERADIAN. ) SOLID_ANGLE_UNIT ( ) );
#23008=FILL_AREA_STYLE_COLOUR ( '', #25037 ) ;
#23015=PRESENTATION_STYLE_ASSIGNMENT (( #26855 ) ) ;
#23017=CARTESIAN_POINT ( 'NONE',  ( 22.99999999999995381, 5.000000000000000000, 32.00402776293825724 ) ) ;
#23022=ORIENTED_EDGE ( 'NONE', *, *, #8212, .T. ) ;
#23026=CIRCLE ( 'NONE', #62325, 1.000000000000000888 ) ;
#23036=SURFACE_STYLE_USAGE ( .BOTH. , #44865 ) ;
#23037=FILL_AREA_STYLE_COLOUR ( '', #20899 ) ;
#23043=MECHANICAL_DESIGN_GEOMETRIC_PRESENTATION_REPRESENTATION('',(#47952),#1629);
#23057=ADVANCED_FACE ( 'NONE', ( #30489 ), #40392, .T. ) ;
#23067=CARTESIAN_POINT ( 'NONE',  ( 7.999999999999992895, 5.000000000000000000, 24.00402776293826079 ) ) ;
#23070=SURFACE_STYLE_FILL_AREA ( #65623 ) ;
#23074=( LENGTH_UNIT ( ) NAMED_UNIT ( * ) SI_UNIT ( .MILLI., .METRE. ) );
#23075=MECHANICAL_DESIGN_GEOMETRIC_PRESENTATION_REPRESENTATION('',(#60119),#65743);
#23088=CARTESIAN_POINT ( 'NONE',  ( 6.000000000000017764, -60.04052944165106709, -35.50000000000000000 ) ) ;
#23098=DIRECTION ( 'NONE',  ( 0.000000000000000000, 0.000000000000000000, -1.000000000000000000 ) ) ;
#23100=SURFACE_SIDE_STYLE ('',( #12512 ) ) ;
#23107=SURFACE_SIDE_STYLE ('',( #11142 ) ) ;
#23115=ORIENTED_EDGE ( 'NONE', *, *, #54007, .T. ) ;
#23120=VECTOR ( 'NONE', #41587, 1000.000000000000000 ) ;
#23128=AXIS2_PLACEMENT_3D ( 'NONE', #32565, #60682, #1892 ) ;
#23163=DIRECTION ( 'NONE',  ( 0.000000000000000000, -1.000000000000000000, 0.000000000000000000 ) ) ;
#23178=VERTEX_POINT ( 'NONE', #66767 ) ;
#23181=SURFACE_STYLE_FILL_AREA ( #27383 ) ;
#23183=AXIS2_PLACEMENT_3D ( 'NONE', #36953, #58718, #10875 ) ;
#23198=VERTEX_POINT ( 'NONE', #68860 ) ;
#23205=SURFACE_STYLE_FILL_AREA ( #11948 ) ;
#23206=EDGE_CURVE ( 'NONE', #10939, #56481, #42968, .T. ) ;
#23207=DIRECTION ( 'NONE',  ( 0.000000000000000000, -0.3420201433256629953, -0.9396926207859104263 ) ) ;
#23209=DIRECTION ( 'NONE',  ( 0.000000000000000000, 0.000000000000000000, -1.000000000000000000 ) ) ;
#23211=ORIENTED_EDGE ( 'NONE', *, *, #22984, .T. ) ;
#23217=EDGE_CURVE ( 'NONE', #56838, #41529, #26601, .T. ) ;
#23225=LINE ( 'NONE', #39777, #20463 ) ;
#23226=SURFACE_STYLE_USAGE ( .BOTH. , #33761 ) ;
#23236=ADVANCED_FACE ( 'NONE', ( #47438 ), #42853, .F. ) ;
#23265=EDGE_LOOP ( 'NONE', ( #67903, #66011, #57089, #1006 ) ) ;
#23266=AXIS2_PLACEMENT_3D ( 'NONE', #61724, #25161, #13203 ) ;
#23268=SURFACE_SIDE_STYLE ('',( #61243 ) ) ;
#23273=SURFACE_STYLE_USAGE ( .BOTH. , #51052 ) ;
#23290=CARTESIAN_POINT ( 'NONE',  ( 22.99999999999996447, 0.000000000000000000, 29.00402776293825369 ) ) ;
#23293=EDGE_CURVE ( 'NONE', #52976, #1567, #62131, .T. ) ;
#23312=CARTESIAN_POINT ( 'NONE',  ( 0.08961491207241870094, 42.48853761352472702, 74.70442652852922549 ) ) ;
#23313=CARTESIAN_POINT ( 'NONE',  ( 27.00000000000001776, 43.00000000000000000, 36.50000000000000000 ) ) ;
#23356=EDGE_CURVE ( 'NONE', #26455, #3143, #17483, .T. ) ;
#23357=DIRECTION ( 'NONE',  ( -0.000000000000000000, -1.000000000000000000, -0.000000000000000000 ) ) ;
#23365=DIRECTION ( 'NONE',  ( 1.000000000000000000, -0.000000000000000000, -1.300977106640434891E-16 ) ) ;
#23380=( NAMED_UNIT ( * ) PLANE_ANGLE_UNIT ( ) SI_UNIT ( $, .RADIAN. ) );
#23382=AXIS2_PLACEMENT_3D ( 'NONE', #10951, #4627, #25732 ) ;
#23383=CARTESIAN_POINT ( 'NONE',  ( 10.00000000000001954, 43.00000000000000000, 45.61250543006183733 ) ) ;
#23404=DIRECTION ( 'NONE',  ( -1.239088197126290817E-16, 0.000000000000000000, -1.000000000000000000 ) ) ;
#23419=CARTESIAN_POINT ( 'NONE',  ( 3.000000000000002665, 43.00000000000000000, -90.00000000000000000 ) ) ;
#23421=VERTEX_POINT ( 'NONE', #49823 ) ;
#23426=STYLED_ITEM ( 'NONE', ( #48549 ), #10344 ) ;
#23434=EDGE_CURVE ( 'NONE', #69376, #582, #36277, .T. ) ;
#23458=DIRECTION ( 'NONE',  ( -1.000000000000000000, 0.000000000000000000, 0.000000000000000000 ) ) ;
#23460=UNCERTAINTY_MEASURE_WITH_UNIT (LENGTH_MEASURE( 1.000000000000000082E-05 ), #45731, 'distance_accuracy_value', 'NONE');
#23466=AXIS2_PLACEMENT_3D ( 'NONE', #28258, #17760, #34270 ) ;
#23469=DIRECTION ( 'NONE',  ( -1.000000000000000000, 0.000000000000000000, 0.000000000000000000 ) ) ;
#23473=FACE_OUTER_BOUND ( 'NONE', #62378, .T. ) ;
#23486=VERTEX_POINT ( 'NONE', #12863 ) ;
#23488=COLOUR_RGB ( '', 0.72549020, 0.75294118, 0.79215686) ;
#23489=ORIENTED_EDGE ( 'NONE', *, *, #44446, .F. ) ;
#23494=CARTESIAN_POINT ( 'NONE',  ( 24.50753990722797226, 26.84611427229081215, -27.39925439962615883 ) ) ;
#23519=ORIENTED_EDGE ( 'NONE', *, *, #13511, .F. ) ;
#23526=CARTESIAN_POINT ( 'NONE',  ( 57.00000000000000000, 16.00000000000000000, 60.00402776293825724 ) ) ;
#23531=CIRCLE ( 'NONE', #62837, 5.000000000000004441 ) ;
#23532=MECHANICAL_DESIGN_GEOMETRIC_PRESENTATION_REPRESENTATION('',(#58338),#68489);
#23536=VECTOR ( 'NONE', #53308, 1000.000000000000000 ) ;
#23540=COLOUR_RGB ( '', 0.66274510, 0.83137255, 0.94901961) ;
#23545=STYLED_ITEM ( 'NONE', ( #36314 ), #15209 ) ;
#23552=ORIENTED_EDGE ( 'NONE', *, *, #19129, .T. ) ;
#23556=( LENGTH_UNIT ( ) NAMED_UNIT ( * ) SI_UNIT ( .MILLI., .METRE. ) );
#23557=MECHANICAL_DESIGN_GEOMETRIC_PRESENTATION_REPRESENTATION('',(#53888),#30315);
#23558=SURFACE_STYLE_USAGE ( .BOTH. , #2033 ) ;
#23564=STYLED_ITEM ( 'NONE', ( #21107 ), #59214 ) ;
#23567=( GEOMETRIC_REPRESENTATION_CONTEXT ( 3 ) GLOBAL_UNCERTAINTY_ASSIGNED_CONTEXT ( ( #49442 ) ) GLOBAL_UNIT_ASSIGNED_CONTEXT ( ( #20447, #41950, #3165 ) ) REPRESENTATION_CONTEXT ( 'NONE', 'WORKASPACE' ) );
#23569=CARTESIAN_POINT ( 'NONE',  ( 98.00000000000000000, 16.00000000000000000, -12.50000000000000178 ) ) ;
#23573=ORIENTED_EDGE ( 'NONE', *, *, #1201, .F. ) ;
#23577=DIRECTION ( 'NONE',  ( 0.000000000000000000, 1.000000000000000000, 0.000000000000000000 ) ) ;
#23579=AXIS2_PLACEMENT_3D ( 'NONE', #37855, #28238, #53626 ) ;
#23584=SURFACE_STYLE_USAGE ( .BOTH. , #34147 ) ;
#23595=UNCERTAINTY_MEASURE_WITH_UNIT (LENGTH_MEASURE( 1.000000000000000082E-05 ), #58794, 'distance_accuracy_value', 'NONE');
#23597=CARTESIAN_POINT ( 'NONE',  ( 57.00000000000000000, 0.000000000000000000, -55.00402776293825724 ) ) ;
#23610=EDGE_LOOP ( 'NONE', ( #34183, #54545, #17877, #14696 ) ) ;
#23611=UNCERTAINTY_MEASURE_WITH_UNIT (LENGTH_MEASURE( 1.000000000000000082E-05 ), #42378, 'distance_accuracy_value', 'NONE');
#23617=SURFACE_STYLE_USAGE ( .BOTH. , #61934 ) ;
#23618=DIRECTION ( 'NONE',  ( -1.000000000000000000, 0.000000000000000000, 0.000000000000000000 ) ) ;
#23620=ORIENTED_EDGE ( 'NONE', *, *, #8212, .F. ) ;
#23622=CARTESIAN_POINT ( 'NONE',  ( 6.330869393641157750, 43.00000000000000000, -28.38386403503541899 ) ) ;
#23640=STYLED_ITEM ( 'NONE', ( #53468 ), #17773 ) ;
#23641=VECTOR ( 'NONE', #49871, 1000.000000000000000 ) ;
#23647=FILL_AREA_STYLE_COLOUR ( '', #27316 ) ;
#23650=CARTESIAN_POINT ( 'NONE',  ( 26.00000000000001776, 15.00000000000000000, -29.68999999999999417 ) ) ;
#23651=CARTESIAN_POINT ( 'NONE',  ( 0.4644257559287117698, 42.85561152959480324, 74.47757672716494426 ) ) ;
#23655=( NAMED_UNIT ( * ) PLANE_ANGLE_UNIT ( ) SI_UNIT ( $, .RADIAN. ) );
#23666=AXIS2_PLACEMENT_3D ( 'NONE', #59131, #11301, #32755 ) ;
#23674=FACE_OUTER_BOUND ( 'NONE', #56284, .T. ) ;
#23679=CIRCLE ( 'NONE', #46172, 1.000000000000000888 ) ;
#23681=VERTEX_POINT ( 'NONE', #36795 ) ;
#23692=ORIENTED_EDGE ( 'NONE', *, *, #60335, .T. ) ;
#23702=MECHANICAL_DESIGN_GEOMETRIC_PRESENTATION_REPRESENTATION('',(#23640),#29257);
#23705=ADVANCED_FACE ( 'NONE', ( #15661 ), #58551, .T. ) ;
#23712=EDGE_LOOP ( 'NONE', ( #54724, #41032, #7047, #24531 ) ) ;
#23721=STYLED_ITEM ( 'NONE', ( #61602 ), #60130 ) ;
#23738=( GEOMETRIC_REPRESENTATION_CONTEXT ( 3 ) GLOBAL_UNCERTAINTY_ASSIGNED_CONTEXT ( ( #29956 ) ) GLOBAL_UNIT_ASSIGNED_CONTEXT ( ( #44897, #23744, #33271 ) ) REPRESENTATION_CONTEXT ( 'NONE', 'WORKASPACE' ) );
#23739=ADVANCED_FACE ( 'NONE', ( #11394 ), #12079, .F. ) ;
#23744=( NAMED_UNIT ( * ) PLANE_ANGLE_UNIT ( ) SI_UNIT ( $, .RADIAN. ) );
#23748=PRESENTATION_STYLE_ASSIGNMENT (( #50491 ) ) ;
#23750=VERTEX_POINT ( 'NONE', #64531 ) ;
#23760=ADVANCED_FACE ( 'NONE', ( #17406 ), #32864, .F. ) ;
#23764=VERTEX_POINT ( 'NONE', #66606 ) ;
#23766=SURFACE_STYLE_FILL_AREA ( #29018 ) ;
#23773=CARTESIAN_POINT ( 'NONE',  ( 8.000000000000035527, 5.000000000000000000, 77.00402776293825013 ) ) ;
#23778=( NAMED_UNIT ( * ) PLANE_ANGLE_UNIT ( ) SI_UNIT ( $, .RADIAN. ) );
#23791=CARTESIAN_POINT ( 'NONE',  ( 10.00000000000000533, 43.00000000000000000, -74.38749456993816978 ) ) ;
#23803=ORIENTED_EDGE ( 'NONE', *, *, #36207, .F. ) ;
#23810=DIRECTION ( 'NONE',  ( 0.000000000000000000, 0.000000000000000000, -1.000000000000000000 ) ) ;
#23816=FACE_OUTER_BOUND ( 'NONE', #34483, .T. ) ;
#23828=ORIENTED_EDGE ( 'NONE', *, *, #25712, .T. ) ;
#23829=( LENGTH_UNIT ( ) NAMED_UNIT ( * ) SI_UNIT ( .MILLI., .METRE. ) );
#23831=SURFACE_STYLE_USAGE ( .BOTH. , #12924 ) ;
#23835=VERTEX_POINT ( 'NONE', #3574 ) ;
#23841=DIRECTION ( 'NONE',  ( -1.000000000000000000, -0.000000000000000000, 4.625929269271505635E-16 ) ) ;
#23848=CARTESIAN_POINT ( 'NONE',  ( 30.99999999999999289, 5.000000000000000000, 24.00402776293822171 ) ) ;
#23851=ORIENTED_EDGE ( 'NONE', *, *, #69500, .T. ) ;
#23856=( NAMED_UNIT ( * ) SI_UNIT ( $, .STERADIAN. ) SOLID_ANGLE_UNIT ( ) );
#23869=COLOUR_RGB ( '', 0.08235294, 0.09019608, 0.10196078) ;
#23876=LINE ( 'NONE', #18261, #17461 ) ;
#23881=( GEOMETRIC_REPRESENTATION_CONTEXT ( 3 ) GLOBAL_UNCERTAINTY_ASSIGNED_CONTEXT ( ( #69446 ) ) GLOBAL_UNIT_ASSIGNED_CONTEXT ( ( #45447, #51028, #66867 ) ) REPRESENTATION_CONTEXT ( 'NONE', 'WORKASPACE' ) );
#23890=PRESENTATION_STYLE_ASSIGNMENT (( #46075 ) ) ;
#23899=SURFACE_SIDE_STYLE ('',( #56246 ) ) ;
#23911=DIRECTION ( 'NONE',  ( -0.000000000000000000, -1.000000000000000000, 0.000000000000000000 ) ) ;
#23945=STYLED_ITEM ( 'NONE', ( #33738 ), #29309 ) ;
#23949=CARTESIAN_POINT ( 'NONE',  ( 1.000000000000000000, 43.00000000000000000, 79.00402776293826435 ) ) ;
#23953=CARTESIAN_POINT ( 'NONE',  ( 10.00000000000001954, 42.00000000000000000, 29.68999999999999417 ) ) ;
#23974=VERTEX_POINT ( 'NONE', #14896 ) ;
#23977=SURFACE_STYLE_FILL_AREA ( #30985 ) ;
#23979=COLOUR_RGB ( '', 0.40784314, 0.44705882, 0.49803922) ;
#23997=CYLINDRICAL_SURFACE ( 'NONE', #20353, 19.99999999999998934 ) ;
#24002=FACE_OUTER_BOUND ( 'NONE', #27828, .T. ) ;
#24007=CARTESIAN_POINT ( 'NONE',  ( 0.000000000000000000, 50.00000000000000000, -60.00000000000000000 ) ) ;
#24012=AXIS2_PLACEMENT_3D ( 'NONE', #22759, #6914, #17504 ) ;
#24017=FACE_OUTER_BOUND ( 'NONE', #69387, .T. ) ;
#24020=VECTOR ( 'NONE', #47912, 1000.000000000000227 ) ;
#24028=STYLED_ITEM ( 'NONE', ( #25389 ), #38079 ) ;
#24041=AXIS2_PLACEMENT_3D ( 'NONE', #35942, #57742, #9572 ) ;
#24046=( NAMED_UNIT ( * ) PLANE_ANGLE_UNIT ( ) SI_UNIT ( $, .RADIAN. ) );
#24054=STYLED_ITEM ( 'NONE', ( #64435 ), #2613 ) ;
#24062=SURFACE_STYLE_FILL_AREA ( #50453 ) ;
#24070=CIRCLE ( 'NONE', #56665, 3.499999999999999556 ) ;
#24071=AXIS2_PLACEMENT_3D ( 'NONE', #43197, #11111, #22034 ) ;
#24076=DIRECTION ( 'NONE',  ( 0.000000000000000000, 1.000000000000000000, 0.000000000000000000 ) ) ;
#24093=CIRCLE ( 'NONE', #17400, 2.500000000000002220 ) ;
#24097=( LENGTH_UNIT ( ) NAMED_UNIT ( * ) SI_UNIT ( .MILLI., .METRE. ) );
#24101=EDGE_CURVE ( 'NONE', #10939, #28531, #44045, .T. ) ;
#24118=CYLINDRICAL_SURFACE ( 'NONE', #34150, 3.499999999999999556 ) ;
#24122=MECHANICAL_DESIGN_GEOMETRIC_PRESENTATION_REPRESENTATION('',(#44426),#60071);
#24125=ORIENTED_EDGE ( 'NONE', *, *, #31260, .F. ) ;
#24137=CARTESIAN_POINT ( 'NONE',  ( 3.000000000000029754, 42.58578643762690774, 80.00402776293826435 ) ) ;
#24138=ORIENTED_EDGE ( 'NONE', *, *, #60025, .T. ) ;
#24139=CARTESIAN_POINT ( 'NONE',  ( 0.000000000000000000, 42.00000000000000711, 44.99999999999999289 ) ) ;
#24141=CARTESIAN_POINT ( 'NONE',  ( 25.00000000000001421, 43.00000000000000000, 0.000000000000000000 ) ) ;
#24149=( NAMED_UNIT ( * ) PLANE_ANGLE_UNIT ( ) SI_UNIT ( $, .RADIAN. ) );
#24152=CARTESIAN_POINT ( 'NONE',  ( 0.000000000000000000, 42.00000000000000000, 36.50000000000000000 ) ) ;
#24155=AXIS2_PLACEMENT_3D ( 'NONE', #32906, #6845, #28268 ) ;
#24169=SURFACE_STYLE_USAGE ( .BOTH. , #40371 ) ;
#24172=( NAMED_UNIT ( * ) SI_UNIT ( $, .STERADIAN. ) SOLID_ANGLE_UNIT ( ) );
#24177=SURFACE_STYLE_FILL_AREA ( #24502 ) ;
#24179=EDGE_LOOP ( 'NONE', ( #61646, #6000, #67328, #6835 ) ) ;
#24198=PRESENTATION_STYLE_ASSIGNMENT (( #2707 ) ) ;
#24203=( NAMED_UNIT ( * ) PLANE_ANGLE_UNIT ( ) SI_UNIT ( $, .RADIAN. ) );
#24206=AXIS2_PLACEMENT_3D ( 'NONE', #57987, #63924, #9803 ) ;
#24230=CIRCLE ( 'NONE', #13038, 3.499999999999999556 ) ;
#24232=DIRECTION ( 'NONE',  ( 1.000000000000000000, 0.000000000000000000, -1.300977106640434891E-16 ) ) ;
#24239=SURFACE_STYLE_USAGE ( .BOTH. , #14043 ) ;
#24246=UNCERTAINTY_MEASURE_WITH_UNIT (LENGTH_MEASURE( 1.000000000000000082E-05 ), #17404, 'distance_accuracy_value', 'NONE');
#24261=CARTESIAN_POINT ( 'NONE',  ( 28.00000000000002842, 43.00000000000000000, 90.00000000000000000 ) ) ;
#24264=DIRECTION ( 'NONE',  ( -0.000000000000000000, -1.000000000000000000, -0.000000000000000000 ) ) ;
#24266=ORIENTED_EDGE ( 'NONE', *, *, #22312, .T. ) ;
#24269=CARTESIAN_POINT ( 'NONE',  ( 98.00000000000000000, 16.00000000000000000, 0.000000000000000000 ) ) ;
#24278=FILL_AREA_STYLE ('',( #3837 ) ) ;
#24281=CYLINDRICAL_SURFACE ( 'NONE', #27394, 1.000000000000000000 ) ;
#24288=LINE ( 'NONE', #29919, #46361 ) ;
#24299=( NAMED_UNIT ( * ) SI_UNIT ( $, .STERADIAN. ) SOLID_ANGLE_UNIT ( ) );
#24300=UNCERTAINTY_MEASURE_WITH_UNIT (LENGTH_MEASURE( 1.000000000000000082E-05 ), #66822, 'distance_accuracy_value', 'NONE');
#24301=EDGE_CURVE ( 'NONE', #60790, #6587, #5817, .T. ) ;
#24309=FILL_AREA_STYLE_COLOUR ( '', #59693 ) ;
#24316=( GEOMETRIC_REPRESENTATION_CONTEXT ( 3 ) GLOBAL_UNCERTAINTY_ASSIGNED_CONTEXT ( ( #1523 ) ) GLOBAL_UNIT_ASSIGNED_CONTEXT ( ( #37418, #27474, #59142 ) ) REPRESENTATION_CONTEXT ( 'NONE', 'WORKASPACE' ) );
#24317=CARTESIAN_POINT ( 'NONE',  ( 6.000000000000017764, 43.00000000000000000, -29.06445261836602256 ) ) ;
#24321=CARTESIAN_POINT ( 'NONE',  ( 22.83552561521075575, 27.23845256177168039, -27.27469245111273111 ) ) ;
#24323=FACE_OUTER_BOUND ( 'NONE', #21207, .T. ) ;
#24324=STYLED_ITEM ( 'NONE', ( #27632 ), #40275 ) ;
#24362=DIRECTION ( 'NONE',  ( 0.000000000000000000, 1.000000000000000000, 0.000000000000000000 ) ) ;
#24364=( LENGTH_UNIT ( ) NAMED_UNIT ( * ) SI_UNIT ( .MILLI., .METRE. ) );
#24375=FILL_AREA_STYLE ('',( #13130 ) ) ;
#24376=VERTEX_POINT ( 'NONE', #39557 ) ;
#24383=ADVANCED_FACE ( 'NONE', ( #44841 ), #45865, .T. ) ;
#24390=SURFACE_STYLE_USAGE ( .BOTH. , #30021 ) ;
#24395=DIRECTION ( 'NONE',  ( 0.000000000000000000, 1.000000000000000000, 0.000000000000000000 ) ) ;
#24406=DIRECTION ( 'NONE',  ( -0.000000000000000000, -1.000000000000000000, -0.000000000000000000 ) ) ;
#24409=CIRCLE ( 'NONE', #31171, 16.00000000000000000 ) ;
#24412=DIRECTION ( 'NONE',  ( -0.000000000000000000, 1.000000000000000000, -0.000000000000000000 ) ) ;
#24426=CARTESIAN_POINT ( 'NONE',  ( 27.00000000000001776, 42.00000000000000000, -35.50000000000000000 ) ) ;
#24434=( NAMED_UNIT ( * ) PLANE_ANGLE_UNIT ( ) SI_UNIT ( $, .RADIAN. ) );
#24438=DIRECTION ( 'NONE',  ( 0.000000000000000000, 0.000000000000000000, -1.000000000000000000 ) ) ;
#24443=FACE_OUTER_BOUND ( 'NONE', #48551, .T. ) ;
#24444=SURFACE_SIDE_STYLE ('',( #2618 ) ) ;
#24450=EDGE_CURVE ( 'NONE', #46237, #46026, #18746, .T. ) ;
#24470=DIRECTION ( 'NONE',  ( 0.000000000000000000, 0.000000000000000000, -1.000000000000000000 ) ) ;
#24473=CARTESIAN_POINT ( 'NONE',  ( 23.50000000000001776, 15.00000000000000000, 29.68999999999999417 ) ) ;
#24479=( NAMED_UNIT ( * ) PLANE_ANGLE_UNIT ( ) SI_UNIT ( $, .RADIAN. ) );
#24489=SURFACE_SIDE_STYLE ('',( #34708 ) ) ;
#24500=( GEOMETRIC_REPRESENTATION_CONTEXT ( 3 ) GLOBAL_UNCERTAINTY_ASSIGNED_CONTEXT ( ( #5244 ) ) GLOBAL_UNIT_ASSIGNED_CONTEXT ( ( #56322, #29947, #30269 ) ) REPRESENTATION_CONTEXT ( 'NONE', 'WORKASPACE' ) );
#24502=FILL_AREA_STYLE ('',( #1958 ) ) ;
#24505=AXIS2_PLACEMENT_3D ( 'NONE', #22238, #43734, #16982 ) ;
#24508=SURFACE_SIDE_STYLE ('',( #19235 ) ) ;
#24510=ORIENTED_EDGE ( 'NONE', *, *, #34379, .T. ) ;
#24519=( LENGTH_UNIT ( ) NAMED_UNIT ( * ) SI_UNIT ( .MILLI., .METRE. ) );
#24526=EDGE_CURVE ( 'NONE', #68025, #6587, #68347, .T. ) ;
#24527=DIRECTION ( 'NONE',  ( 1.000000000000000000, -0.000000000000000000, -1.300977106640434891E-16 ) ) ;
#24528=SURFACE_STYLE_FILL_AREA ( #57609 ) ;
#24531=ORIENTED_EDGE ( 'NONE', *, *, #39346, .T. ) ;
#24538=( NAMED_UNIT ( * ) SI_UNIT ( $, .STERADIAN. ) SOLID_ANGLE_UNIT ( ) );
#24553=EDGE_CURVE ( 'NONE', #408, #4398, #35647, .T. ) ;
#24558=DIRECTION ( 'NONE',  ( -1.000000000000000000, 0.000000000000000000, 0.000000000000000000 ) ) ;
#24559=ORIENTED_EDGE ( 'NONE', *, *, #6662, .T. ) ;
#24561=( GEOMETRIC_REPRESENTATION_CONTEXT ( 3 ) GLOBAL_UNCERTAINTY_ASSIGNED_CONTEXT ( ( #19907 ) ) GLOBAL_UNIT_ASSIGNED_CONTEXT ( ( #5522, #58325, #43246 ) ) REPRESENTATION_CONTEXT ( 'NONE', 'WORKASPACE' ) );
#24563=DIRECTION ( 'NONE',  ( -0.000000000000000000, -1.000000000000000000, 0.000000000000000000 ) ) ;
#24566=SURFACE_STYLE_FILL_AREA ( #3075 ) ;
#24571=( NAMED_UNIT ( * ) PLANE_ANGLE_UNIT ( ) SI_UNIT ( $, .RADIAN. ) );
#24572=TOROIDAL_SURFACE ( 'NONE', #38095, 1.499999999999998668, 1.000000000000000000 ) ;
#24581=( GEOMETRIC_REPRESENTATION_CONTEXT ( 3 ) GLOBAL_UNCERTAINTY_ASSIGNED_CONTEXT ( ( #51775 ) ) GLOBAL_UNIT_ASSIGNED_CONTEXT ( ( #65605, #23380, #39253 ) ) REPRESENTATION_CONTEXT ( 'NONE', 'WORKASPACE' ) );
#24583=CARTESIAN_POINT ( 'NONE',  ( 179.4361977533490347, 5.000000000000000000, -103.7004518695263044 ) ) ;
#24584=EDGE_CURVE ( 'NONE', #55142, #38982, #43996, .T. ) ;
#24597=FACE_OUTER_BOUND ( 'NONE', #47524, .T. ) ;
#24606=ORIENTED_EDGE ( 'NONE', *, *, #43877, .T. ) ;
#24619=CIRCLE ( 'NONE', #46005, 1.000000000000000888 ) ;
#24634=EDGE_LOOP ( 'NONE', ( #40322, #16597, #53608, #36298, #35457, #26129, #1209 ) ) ;
#24647=CARTESIAN_POINT ( 'NONE',  ( 31.00000000000002132, 42.00000000000000000, 75.00000000000000000 ) ) ;
#24648=ORIENTED_EDGE ( 'NONE', *, *, #58546, .F. ) ;
#24664=DIRECTION ( 'NONE',  ( -0.000000000000000000, 1.000000000000000000, -0.000000000000000000 ) ) ;
#24667=VECTOR ( 'NONE', #16598, 1000.000000000000000 ) ;
#24672=AXIS2_PLACEMENT_3D ( 'NONE', #35306, #51839, #61650 ) ;
#24686=EDGE_CURVE ( 'NONE', #38153, #10996, #8162, .T. ) ;
#24696=CARTESIAN_POINT ( 'NONE',  ( 82.09357085539566867, 5.000000000000000000, -32.00402776293823592 ) ) ;
#24706=AXIS2_PLACEMENT_3D ( 'NONE', #29122, #1996, #61161 ) ;
#24713=AXIS2_PLACEMENT_3D ( 'NONE', #46809, #51338, #68216 ) ;
#24714=PRESENTATION_STYLE_ASSIGNMENT (( #68016 ) ) ;
#24715=EDGE_LOOP ( 'NONE', ( #65494, #2466, #44105, #25604 ) ) ;
#24720=VERTEX_POINT ( 'NONE', #48666 ) ;
#24729=VECTOR ( 'NONE', #24664, 1000.000000000000000 ) ;
#24730=CARTESIAN_POINT ( 'NONE',  ( 7.000000000000017764, 42.74314482547740113, -27.71473342867655987 ) ) ;
#24732=CIRCLE ( 'NONE', #39343, 17.00000000000000711 ) ;
#24733=PRESENTATION_STYLE_ASSIGNMENT (( #66988 ) ) ;
#24742=ORIENTED_EDGE ( 'NONE', *, *, #5383, .T. ) ;
#24758=EDGE_CURVE ( 'NONE', #23750, #23681, #38798, .T. ) ;
#24760=AXIS2_PLACEMENT_3D ( 'NONE', #36355, #31019, #57778 ) ;
#24763=SURFACE_SIDE_STYLE ('',( #18806 ) ) ;
#24771=LINE ( 'NONE', #51189, #14960 ) ;
#24774=FILL_AREA_STYLE_COLOUR ( '', #27428 ) ;
#24778=LINE ( 'NONE', #56104, #49614 ) ;
#24785=CARTESIAN_POINT ( 'NONE',  ( 2.000000000000015543, 26.00000000000000355, 23.99999999999999645 ) ) ;
#24795=UNCERTAINTY_MEASURE_WITH_UNIT (LENGTH_MEASURE( 1.000000000000000082E-05 ), #24519, 'distance_accuracy_value', 'NONE');
#24798=SURFACE_STYLE_FILL_AREA ( #7593 ) ;
#24806=AXIS2_PLACEMENT_3D ( 'NONE', #7309, #28736, #66031 ) ;
#24807=SURFACE_STYLE_FILL_AREA ( #13566 ) ;
#24821=FILL_AREA_STYLE ('',( #15367 ) ) ;
#24827=AXIS2_PLACEMENT_3D ( 'NONE', #62759, #29732, #46659 ) ;
#24834=PLANE ( 'NONE',  #42806 ) ;
#24839=EDGE_CURVE ( 'NONE', #26439, #33948, #57559, .T. ) ;
#24851=DIRECTION ( 'NONE',  ( 0.000000000000000000, -1.000000000000000000, 0.000000000000000000 ) ) ;
#24852=ADVANCED_FACE ( 'NONE', ( #50355 ), #17672, .F. ) ;
#24855=VERTEX_POINT ( 'NONE', #33813 ) ;
#24856=FILL_AREA_STYLE_COLOUR ( '', #29645 ) ;
#24860=FILL_AREA_STYLE ('',( #7055 ) ) ;
#24865=ORIENTED_EDGE ( 'NONE', *, *, #47304, .T. ) ;
#24870=CARTESIAN_POINT ( 'NONE',  ( 23.00000000000000000, 5.000000000000000000, -24.00402776293825013 ) ) ;
#24872=STYLED_ITEM ( 'NONE', ( #63968 ), #22015 ) ;
#24873=AXIS2_PLACEMENT_3D ( 'NONE', #32323, #48208, #65386 ) ;
#24879=FACE_OUTER_BOUND ( 'NONE', #36935, .T. ) ;
#24911=CARTESIAN_POINT ( 'NONE',  ( 22.00000000000002132, 50.00000000000000000, 46.00000000000000000 ) ) ;
#24920=VECTOR ( 'NONE', #38216, 1000.000000000000000 ) ;
#24922=DIRECTION ( 'NONE',  ( 0.000000000000000000, 0.000000000000000000, -1.000000000000000000 ) ) ;
#24925=CARTESIAN_POINT ( 'NONE',  ( 2.000000000000008882, 26.00000000000000355, -24.00000000000000355 ) ) ;
#24936=( LENGTH_UNIT ( ) NAMED_UNIT ( * ) SI_UNIT ( .MILLI., .METRE. ) );
#24950=SURFACE_SIDE_STYLE ('',( #62578 ) ) ;
#24953=LINE ( 'NONE', #51353, #40991 ) ;
#24958=ORIENTED_EDGE ( 'NONE', *, *, #68464, .F. ) ;
#24972=( LENGTH_UNIT ( ) NAMED_UNIT ( * ) SI_UNIT ( .MILLI., .METRE. ) );
#24978=ORIENTED_EDGE ( 'NONE', *, *, #68940, .F. ) ;
#24981=UNCERTAINTY_MEASURE_WITH_UNIT (LENGTH_MEASURE( 1.000000000000000082E-05 ), #50719, 'distance_accuracy_value', 'NONE');
#24985=FACE_BOUND ( 'NONE', #4559, .T. ) ;
#24988=CARTESIAN_POINT ( 'NONE',  ( 109.0067032876572455, 14.00000000000000000, -19.20378738324562207 ) ) ;
#24989=ORIENTED_EDGE ( 'NONE', *, *, #40301, .T. ) ;
#24991=LINE ( 'NONE', #46500, #14313 ) ;
#25011=CIRCLE ( 'NONE', #53088, 1.000000000000000888 ) ;
#25013=( LENGTH_UNIT ( ) NAMED_UNIT ( * ) SI_UNIT ( .MILLI., .METRE. ) );
#25015=ORIENTED_EDGE ( 'NONE', *, *, #13825, .F. ) ;
#25032=ORIENTED_EDGE ( 'NONE', *, *, #37471, .T. ) ;
#25037=COLOUR_RGB ( '', 0.40784314, 0.44705882, 0.49803922) ;
#25046=CARTESIAN_POINT ( 'NONE',  ( 21.00000000000001776, 42.00000000000000000, -29.68999999999999417 ) ) ;
#25051=ORIENTED_EDGE ( 'NONE', *, *, #49039, .T. ) ;
#25055=( GEOMETRIC_REPRESENTATION_CONTEXT ( 3 ) GLOBAL_UNCERTAINTY_ASSIGNED_CONTEXT ( ( #41084 ) ) GLOBAL_UNIT_ASSIGNED_CONTEXT ( ( #786, #22331, #49769 ) ) REPRESENTATION_CONTEXT ( 'NONE', 'WORKASPACE' ) );
#25058=ORIENTED_EDGE ( 'NONE', *, *, #38497, .T. ) ;
#25059=LINE ( 'NONE', #14169, #3340 ) ;
#25060=EDGE_CURVE ( 'NONE', #42967, #5418, #7039, .T. ) ;
#25071=DIRECTION ( 'NONE',  ( -0.000000000000000000, 1.000000000000000000, 0.000000000000000000 ) ) ;
#25094=PLANE ( 'NONE',  #16010 ) ;
#25099=CARTESIAN_POINT ( 'NONE',  ( 27.00000000000001776, 15.00000000000000000, -35.50000000000000000 ) ) ;
#25101=DIRECTION ( 'NONE',  ( 0.000000000000000000, 1.000000000000000000, 0.000000000000000000 ) ) ;
#25107=ADVANCED_FACE ( 'NONE', ( #36980 ), #12612, .T. ) ;
#25110=EDGE_CURVE ( 'NONE', #18094, #62990, #28235, .T. ) ;
#25114=STYLED_ITEM ( 'NONE', ( #6875 ), #9057 ) ;
#25115=EDGE_CURVE ( 'NONE', #62949, #4733, #39737, .T. ) ;
#25116=CARTESIAN_POINT ( 'NONE',  ( 8.000000000000035527, 5.000000000000000000, -77.00402776293825013 ) ) ;
#25121=MECHANICAL_DESIGN_GEOMETRIC_PRESENTATION_REPRESENTATION('',(#16167),#38733);
#25131=DIRECTION ( 'NONE',  ( 0.000000000000000000, 0.000000000000000000, 1.000000000000000000 ) ) ;
#25139=DIRECTION ( 'NONE',  ( 0.000000000000000000, 0.000000000000000000, -1.000000000000000000 ) ) ;
#25142=SURFACE_STYLE_FILL_AREA ( #51524 ) ;
#25147=( GEOMETRIC_REPRESENTATION_CONTEXT ( 3 ) GLOBAL_UNCERTAINTY_ASSIGNED_CONTEXT ( ( #29992 ) ) GLOBAL_UNIT_ASSIGNED_CONTEXT ( ( #37368, #15884, #41579 ) ) REPRESENTATION_CONTEXT ( 'NONE', 'WORKASPACE' ) );
#25148=( NAMED_UNIT ( * ) SI_UNIT ( $, .STERADIAN. ) SOLID_ANGLE_UNIT ( ) );
#25155=( GEOMETRIC_REPRESENTATION_CONTEXT ( 3 ) GLOBAL_UNCERTAINTY_ASSIGNED_CONTEXT ( ( #43406 ) ) GLOBAL_UNIT_ASSIGNED_CONTEXT ( ( #55608, #12323, #9857 ) ) REPRESENTATION_CONTEXT ( 'NONE', 'WORKASPACE' ) );
#25158=EDGE_LOOP ( 'NONE', ( #33782, #7077, #58719, #47331, #34480, #26796, #40521, #34781, #37795, #66085 ) ) ;
#25161=DIRECTION ( 'NONE',  ( 0.000000000000000000, -0.3420201433256630508, 0.9396926207859105373 ) ) ;
#25163=LINE ( 'NONE', #15347, #11123 ) ;
#25165=AXIS2_PLACEMENT_3D ( 'NONE', #16477, #37941, #59315 ) ;
#25182=EDGE_CURVE ( 'NONE', #1374, #3091, #8042, .T. ) ;
#25195=STYLED_ITEM ( 'NONE', ( #5077 ), #413 ) ;
#25199=COLOUR_RGB ( '', 0.08235294, 0.09019608, 0.10196078) ;
#25201=CIRCLE ( 'NONE', #15099, 1.000000000000000888 ) ;
#25204=CARTESIAN_POINT ( 'NONE',  ( 3.000000000000002665, 5.569094604152796002, 2.026984667724101463 ) ) ;
#25205=( LENGTH_UNIT ( ) NAMED_UNIT ( * ) SI_UNIT ( .MILLI., .METRE. ) );
#25214=LINE ( 'NONE', #35775, #54188 ) ;
#25215=VERTEX_POINT ( 'NONE', #44345 ) ;
#25217=VECTOR ( 'NONE', #49072, 1000.000000000000000 ) ;
#25220=ADVANCED_FACE ( 'NONE', ( #65746 ), #39054, .T. ) ;
#25221=CIRCLE ( 'NONE', #1625, 5.000000000000004441 ) ;
#25222=FILL_AREA_STYLE ('',( #3730 ) ) ;
#25229=DIRECTION ( 'NONE',  ( 1.000000000000000000, 0.000000000000000000, -1.300977106640434891E-16 ) ) ;
#25232=( NAMED_UNIT ( * ) SI_UNIT ( $, .STERADIAN. ) SOLID_ANGLE_UNIT ( ) );
#25234=ORIENTED_EDGE ( 'NONE', *, *, #55670, .T. ) ;
#25236=CARTESIAN_POINT ( 'NONE',  ( 6.000000000000017764, 43.00000000000000000, -35.50000000000000000 ) ) ;
#25248=CARTESIAN_POINT ( 'NONE',  ( 29.00000000000002842, 42.00000000000000000, 80.00402776293826435 ) ) ;
#25269=SURFACE_STYLE_FILL_AREA ( #57636 ) ;
#25271=EDGE_CURVE ( 'NONE', #4737, #19853, #35118, .T. ) ;
#25279=( NAMED_UNIT ( * ) PLANE_ANGLE_UNIT ( ) SI_UNIT ( $, .RADIAN. ) );
#25289=COLOUR_RGB ( '', 0.40784314, 0.44705882, 0.49803922) ;
#25297=SURFACE_STYLE_FILL_AREA ( #3813 ) ;
#25332=EDGE_CURVE ( 'NONE', #4733, #22405, #9215, .T. ) ;
#25335=CARTESIAN_POINT ( 'NONE',  ( 16.00000000000001776, 42.00000000000000000, 29.68999999999999417 ) ) ;
#25336=EDGE_CURVE ( 'NONE', #34757, #9284, #19264, .T. ) ;
#25337=ORIENTED_EDGE ( 'NONE', *, *, #28891, .T. ) ;
#25354=CARTESIAN_POINT ( 'NONE',  ( 22.29420333151774614, 25.82372757702023236, 27.50001041218374453 ) ) ;
#25357=DIRECTION ( 'NONE',  ( 0.000000000000000000, 0.000000000000000000, -1.000000000000000000 ) ) ;
#25369=VECTOR ( 'NONE', #65391, 1000.000000000000000 ) ;
#25379=( NAMED_UNIT ( * ) PLANE_ANGLE_UNIT ( ) SI_UNIT ( $, .RADIAN. ) );
#25380=CIRCLE ( 'NONE', #19810, 111.0000000000000142 ) ;
#25381=LINE ( 'NONE', #8862, #24729 ) ;
#25388=AXIS2_PLACEMENT_3D ( 'NONE', #68942, #37664, #20750 ) ;
#25389=PRESENTATION_STYLE_ASSIGNMENT (( #3915 ) ) ;
#25396=LINE ( 'NONE', #40567, #39191 ) ;
#25400=CARTESIAN_POINT ( 'NONE',  ( 36.00000000000002842, 5.000000000000000000, 32.00402776293825724 ) ) ;
#25426=DIRECTION ( 'NONE',  ( 0.000000000000000000, 1.000000000000000000, 0.000000000000000000 ) ) ;
#25437=( LENGTH_UNIT ( ) NAMED_UNIT ( * ) SI_UNIT ( .MILLI., .METRE. ) );
#25445=( LENGTH_UNIT ( ) NAMED_UNIT ( * ) SI_UNIT ( .MILLI., .METRE. ) );
#25448=CARTESIAN_POINT ( 'NONE',  ( 16.00000000000001776, 15.00000000000000000, -29.68999999999999417 ) ) ;
#25457=DIRECTION ( 'NONE',  ( 1.000000000000000000, 0.000000000000000000, 0.000000000000000000 ) ) ;
#25460=VECTOR ( 'NONE', #21990, 1000.000000000000000 ) ;
#25463=DIRECTION ( 'NONE',  ( 0.000000000000000000, 0.000000000000000000, 1.000000000000000000 ) ) ;
#25465=ORIENTED_EDGE ( 'NONE', *, *, #56534, .F. ) ;
#25470=PLANE ( 'NONE',  #30383 ) ;
#25475=EDGE_CURVE ( 'NONE', #69517, #39729, #6821, .T. ) ;
#25477=DIRECTION ( 'NONE',  ( 0.000000000000000000, -1.000000000000000000, 0.000000000000000000 ) ) ;
#25478=LINE ( 'NONE', #14961, #26329 ) ;
#25490=ORIENTED_EDGE ( 'NONE', *, *, #56144, .T. ) ;
#25491=ADVANCED_FACE ( 'NONE', ( #21987 ), #60620, .T. ) ;
#25495=CARTESIAN_POINT ( 'NONE',  ( 22.99999999999998934, 0.000000000000000000, 37.00402776293825724 ) ) ;
#25515=CARTESIAN_POINT ( 'NONE',  ( 8.000000000000035527, 5.000000000000000000, -77.00402776293825013 ) ) ;
#25528=LINE ( 'NONE', #68821, #32450 ) ;
#25542=MECHANICAL_DESIGN_GEOMETRIC_PRESENTATION_REPRESENTATION('',(#4193),#7660);
#25551=CARTESIAN_POINT ( 'NONE',  ( 22.29422224269975672, 26.00000000000000355, -27.50000000000000711 ) ) ;
#25556=LINE ( 'NONE', #63886, #1617 ) ;
#25561=VERTEX_POINT ( 'NONE', #39925 ) ;
#25573=( NAMED_UNIT ( * ) SI_UNIT ( $, .STERADIAN. ) SOLID_ANGLE_UNIT ( ) );
#25574=( NAMED_UNIT ( * ) SI_UNIT ( $, .STERADIAN. ) SOLID_ANGLE_UNIT ( ) );
#25588=DIRECTION ( 'NONE',  ( 0.000000000000000000, -1.000000000000000000, 0.000000000000000000 ) ) ;
#25604=ORIENTED_EDGE ( 'NONE', *, *, #41585, .T. ) ;
#25609=FILL_AREA_STYLE ('',( #31585 ) ) ;
#25610=MECHANICAL_DESIGN_GEOMETRIC_PRESENTATION_REPRESENTATION('',(#43600),#61554);
#25619=UNCERTAINTY_MEASURE_WITH_UNIT (LENGTH_MEASURE( 1.000000000000000082E-05 ), #36213, 'distance_accuracy_value', 'NONE');
#25631=( GEOMETRIC_REPRESENTATION_CONTEXT ( 3 ) GLOBAL_UNCERTAINTY_ASSIGNED_CONTEXT ( ( #34854 ) ) GLOBAL_UNIT_ASSIGNED_CONTEXT ( ( #64770, #2050, #11297 ) ) REPRESENTATION_CONTEXT ( 'NONE', 'WORKASPACE' ) );
#25632=ORIENTED_EDGE ( 'NONE', *, *, #49116, .T. ) ;
#25636=DIRECTION ( 'NONE',  ( -0.000000000000000000, -1.000000000000000000, -0.000000000000000000 ) ) ;
#25641=DIRECTION ( 'NONE',  ( 0.000000000000000000, 0.000000000000000000, 1.000000000000000000 ) ) ;
#25645=FILL_AREA_STYLE ('',( #21413 ) ) ;
#25656=ORIENTED_EDGE ( 'NONE', *, *, #15680, .T. ) ;
#25659=ADVANCED_FACE ( 'NONE', ( #20511 ), #25094, .F. ) ;
#25669=CARTESIAN_POINT ( 'NONE',  ( 26.00000000000001776, 43.00000000000000000, 36.50000000000000000 ) ) ;
#25676=UNCERTAINTY_MEASURE_WITH_UNIT (LENGTH_MEASURE( 1.000000000000000082E-05 ), #28297, 'distance_accuracy_value', 'NONE');
#25680=ORIENTED_EDGE ( 'NONE', *, *, #47785, .F. ) ;
#25682=DIRECTION ( 'NONE',  ( 1.000000000000000000, 0.000000000000000000, 0.000000000000000000 ) ) ;
#25687=COLOUR_RGB ( '', 0.08235294, 0.09019608, 0.10196078) ;
#25704=MECHANICAL_DESIGN_GEOMETRIC_PRESENTATION_REPRESENTATION('',(#44891),#59440);
#25706=EDGE_LOOP ( 'NONE', ( #7606, #664, #38029, #9086 ) ) ;
#25712=EDGE_CURVE ( 'NONE', #68025, #38153, #26472, .T. ) ;
#25718=SURFACE_SIDE_STYLE ('',( #31005 ) ) ;
#25720=UNCERTAINTY_MEASURE_WITH_UNIT (LENGTH_MEASURE( 1.000000000000000082E-05 ), #7268, 'distance_accuracy_value', 'NONE');
#25726=ADVANCED_FACE ( 'NONE', ( #47287, #47655 ), #68359, .T. ) ;
#25731=VERTEX_POINT ( 'NONE', #43060 ) ;
#25732=DIRECTION ( 'NONE',  ( 0.000000000000000000, 0.000000000000000000, 1.000000000000000000 ) ) ;
#25742=ORIENTED_EDGE ( 'NONE', *, *, #31299, .T. ) ;
#25751=STYLED_ITEM ( 'NONE', ( #50652 ), #51411 ) ;
#25753=DIRECTION ( 'NONE',  ( 0.000000000000000000, 0.000000000000000000, -1.000000000000000000 ) ) ;
#25755=DIRECTION ( 'NONE',  ( 1.000000000000000000, 0.000000000000000000, -1.300977106640442040E-16 ) ) ;
#25756=EDGE_LOOP ( 'NONE', ( #7327, #5318, #13663, #58143 ) ) ;
#25763=( GEOMETRIC_REPRESENTATION_CONTEXT ( 3 ) GLOBAL_UNCERTAINTY_ASSIGNED_CONTEXT ( ( #49584 ) ) GLOBAL_UNIT_ASSIGNED_CONTEXT ( ( #36125, #5365, #53910 ) ) REPRESENTATION_CONTEXT ( 'NONE', 'WORKASPACE' ) );
#25768=DIRECTION ( 'NONE',  ( 0.000000000000000000, 1.000000000000000000, 0.000000000000000000 ) ) ;
#25779=CYLINDRICAL_SURFACE ( 'NONE', #29457, 4.999999999999997335 ) ;
#25783=VECTOR ( 'NONE', #14554, 1000.000000000000000 ) ;
#25798=ADVANCED_FACE ( 'NONE', ( #22595 ), #38117, .F. ) ;
#25802=( NAMED_UNIT ( * ) SI_UNIT ( $, .STERADIAN. ) SOLID_ANGLE_UNIT ( ) );
#25805=SURFACE_STYLE_USAGE ( .BOTH. , #62408 ) ;
#25807=FILL_AREA_STYLE ('',( #26496 ) ) ;
#25828=LINE ( 'NONE', #47341, #40637 ) ;
#25831=SURFACE_STYLE_USAGE ( .BOTH. , #4348 ) ;
#25833=DIRECTION ( 'NONE',  ( 0.000000000000000000, 0.000000000000000000, -1.000000000000000000 ) ) ;
#25837=CARTESIAN_POINT ( 'NONE',  ( 0.000000000000000000, 42.00000000000000000, 36.50000000000000000 ) ) ;
#25849=CARTESIAN_POINT ( 'NONE',  ( 0.9999999999999991118, 50.00000000000000000, 60.00000000000000000 ) ) ;
#25873=EDGE_LOOP ( 'NONE', ( #20396, #59125, #18698, #39887 ) ) ;
#25874=FACE_OUTER_BOUND ( 'NONE', #62724, .T. ) ;
#25887=SURFACE_STYLE_FILL_AREA ( #4412 ) ;
#25890=DIRECTION ( 'NONE',  ( 0.000000000000000000, 0.000000000000000000, -1.000000000000000000 ) ) ;
#25899=PRESENTATION_STYLE_ASSIGNMENT (( #64227 ) ) ;
#25907=( LENGTH_UNIT ( ) NAMED_UNIT ( * ) SI_UNIT ( .MILLI., .METRE. ) );
#25929=CARTESIAN_POINT ( 'NONE',  ( 57.00000000000000000, 16.00000000000000000, 55.00402776293826435 ) ) ;
#25938=ORIENTED_EDGE ( 'NONE', *, *, #52333, .F. ) ;
#25944=VERTEX_POINT ( 'NONE', #2821 ) ;
#25955=DIRECTION ( 'NONE',  ( -1.000000000000000000, 0.000000000000000000, 0.000000000000000000 ) ) ;
#25963=ADVANCED_FACE ( 'NONE', ( #7107 ), #53095, .T. ) ;
#25974=PRODUCT ( '1. Base', '1. Base', '', ( #45914 ) ) ;
#25975=CARTESIAN_POINT ( 'NONE',  ( 23.50000000000001776, -3.148064030671221758, -29.68999999999999417 ) ) ;
#25981=ORIENTED_EDGE ( 'NONE', *, *, #33451, .T. ) ;
#25996=ORIENTED_EDGE ( 'NONE', *, *, #20248, .T. ) ;
#26001=CARTESIAN_POINT ( 'NONE',  ( 33.00000000000002132, 13.00000000000000178, 80.00402776293826435 ) ) ;
#26014=ORIENTED_EDGE ( 'NONE', *, *, #38403, .T. ) ;
#26022=COLOUR_RGB ( '', 0.31764706, 0.68627451, 0.89019608) ;
#26030=ORIENTED_EDGE ( 'NONE', *, *, #42705, .T. ) ;
#26031=CARTESIAN_POINT ( 'NONE',  ( 22.49375942073035617, 25.15171118985935550, 27.39868845849637324 ) ) ;
#26033=( NAMED_UNIT ( * ) SI_UNIT ( $, .STERADIAN. ) SOLID_ANGLE_UNIT ( ) );
#26051=EDGE_CURVE ( 'NONE', #54496, #55122, #54230, .T. ) ;
#26058=CARTESIAN_POINT ( 'NONE',  ( 29.00000000000002842, 35.42594141563417054, 80.00402776293826435 ) ) ;
#26060=MECHANICAL_DESIGN_GEOMETRIC_PRESENTATION_REPRESENTATION('',(#57555),#65384);
#26068=DIRECTION ( 'NONE',  ( 0.000000000000000000, -1.000000000000000000, 0.000000000000000000 ) ) ;
#26069=ORIENTED_EDGE ( 'NONE', *, *, #58695, .F. ) ;
#26083=VECTOR ( 'NONE', #47969, 1000.000000000000000 ) ;
#26088=LINE ( 'NONE', #38078, #26083 ) ;
#26089=EDGE_CURVE ( 'NONE', #50403, #26109, #27284, .T. ) ;
#26090=COLOUR_RGB ( '', 0.08235294, 0.09019608, 0.10196078) ;
#26103=( NAMED_UNIT ( * ) SI_UNIT ( $, .STERADIAN. ) SOLID_ANGLE_UNIT ( ) );
#26109=VERTEX_POINT ( 'NONE', #41228 ) ;
#26113=VECTOR ( 'NONE', #58480, 1000.000000000000000 ) ;
#26121=CYLINDRICAL_SURFACE ( 'NONE', #16791, 1.000000000000000888 ) ;
#26129=ORIENTED_EDGE ( 'NONE', *, *, #30147, .T. ) ;
#26156=FILL_AREA_STYLE_COLOUR ( '', #65331 ) ;
#26159=FACE_OUTER_BOUND ( 'NONE', #837, .T. ) ;
#26162=FILL_AREA_STYLE_COLOUR ( '', #16843 ) ;
#26168=DIRECTION ( 'NONE',  ( 1.300977106640434891E-16, -0.000000000000000000, 1.000000000000000000 ) ) ;
#26170=EDGE_CURVE ( 'NONE', #14584, #29977, #59902, .T. ) ;
#26178=CARTESIAN_POINT ( 'NONE',  ( 10.00000000000000533, 50.00000000000000000, -46.00000000000000000 ) ) ;
#26186=CIRCLE ( 'NONE', #32935, 113.0000000000000284 ) ;
#26189=DIRECTION ( 'NONE',  ( -1.239088197126290817E-16, 0.000000000000000000, -1.000000000000000000 ) ) ;
#26193=CARTESIAN_POINT ( 'NONE',  ( 93.00000000000000000, 0.9999999999999991118, 0.000000000000000000 ) ) ;
#26195=EDGE_CURVE ( 'NONE', #25944, #22594, #27411, .T. ) ;
#26213=ADVANCED_FACE ( 'NONE', ( #26392 ), #16905, .F. ) ;
#26221=AXIS2_PLACEMENT_3D ( 'NONE', #59368, #54456, #17217 ) ;
#26227=( GEOMETRIC_REPRESENTATION_CONTEXT ( 3 ) GLOBAL_UNCERTAINTY_ASSIGNED_CONTEXT ( ( #10760 ) ) GLOBAL_UNIT_ASSIGNED_CONTEXT ( ( #45869, #67652, #51469 ) ) REPRESENTATION_CONTEXT ( 'NONE', 'WORKASPACE' ) );
#26230=UNCERTAINTY_MEASURE_WITH_UNIT (LENGTH_MEASURE( 1.000000000000000082E-05 ), #29303, 'distance_accuracy_value', 'NONE');
#26244=CARTESIAN_POINT ( 'NONE',  ( 3.000000000000002665, 42.00000000000000000, -89.00000000000000000 ) ) ;
#26248=DIRECTION ( 'NONE',  ( 0.000000000000000000, 1.000000000000000000, 0.000000000000000000 ) ) ;
#26249=CARTESIAN_POINT ( 'NONE',  ( 23.50000000000001776, 42.00000000000000000, -29.68999999999999417 ) ) ;
#26250=LINE ( 'NONE', #21310, #67714 ) ;
#26259=CARTESIAN_POINT ( 'NONE',  ( 2.999999999999998668, 5.000000000000000000, -37.00402776293829277 ) ) ;
#26261=SURFACE_STYLE_FILL_AREA ( #10790 ) ;
#26276=VECTOR ( 'NONE', #42650, 1000.000000000000000 ) ;
#26303=CARTESIAN_POINT ( 'NONE',  ( 57.00000000000000000, 5.000000000000000000, -60.00402776293827145 ) ) ;
#26304=( NAMED_UNIT ( * ) PLANE_ANGLE_UNIT ( ) SI_UNIT ( $, .RADIAN. ) );
#26312=CIRCLE ( 'NONE', #30832, 1.000000000000000888 ) ;
#26321=FACE_OUTER_BOUND ( 'NONE', #592, .T. ) ;
#26327=AXIS2_PLACEMENT_3D ( 'NONE', #42794, #5420, #37160 ) ;
#26329=VECTOR ( 'NONE', #14591, 1000.000000000000000 ) ;
#26330=UNCERTAINTY_MEASURE_WITH_UNIT (LENGTH_MEASURE( 1.000000000000000082E-05 ), #32350, 'distance_accuracy_value', 'NONE');
#26333=SURFACE_STYLE_FILL_AREA ( #63636 ) ;
#26335=CARTESIAN_POINT ( 'NONE',  ( 16.00000000000001776, 15.00000000000000000, -29.68999999999999417 ) ) ;
#26341=FACE_BOUND ( 'NONE', #1157, .T. ) ;
#26347=EDGE_CURVE ( 'NONE', #32128, #53024, #7017, .T. ) ;
#26366=LINE ( 'NONE', #25669, #50906 ) ;
#26369=STYLED_ITEM ( 'NONE', ( #11738 ), #62457 ) ;
#26384=CARTESIAN_POINT ( 'NONE',  ( 22.70969830132048628, 24.88211553739179394, 27.31720690014012121 ) ) ;
#26391=DIRECTION ( 'NONE',  ( 0.000000000000000000, 0.000000000000000000, -1.000000000000000000 ) ) ;
#26392=FACE_OUTER_BOUND ( 'NONE', #56361, .T. ) ;
#26393=AXIS2_PLACEMENT_3D ( 'NONE', #11390, #53947, #65553 ) ;
#26396=VERTEX_POINT ( 'NONE', #4480 ) ;
#26415=CIRCLE ( 'NONE', #45560, 16.99999999999998579 ) ;
#26416=DIRECTION ( 'NONE',  ( 0.000000000000000000, 0.000000000000000000, -1.000000000000000000 ) ) ;
#26421=DIRECTION ( 'NONE',  ( 1.000000000000000000, -0.000000000000000000, -0.000000000000000000 ) ) ;
#26424=( NAMED_UNIT ( * ) SI_UNIT ( $, .STERADIAN. ) SOLID_ANGLE_UNIT ( ) );
#26431=VERTEX_POINT ( 'NONE', #8751 ) ;
#26433=FILL_AREA_STYLE_COLOUR ( '', #38325 ) ;
#26439=VERTEX_POINT ( 'NONE', #24911 ) ;
#26440=EDGE_CURVE ( 'NONE', #65467, #66860, #20644, .T. ) ;
#26455=VERTEX_POINT ( 'NONE', #56587 ) ;
#26456=( LENGTH_UNIT ( ) NAMED_UNIT ( * ) SI_UNIT ( .MILLI., .METRE. ) );
#26468=ORIENTED_EDGE ( 'NONE', *, *, #5371, .T. ) ;
#26469=DIRECTION ( 'NONE',  ( 0.000000000000000000, -0.9984713486292863260, 0.05527174654752588234 ) ) ;
#26472=LINE ( 'NONE', #36393, #6982 ) ;
#26475=FILL_AREA_STYLE_COLOUR ( '', #4763 ) ;
#26494=DIRECTION ( 'NONE',  ( 0.9418169057949938860, 0.000000000000000000, 0.3361263392814427542 ) ) ;
#26496=FILL_AREA_STYLE_COLOUR ( '', #20027 ) ;
#26500=DIRECTION ( 'NONE',  ( 0.000000000000000000, 0.000000000000000000, -1.000000000000000000 ) ) ;
#26501=( NAMED_UNIT ( * ) PLANE_ANGLE_UNIT ( ) SI_UNIT ( $, .RADIAN. ) );
#26529=CARTESIAN_POINT ( 'NONE',  ( 30.99999999999999289, 0.000000000000000000, 24.00402776293822171 ) ) ;
#26532=ORIENTED_EDGE ( 'NONE', *, *, #30740, .F. ) ;
#26551=CARTESIAN_POINT ( 'NONE',  ( 57.00000000000000000, 0.000000000000000000, -60.00402776293825724 ) ) ;
#26555=FACE_BOUND ( 'NONE', #25158, .T. ) ;
#26556=AXIS2_PLACEMENT_3D ( 'NONE', #56484, #45285, #7952 ) ;
#26565=LINE ( 'NONE', #57194, #5534 ) ;
#26582=CYLINDRICAL_SURFACE ( 'NONE', #15121, 1.000000000000000000 ) ;
#26601=LINE ( 'NONE', #10458, #14862 ) ;
#26617=DIRECTION ( 'NONE',  ( -0.3361263392814427542, 0.000000000000000000, 0.9418169057949938860 ) ) ;
#26622=ORIENTED_EDGE ( 'NONE', *, *, #56688, .T. ) ;
#26623=ORIENTED_EDGE ( 'NONE', *, *, #18006, .T. ) ;
#26624=DIRECTION ( 'NONE',  ( 1.000000000000000000, -0.000000000000000000, 0.000000000000000000 ) ) ;
#26625=DIRECTION ( 'NONE',  ( -0.000000000000000000, -1.000000000000000000, -0.000000000000000000 ) ) ;
#26640=CARTESIAN_POINT ( 'NONE',  ( 23.67249405129376072, 27.44083605074020937, 27.18966959687858775 ) ) ;
#26643=VECTOR ( 'NONE', #3773, 1000.000000000000000 ) ;
#26647=PLANE ( 'NONE',  #12887 ) ;
#26657=PRESENTATION_STYLE_ASSIGNMENT (( #4515 ) ) ;
#26661=ORIENTED_EDGE ( 'NONE', *, *, #51084, .T. ) ;
#26669=ORIENTED_EDGE ( 'NONE', *, *, #60219, .F. ) ;
#26672=( LENGTH_UNIT ( ) NAMED_UNIT ( * ) SI_UNIT ( .MILLI., .METRE. ) );
#26678=SURFACE_STYLE_USAGE ( .BOTH. , #69610 ) ;
#26693=EDGE_CURVE ( 'NONE', #9552, #33374, #20704, .T. ) ;
#26695=DIRECTION ( 'NONE',  ( -0.000000000000000000, 1.000000000000000000, -0.000000000000000000 ) ) ;
#26702=DIRECTION ( 'NONE',  ( 0.000000000000000000, 0.000000000000000000, -1.000000000000000000 ) ) ;
#26715=ORIENTED_EDGE ( 'NONE', *, *, #63830, .T. ) ;
#26729=CARTESIAN_POINT ( 'NONE',  ( 29.00000000000000000, 43.00000000000000000, -89.00000000000000000 ) ) ;
#26732=VERTEX_POINT ( 'NONE', #60046 ) ;
#26739=MECHANICAL_DESIGN_GEOMETRIC_PRESENTATION_REPRESENTATION('',(#866),#44789);
#26742=SURFACE_STYLE_USAGE ( .BOTH. , #1363 ) ;
#26751=SURFACE_STYLE_FILL_AREA ( #5647 ) ;
#26759=SURFACE_STYLE_USAGE ( .BOTH. , #42664 ) ;
#26772=CIRCLE ( 'NONE', #44811, 12.50000000000000178 ) ;
#26776=VECTOR ( 'NONE', #10276, 1000.000000000000000 ) ;
#26796=ORIENTED_EDGE ( 'NONE', *, *, #40763, .F. ) ;
#26815=AXIS2_PLACEMENT_3D ( 'NONE', #67537, #9160, #55939 ) ;
#26825=EDGE_CURVE ( 'NONE', #15954, #41524, #8352, .T. ) ;
#26839=EDGE_LOOP ( 'NONE', ( #14490, #64288, #44048, #47391 ) ) ;
#26841=CARTESIAN_POINT ( 'NONE',  ( 108.3664351561509278, 1.000000000000000000, 18.43563588791581509 ) ) ;
#26843=DIRECTION ( 'NONE',  ( 1.000000000000000000, -0.000000000000000000, -1.300977106640434891E-16 ) ) ;
#26845=CARTESIAN_POINT ( 'NONE',  ( 23.50000000000001776, 27.44010416289936316, -27.18999999999999417 ) ) ;
#26852=LINE ( 'NONE', #81, #61106 ) ;
#26855=SURFACE_STYLE_USAGE ( .BOTH. , #53959 ) ;
#26859=ORIENTED_EDGE ( 'NONE', *, *, #62333, .F. ) ;
#26861=VERTEX_POINT ( 'NONE', #35753 ) ;
#26873=AXIS2_PLACEMENT_3D ( 'NONE', #12091, #54992, #33895 ) ;
#26875=SURFACE_SIDE_STYLE ('',( #48075 ) ) ;
#26881=CARTESIAN_POINT ( 'NONE',  ( 26.00000000000001776, 42.00000000000000000, 34.49999999999999289 ) ) ;
#26885=( GEOMETRIC_REPRESENTATION_CONTEXT ( 3 ) GLOBAL_UNCERTAINTY_ASSIGNED_CONTEXT ( ( #941 ) ) GLOBAL_UNIT_ASSIGNED_CONTEXT ( ( #61585, #35591, #51416 ) ) REPRESENTATION_CONTEXT ( 'NONE', 'WORKASPACE' ) );
#26903=AXIS2_PLACEMENT_3D ( 'NONE', #46173, #20078, #47224 ) ;
#26907=( NAMED_UNIT ( * ) PLANE_ANGLE_UNIT ( ) SI_UNIT ( $, .RADIAN. ) );
#26911=ORIENTED_EDGE ( 'NONE', *, *, #31186, .F. ) ;
#26913=AXIS2_PLACEMENT_3D ( 'NONE', #9926, #32743, #32380 ) ;
#26919=ORIENTED_EDGE ( 'NONE', *, *, #44390, .F. ) ;
#26937=SURFACE_SIDE_STYLE ('',( #36549 ) ) ;
#26945=CARTESIAN_POINT ( 'NONE',  ( 57.00000000000000000, 16.00000000000000000, 60.00402776293825724 ) ) ;
#26947=CARTESIAN_POINT ( 'NONE',  ( 3.000000000000000000, 5.000000000000000000, -72.00402776293822171 ) ) ;
#26963=EDGE_CURVE ( 'NONE', #27344, #50401, #19525, .T. ) ;
#26974=SURFACE_SIDE_STYLE ('',( #37962 ) ) ;
#26985=CARTESIAN_POINT ( 'NONE',  ( 179.4361977533518484, 5.000000000000000000, 103.7004518695275550 ) ) ;
#26988=( GEOMETRIC_REPRESENTATION_CONTEXT ( 3 ) GLOBAL_UNCERTAINTY_ASSIGNED_CONTEXT ( ( #53094 ) ) GLOBAL_UNIT_ASSIGNED_CONTEXT ( ( #61105, #34027, #65691 ) ) REPRESENTATION_CONTEXT ( 'NONE', 'WORKASPACE' ) );
#26992=ORIENTED_EDGE ( 'NONE', *, *, #55340, .T. ) ;
#26993=ADVANCED_FACE ( 'NONE', ( #20960 ), #29730, .T. ) ;
#26996=( LENGTH_UNIT ( ) NAMED_UNIT ( * ) SI_UNIT ( .MILLI., .METRE. ) );
#27002=CARTESIAN_POINT ( 'NONE',  ( 0.000000000000000000, 13.00000000000000178, -36.49999999999999289 ) ) ;
#27004=VECTOR ( 'NONE', #17609, 1000.000000000000000 ) ;
#27007=EDGE_LOOP ( 'NONE', ( #55872, #22114, #4804, #7319, #5503, #37726, #66880 ) ) ;
#27013=DIRECTION ( 'NONE',  ( 0.000000000000000000, 0.000000000000000000, -1.000000000000000000 ) ) ;
#27016=COLOUR_RGB ( '', 0.31764706, 0.68627451, 0.89019608) ;
#27021=EDGE_CURVE ( 'NONE', #41519, #49984, #53295, .T. ) ;
#27022=CIRCLE ( 'NONE', #54011, 5.000000000000004441 ) ;
#27024=PRESENTATION_STYLE_ASSIGNMENT (( #5577 ) ) ;
#27027=ORIENTED_EDGE ( 'NONE', *, *, #26089, .F. ) ;
#27050=CARTESIAN_POINT ( 'NONE',  ( 1.000000000000000888, 13.00000000000000178, -60.00402776293827145 ) ) ;
#27053=EDGE_LOOP ( 'NONE', ( #43484, #59844, #62861, #64401 ) ) ;
#27057=DIRECTION ( 'NONE',  ( -0.000000000000000000, 1.000000000000000000, -0.000000000000000000 ) ) ;
#27070=( NAMED_UNIT ( * ) PLANE_ANGLE_UNIT ( ) SI_UNIT ( $, .RADIAN. ) );
#27089=CARTESIAN_POINT ( 'NONE',  ( 36.00000000000002842, 5.000000000000000000, 77.00402776293825013 ) ) ;
#27092=EDGE_CURVE ( 'NONE', #23198, #25944, #13150, .T. ) ;
#27093=( GEOMETRIC_REPRESENTATION_CONTEXT ( 3 ) GLOBAL_UNCERTAINTY_ASSIGNED_CONTEXT ( ( #68577 ) ) GLOBAL_UNIT_ASSIGNED_CONTEXT ( ( #15638, #26501, #5379 ) ) REPRESENTATION_CONTEXT ( 'NONE', 'WORKASPACE' ) );
#27096=( NAMED_UNIT ( * ) PLANE_ANGLE_UNIT ( ) SI_UNIT ( $, .RADIAN. ) );
#27120=UNCERTAINTY_MEASURE_WITH_UNIT (LENGTH_MEASURE( 1.000000000000000082E-05 ), #2942, 'distance_accuracy_value', 'NONE');
#27137=DIRECTION ( 'NONE',  ( 1.000000000000000000, 0.000000000000000000, 0.000000000000000000 ) ) ;
#27138=COLOUR_RGB ( '', 0.09019608, 0.27058824, 0.51372549) ;
#27148=CARTESIAN_POINT ( 'NONE',  ( 98.00000000000000000, 16.00000000000000000, 12.50000000000000178 ) ) ;
#27152=PRESENTATION_STYLE_ASSIGNMENT (( #53242 ) ) ;
#27153=FILL_AREA_STYLE_COLOUR ( '', #5496 ) ;
#27168=LINE ( 'NONE', #53921, #16755 ) ;
#27170=ORIENTED_EDGE ( 'NONE', *, *, #3127, .F. ) ;
#27175=FILL_AREA_STYLE_COLOUR ( '', #14625 ) ;
#27181=ORIENTED_EDGE ( 'NONE', *, *, #54064, .F. ) ;
#27190=UNCERTAINTY_MEASURE_WITH_UNIT (LENGTH_MEASURE( 1.000000000000000082E-05 ), #43620, 'distance_accuracy_value', 'NONE');
#27201=SURFACE_STYLE_USAGE ( .BOTH. , #17056 ) ;
#27210=AXIS2_PLACEMENT_3D ( 'NONE', #441, #39207, #16374 ) ;
#27216=CARTESIAN_POINT ( 'NONE',  ( 23.50000000000001776, 13.99999999999999822, 26.18999999999999417 ) ) ;
#27218=FILL_AREA_STYLE_COLOUR ( '', #62556 ) ;
#27235=DIRECTION ( 'NONE',  ( 0.000000000000000000, 0.000000000000000000, -1.000000000000000000 ) ) ;
#27240=VERTEX_POINT ( 'NONE', #68991 ) ;
#27251=COLOUR_RGB ( '', 0.08235294, 0.09019608, 0.10196078) ;
#27256=CARTESIAN_POINT ( 'NONE',  ( 10.00000000000001954, 43.00000000000000000, -28.38386403503541899 ) ) ;
#27260=DIRECTION ( 'NONE',  ( 0.000000000000000000, 0.000000000000000000, -1.000000000000000000 ) ) ;
#27262=ORIENTED_EDGE ( 'NONE', *, *, #7684, .F. ) ;
#27280=CARTESIAN_POINT ( 'NONE',  ( 16.00000000000001776, 14.00000000000000000, -29.68999999999999417 ) ) ;
#27284=CIRCLE ( 'NONE', #54275, 4.999999999999997335 ) ;
#27290=SURFACE_SIDE_STYLE ('',( #524 ) ) ;
#27291=EDGE_CURVE ( 'NONE', #15615, #49912, #36506, .T. ) ;
#27293=SURFACE_STYLE_USAGE ( .BOTH. , #58992 ) ;
#27294=ADVANCED_FACE ( 'NONE', ( #62635 ), #9567, .F. ) ;
#27300=CARTESIAN_POINT ( 'NONE',  ( 8.000000000000030198, 0.000000000000000000, -29.00402776293826079 ) ) ;
#27304=SURFACE_SIDE_STYLE ('',( #11144 ) ) ;
#27316=COLOUR_RGB ( '', 0.72549020, 0.75294118, 0.79215686) ;
#27324=EDGE_LOOP ( 'NONE', ( #32861, #55062, #42440, #8757 ) ) ;
#27332=CARTESIAN_POINT ( 'NONE',  ( 1.000000000000000000, 14.00000000000000000, 79.00402776293826435 ) ) ;
#27341=FILL_AREA_STYLE ('',( #54437 ) ) ;
#27343=VECTOR ( 'NONE', #60670, 1000.000000000000000 ) ;
#27344=VERTEX_POINT ( 'NONE', #53818 ) ;
#27346=STYLED_ITEM ( 'NONE', ( #58999 ), #62726 ) ;
#27358=FILL_AREA_STYLE_COLOUR ( '', #22880 ) ;
#27365=VERTEX_POINT ( 'NONE', #69659 ) ;
#27368=ORIENTED_EDGE ( 'NONE', *, *, #22553, .F. ) ;
#27372=( NAMED_UNIT ( * ) PLANE_ANGLE_UNIT ( ) SI_UNIT ( $, .RADIAN. ) );
#27374=ADVANCED_FACE ( 'NONE', ( #28100 ), #59427, .F. ) ;
#27383=FILL_AREA_STYLE ('',( #22834 ) ) ;
#27384=SURFACE_STYLE_USAGE ( .BOTH. , #64708 ) ;
#27394=AXIS2_PLACEMENT_3D ( 'NONE', #67910, #19702, #68595 ) ;
#27407=CYLINDRICAL_SURFACE ( 'NONE', #41314, 1.000000000000000000 ) ;
#27409=ORIENTED_EDGE ( 'NONE', *, *, #31369, .T. ) ;
#27411=LINE ( 'NONE', #33070, #39695 ) ;
#27417=DIRECTION ( 'NONE',  ( -1.000000000000000000, 0.000000000000000000, -1.982541115402069054E-16 ) ) ;
#27420=AXIS2_PLACEMENT_3D ( 'NONE', #20012, #62924, #14770 ) ;
#27424=CARTESIAN_POINT ( 'NONE',  ( 30.99999999999999289, 5.000000000000000000, 24.00402776293822171 ) ) ;
#27428=COLOUR_RGB ( '', 0.66274510, 0.83137255, 0.94901961) ;
#27431=ORIENTED_EDGE ( 'NONE', *, *, #766, .F. ) ;
#27437=DIRECTION ( 'NONE',  ( -0.000000000000000000, 0.9984713486292863260, 0.05527174654752588928 ) ) ;
#27440=ORIENTED_EDGE ( 'NONE', *, *, #37876, .F. ) ;
#27459=AXIS2_PLACEMENT_3D ( 'NONE', #51360, #57320, #29901 ) ;
#27460=MECHANICAL_DESIGN_GEOMETRIC_PRESENTATION_REPRESENTATION('',(#65639),#36520);
#27473=VECTOR ( 'NONE', #13929, 1000.000000000000000 ) ;
#27474=( NAMED_UNIT ( * ) PLANE_ANGLE_UNIT ( ) SI_UNIT ( $, .RADIAN. ) );
#27475=EDGE_CURVE ( 'NONE', #46401, #37912, #60096, .T. ) ;
#27483=ORIENTED_EDGE ( 'NONE', *, *, #2299, .T. ) ;
#27488=STYLED_ITEM ( 'NONE', ( #27676 ), #31854 ) ;
#27504=SURFACE_STYLE_FILL_AREA ( #32118 ) ;
#27505=COLOUR_RGB ( '', 0.08235294, 0.09019608, 0.10196078) ;
#27511=CARTESIAN_POINT ( 'NONE',  ( 32.00000000000001421, 15.00000000000000000, 35.49999999999999289 ) ) ;
#27520=EDGE_LOOP ( 'NONE', ( #10643, #69656, #9758, #13894, #46883, #1950, #26992, #18585, #52457, #64930, #17540, #31242, #45606, #65725, #30782, #42044 ) ) ;
#27526=STYLED_ITEM ( 'NONE', ( #6705 ), #56868 ) ;
#27529=ADVANCED_FACE ( 'NONE', ( #9819 ), #30536, .T. ) ;
#27531=( LENGTH_UNIT ( ) NAMED_UNIT ( * ) SI_UNIT ( .MILLI., .METRE. ) );
#27534=DIRECTION ( 'NONE',  ( 0.000000000000000000, 0.000000000000000000, 1.000000000000000000 ) ) ;
#27535=ORIENTED_EDGE ( 'NONE', *, *, #42040, .F. ) ;
#27537=EDGE_CURVE ( 'NONE', #11058, #50024, #47822, .T. ) ;
#27538=ORIENTED_EDGE ( 'NONE', *, *, #5693, .T. ) ;
#27552=DIRECTION ( 'NONE',  ( -0.000000000000000000, -1.000000000000000000, -0.000000000000000000 ) ) ;
#27558=SURFACE_STYLE_FILL_AREA ( #6125 ) ;
#27562=CARTESIAN_POINT ( 'NONE',  ( 12.00000000000001776, 15.00000000000000000, 29.68999999999999417 ) ) ;
#27564=ORIENTED_EDGE ( 'NONE', *, *, #41997, .T. ) ;
#27584=CARTESIAN_POINT ( 'NONE',  ( 22.00000000000000711, 50.00000000000000000, -46.00000000000000000 ) ) ;
#27585=FACE_BOUND ( 'NONE', #55621, .T. ) ;
#27589=CARTESIAN_POINT ( 'NONE',  ( 28.00000000000000000, 34.36176364315827669, -80.00402776293830698 ) ) ;
#27595=FILL_AREA_STYLE ('',( #49783 ) ) ;
#27603=EDGE_CURVE ( 'NONE', #10014, #41012, #54276, .T. ) ;
#27604=AXIS2_PLACEMENT_3D ( 'NONE', #3211, #8560, #56375 ) ;
#27615=ORIENTED_EDGE ( 'NONE', *, *, #39881, .F. ) ;
#27618=CIRCLE ( 'NONE', #5135, 1.000000000000000888 ) ;
#27628=( LENGTH_UNIT ( ) NAMED_UNIT ( * ) SI_UNIT ( .MILLI., .METRE. ) );
#27632=PRESENTATION_STYLE_ASSIGNMENT (( #65287 ) ) ;
#27633=DIRECTION ( 'NONE',  ( -8.391040747885011388E-17, 0.7641995406119433953, -0.6449798928094538919 ) ) ;
#27635=EDGE_LOOP ( 'NONE', ( #61142, #6849, #46933, #46743 ) ) ;
#27639=ORIENTED_EDGE ( 'NONE', *, *, #41110, .F. ) ;
#27641=FILL_AREA_STYLE_COLOUR ( '', #8969 ) ;
#27646=CARTESIAN_POINT ( 'NONE',  ( 8.000000000000030198, 5.000000000000000000, -29.00402776293826079 ) ) ;
#27652=CARTESIAN_POINT ( 'NONE',  ( 22.99999999999995381, 5.000000000000000000, 32.00402776293825724 ) ) ;
#27653=FILL_AREA_STYLE_COLOUR ( '', #30778 ) ;
#27673=CARTESIAN_POINT ( 'NONE',  ( 24.35070397832969391, 24.94665475208109839, 27.33851719159103766 ) ) ;
#27676=PRESENTATION_STYLE_ASSIGNMENT (( #6251 ) ) ;
#27688=EDGE_CURVE ( 'NONE', #21029, #33110, #488, .T. ) ;
#27702=PRESENTATION_STYLE_ASSIGNMENT (( #43285 ) ) ;
#27703=VERTEX_POINT ( 'NONE', #37072 ) ;
#27705=ORIENTED_EDGE ( 'NONE', *, *, #59422, .F. ) ;
#27710=ORIENTED_EDGE ( 'NONE', *, *, #33451, .F. ) ;
#27722=CARTESIAN_POINT ( 'NONE',  ( 22.99999999999999289, 5.000000000000000000, -37.00402776293825013 ) ) ;
#27723=( NAMED_UNIT ( * ) PLANE_ANGLE_UNIT ( ) SI_UNIT ( $, .RADIAN. ) );
#27727=DIRECTION ( 'NONE',  ( 0.000000000000000000, 0.000000000000000000, 1.000000000000000000 ) ) ;
#27737=ORIENTED_EDGE ( 'NONE', *, *, #9661, .F. ) ;
#27741=DIRECTION ( 'NONE',  ( -0.000000000000000000, -1.000000000000000000, -0.000000000000000000 ) ) ;
#27745=DIRECTION ( 'NONE',  ( 1.982541115402069054E-16, 0.000000000000000000, -1.000000000000000000 ) ) ;
#27752=SURFACE_STYLE_USAGE ( .BOTH. , #1694 ) ;
#27768=FILL_AREA_STYLE ('',( #65786 ) ) ;
#27801=CARTESIAN_POINT ( 'NONE',  ( 31.00000000000001421, 15.00000000000000000, 36.49999999999999289 ) ) ;
#27807=CARTESIAN_POINT ( 'NONE',  ( 57.00000000000000000, 16.00000000000000000, -60.00402776293825724 ) ) ;
#27809=DIRECTION ( 'NONE',  ( 1.000000000000000000, 0.000000000000000000, 0.000000000000000000 ) ) ;
#27828=EDGE_LOOP ( 'NONE', ( #9801, #49381, #53334, #20110 ) ) ;
#27829=DIRECTION ( 'NONE',  ( 0.000000000000000000, 1.000000000000000000, 0.000000000000000000 ) ) ;
#27836=( NAMED_UNIT ( * ) PLANE_ANGLE_UNIT ( ) SI_UNIT ( $, .RADIAN. ) );
#27843=COLOUR_RGB ( '', 0.40784314, 0.44705882, 0.49803922) ;
#27852=EDGE_CURVE ( 'NONE', #31434, #19928, #39484, .T. ) ;
#27853=DIRECTION ( 'NONE',  ( -0.000000000000000000, -1.000000000000000000, -0.000000000000000000 ) ) ;
#27867=( NAMED_UNIT ( * ) PLANE_ANGLE_UNIT ( ) SI_UNIT ( $, .RADIAN. ) );
#27873=VECTOR ( 'NONE', #37596, 1000.000000000000000 ) ;
#27875=ORIENTED_EDGE ( 'NONE', *, *, #32189, .T. ) ;
#27884=LINE ( 'NONE', #37842, #11938 ) ;
#27896=EDGE_LOOP ( 'NONE', ( #48532, #7672, #18843, #60961 ) ) ;
#27897=DIRECTION ( 'NONE',  ( -0.000000000000000000, -1.000000000000000000, -0.000000000000000000 ) ) ;
#27914=( NAMED_UNIT ( * ) PLANE_ANGLE_UNIT ( ) SI_UNIT ( $, .RADIAN. ) );
#27915=( LENGTH_UNIT ( ) NAMED_UNIT ( * ) SI_UNIT ( .MILLI., .METRE. ) );
#27936=PRESENTATION_STYLE_ASSIGNMENT (( #17781 ) ) ;
#27946=FILL_AREA_STYLE_COLOUR ( '', #48392 ) ;
#27950=DIRECTION ( 'NONE',  ( 0.000000000000000000, 0.000000000000000000, -1.000000000000000000 ) ) ;
#27952=ORIENTED_EDGE ( 'NONE', *, *, #62802, .T. ) ;
#27959=FILL_AREA_STYLE_COLOUR ( '', #34211 ) ;
#27961=CIRCLE ( 'NONE', #54937, 1.000000000000000888 ) ;
#27979=SURFACE_STYLE_USAGE ( .BOTH. , #27290 ) ;
#27981=PRESENTATION_STYLE_ASSIGNMENT (( #50182 ) ) ;
#27984=PRESENTATION_STYLE_ASSIGNMENT (( #49492 ) ) ;
#27985=ORIENTED_EDGE ( 'NONE', *, *, #56285, .T. ) ;
#27986=CARTESIAN_POINT ( 'NONE',  ( 27.00000000000001776, 14.00000000000000000, -34.49999999999999289 ) ) ;
#27991=MECHANICAL_DESIGN_GEOMETRIC_PRESENTATION_REPRESENTATION('',(#56091),#61692);
#28003=SURFACE_STYLE_FILL_AREA ( #39319 ) ;
#28013=CARTESIAN_POINT ( 'NONE',  ( 0.4142135623730951455, 42.99999999999999289, 35.50000000000000000 ) ) ;
#28019=LINE ( 'NONE', #6574, #3886 ) ;
#28020=AXIS2_PLACEMENT_3D ( 'NONE', #24583, #13009, #2395 ) ;
#28022=AXIS2_PLACEMENT_3D ( 'NONE', #59458, #53519, #53185 ) ;
#28023=PRESENTATION_STYLE_ASSIGNMENT (( #48872 ) ) ;
#28031=CARTESIAN_POINT ( 'NONE',  ( 0.000000000000000000, 42.00000000000000000, 79.00402776293826435 ) ) ;
#28037=STYLED_ITEM ( 'NONE', ( #48947 ), #69042 ) ;
#28058=CYLINDRICAL_SURFACE ( 'NONE', #2875, 5.000000000000004441 ) ;
#28062=EDGE_CURVE ( 'NONE', #2941, #23178, #4205, .T. ) ;
#28075=CARTESIAN_POINT ( 'NONE',  ( -2.376974287405969816E-15, 13.58578643762690419, 35.91421356237309226 ) ) ;
#28081=CARTESIAN_POINT ( 'NONE',  ( 22.99999999999996092, 5.000000000000000000, -77.00402776293825013 ) ) ;
#28090=STYLED_ITEM ( 'NONE', ( #13689 ), #15583 ) ;
#28097=( LENGTH_UNIT ( ) NAMED_UNIT ( * ) SI_UNIT ( .MILLI., .METRE. ) );
#28100=FACE_OUTER_BOUND ( 'NONE', #56225, .T. ) ;
#28101=COLOUR_RGB ( '', 0.66274510, 0.83137255, 0.94901961) ;
#28120=ORIENTED_EDGE ( 'NONE', *, *, #18413, .T. ) ;
#28121=TOROIDAL_SURFACE ( 'NONE', #18070, 2.000000000000000000, 1.000000000000000000 ) ;
#28129=ORIENTED_EDGE ( 'NONE', *, *, #40438, .T. ) ;
#28133=ORIENTED_EDGE ( 'NONE', *, *, #34159, .F. ) ;
#28138=PRODUCT_DEFINITION_FORMATION_WITH_SPECIFIED_SOURCE ( 'ANY', '', #25974, .NOT_KNOWN. ) ;
#28145=DIRECTION ( 'NONE',  ( -0.000000000000000000, 1.000000000000000000, -0.000000000000000000 ) ) ;
#28156=FILL_AREA_STYLE_COLOUR ( '', #11545 ) ;
#28157=EDGE_CURVE ( 'NONE', #17912, #65192, #11941, .T. ) ;
#28160=DIRECTION ( 'NONE',  ( 1.000000000000000000, 0.000000000000000000, 0.000000000000000000 ) ) ;
#28170=CARTESIAN_POINT ( 'NONE',  ( 57.00000000000000000, 16.00000000000000000, 60.00402776293825724 ) ) ;
#28171=AXIS2_PLACEMENT_3D ( 'NONE', #13713, #35170, #56631 ) ;
#28173=COLOUR_RGB ( '', 0.08235294, 0.09019608, 0.10196078) ;
#28182=CARTESIAN_POINT ( 'NONE',  ( 8.000000000000000000, 5.000000000000000000, 72.00402776293825013 ) ) ;
#28185=SURFACE_STYLE_FILL_AREA ( #60240 ) ;
#28188=CARTESIAN_POINT ( 'NONE',  ( 1.709458476932651091E-14, 14.00000000000000533, -35.50000000000000000 ) ) ;
#28197=FILL_AREA_STYLE ('',( #43766 ) ) ;
#28201=FACE_OUTER_BOUND ( 'NONE', #1420, .T. ) ;
#28202=FILL_AREA_STYLE ('',( #27175 ) ) ;
#28206=( NAMED_UNIT ( * ) SI_UNIT ( $, .STERADIAN. ) SOLID_ANGLE_UNIT ( ) );
#28213=DIRECTION ( 'NONE',  ( -6.938893903907221278E-15, 0.000000000000000000, -1.000000000000000000 ) ) ;
#28223=SURFACE_STYLE_FILL_AREA ( #1107 ) ;
#28224=EDGE_CURVE ( 'NONE', #44696, #51304, #47992, .T. ) ;
#28228=DIRECTION ( 'NONE',  ( -0.000000000000000000, -0.000000000000000000, -1.000000000000000000 ) ) ;
#28231=CARTESIAN_POINT ( 'NONE',  ( 36.00000000000002132, 5.000000000000000000, -77.00402776293825013 ) ) ;
#28235=CIRCLE ( 'NONE', #60848, 1.000000000000000888 ) ;
#28238=DIRECTION ( 'NONE',  ( 0.000000000000000000, 1.000000000000000000, 0.000000000000000000 ) ) ;
#28252=CARTESIAN_POINT ( 'NONE',  ( 29.00000000000000000, 38.93969262078592664, -89.65797985667437331 ) ) ;
#28258=CARTESIAN_POINT ( 'NONE',  ( 179.4361977533490347, 0.9999999999999991118, 103.7004518695263044 ) ) ;
#28260=LINE ( 'NONE', #29324, #52698 ) ;
#28268=DIRECTION ( 'NONE',  ( 0.000000000000000000, -0.7431448254773944662, -0.6691306063588580155 ) ) ;
#28278=UNCERTAINTY_MEASURE_WITH_UNIT (LENGTH_MEASURE( 1.000000000000000082E-05 ), #61316, 'distance_accuracy_value', 'NONE');
#28297=( LENGTH_UNIT ( ) NAMED_UNIT ( * ) SI_UNIT ( .MILLI., .METRE. ) );
#28300=( NAMED_UNIT ( * ) PLANE_ANGLE_UNIT ( ) SI_UNIT ( $, .RADIAN. ) );
#28312=EDGE_CURVE ( 'NONE', #17287, #15954, #14351, .T. ) ;
#28313=DIRECTION ( 'NONE',  ( 1.000000000000000000, 0.000000000000000000, 0.000000000000000000 ) ) ;
#28314=ORIENTED_EDGE ( 'NONE', *, *, #9390, .T. ) ;
#28322=AXIS2_PLACEMENT_3D ( 'NONE', #59387, #55519, #48909 ) ;
#28334=CARTESIAN_POINT ( 'NONE',  ( 31.00000000000001066, 42.00000000000000000, -4.033029030585349936E-15 ) ) ;
#28336=DIRECTION ( 'NONE',  ( 0.000000000000000000, 0.000000000000000000, -1.000000000000000000 ) ) ;
#28339=LINE ( 'NONE', #182, #41225 ) ;
#28347=VERTEX_POINT ( 'NONE', #57264 ) ;
#28355=AXIS2_PLACEMENT_3D ( 'NONE', #60792, #49588, #65037 ) ;
#28364=CARTESIAN_POINT ( 'NONE',  ( 27.99999999999999645, 5.000000000000000000, -24.00402776293821816 ) ) ;
#28372=UNCERTAINTY_MEASURE_WITH_UNIT (LENGTH_MEASURE( 1.000000000000000082E-05 ), #52259, 'distance_accuracy_value', 'NONE');
#28375=VERTEX_POINT ( 'NONE', #15092 ) ;
#28378=STYLED_ITEM ( 'NONE', ( #48414 ), #19538 ) ;
#28384=FILL_AREA_STYLE_COLOUR ( '', #3457 ) ;
#28386=EDGE_CURVE ( 'NONE', #20026, #47636, #14018, .T. ) ;
#28389=SURFACE_STYLE_USAGE ( .BOTH. , #28752 ) ;
#28393=DIRECTION ( 'NONE',  ( 0.000000000000000000, 1.000000000000000000, 0.000000000000000000 ) ) ;
#28396=FACE_OUTER_BOUND ( 'NONE', #58984, .T. ) ;
#28398=EDGE_LOOP ( 'NONE', ( #6614, #15942, #57142, #23803 ) ) ;
#28411=DIRECTION ( 'NONE',  ( 0.000000000000000000, 0.000000000000000000, 1.000000000000000000 ) ) ;
#28416=EDGE_LOOP ( 'NONE', ( #62960, #57114, #7015, #32192 ) ) ;
#28422=MECHANICAL_DESIGN_GEOMETRIC_PRESENTATION_REPRESENTATION('',(#10494),#54303);
#28424=CARTESIAN_POINT ( 'NONE',  ( 31.00000000000002132, 42.00000000000000000, 79.00402776293823592 ) ) ;
#28426=STYLED_ITEM ( 'NONE', ( #49576 ), #55468 ) ;
#28431=EDGE_LOOP ( 'NONE', ( #18895, #3289, #35546, #53188 ) ) ;
#28434=VECTOR ( 'NONE', #6683, 1000.000000000000000 ) ;
#28441=EDGE_CURVE ( 'NONE', #8059, #9217, #47825, .T. ) ;
#28445=CARTESIAN_POINT ( 'NONE',  ( 10.00000000000002309, 60.69879356856722552, 69.02971849933236115 ) ) ;
#28447=CARTESIAN_POINT ( 'NONE',  ( 0.000000000000000000, 43.00000000000000000, 0.000000000000000000 ) ) ;
#28448=PRESENTATION_STYLE_ASSIGNMENT (( #33746 ) ) ;
#28456=SURFACE_STYLE_USAGE ( .BOTH. , #1704 ) ;
#28464=CARTESIAN_POINT ( 'NONE',  ( -3.692675730757587168E-15, 42.00000000000000000, -28.38386403503541899 ) ) ;
#28478=DIRECTION ( 'NONE',  ( 0.000000000000000000, 0.000000000000000000, -1.000000000000000000 ) ) ;
#28487=ORIENTED_EDGE ( 'NONE', *, *, #26195, .F. ) ;
#28492=CARTESIAN_POINT ( 'NONE',  ( 10.00000000000001776, 42.74314482547740113, -27.71473342867655987 ) ) ;
#28493=ORIENTED_EDGE ( 'NONE', *, *, #19194, .T. ) ;
#28495=EDGE_CURVE ( 'NONE', #26861, #65035, #12102, .T. ) ;
#28498=CARTESIAN_POINT ( 'NONE',  ( 25.00000000000001421, 43.00000000000000000, 29.68999999999999417 ) ) ;
#28503=SURFACE_SIDE_STYLE ('',( #66510 ) ) ;
#28505=EDGE_CURVE ( 'NONE', #60023, #50403, #53394, .T. ) ;
#28511=UNCERTAINTY_MEASURE_WITH_UNIT (LENGTH_MEASURE( 1.000000000000000082E-05 ), #38764, 'distance_accuracy_value', 'NONE');
#28514=STYLED_ITEM ( 'NONE', ( #65315 ), #62816 ) ;
#28519=EDGE_LOOP ( 'NONE', ( #52294, #50573, #12700, #7650 ) ) ;
#28531=VERTEX_POINT ( 'NONE', #4468 ) ;
#28537=FILL_AREA_STYLE ('',( #2095 ) ) ;
#28542=CYLINDRICAL_SURFACE ( 'NONE', #63839, 4.999999999999997335 ) ;
#28544=ORIENTED_EDGE ( 'NONE', *, *, #19773, .F. ) ;
#28560=SURFACE_STYLE_USAGE ( .BOTH. , #7131 ) ;
#28566=CARTESIAN_POINT ( 'NONE',  ( 31.00000000000000711, 15.00000000000000000, -34.49999999999999289 ) ) ;
#28567=( NAMED_UNIT ( * ) PLANE_ANGLE_UNIT ( ) SI_UNIT ( $, .RADIAN. ) );
#28571=ORIENTED_EDGE ( 'NONE', *, *, #27852, .T. ) ;
#28575=ORIENTED_EDGE ( 'NONE', *, *, #8766, .F. ) ;
#28577=SURFACE_SIDE_STYLE ('',( #17035 ) ) ;
#28584=SURFACE_SIDE_STYLE ('',( #38859 ) ) ;
#28591=UNCERTAINTY_MEASURE_WITH_UNIT (LENGTH_MEASURE( 1.000000000000000082E-05 ), #22298, 'distance_accuracy_value', 'NONE');
#28598=( NAMED_UNIT ( * ) SI_UNIT ( $, .STERADIAN. ) SOLID_ANGLE_UNIT ( ) );
#28600=ORIENTED_EDGE ( 'NONE', *, *, #65212, .F. ) ;
#28602=( GEOMETRIC_REPRESENTATION_CONTEXT ( 3 ) GLOBAL_UNCERTAINTY_ASSIGNED_CONTEXT ( ( #3206 ) ) GLOBAL_UNIT_ASSIGNED_CONTEXT ( ( #54167, #65059, #6324 ) ) REPRESENTATION_CONTEXT ( 'NONE', 'WORKASPACE' ) );
#28607=ORIENTED_EDGE ( 'NONE', *, *, #55188, .T. ) ;
#28620=STYLED_ITEM ( 'NONE', ( #13623 ), #5852 ) ;
#28632=SURFACE_STYLE_FILL_AREA ( #12451 ) ;
#28640=EDGE_LOOP ( 'NONE', ( #4536, #1649, #48968, #4882 ) ) ;
#28643=LINE ( 'NONE', #8603, #17081 ) ;
#28644=( GEOMETRIC_REPRESENTATION_CONTEXT ( 3 ) GLOBAL_UNCERTAINTY_ASSIGNED_CONTEXT ( ( #3941 ) ) GLOBAL_UNIT_ASSIGNED_CONTEXT ( ( #17192, #38663, #18553 ) ) REPRESENTATION_CONTEXT ( 'NONE', 'WORKASPACE' ) );
#28646=SURFACE_SIDE_STYLE ('',( #38577 ) ) ;
#28654=( LENGTH_UNIT ( ) NAMED_UNIT ( * ) SI_UNIT ( .MILLI., .METRE. ) );
#28658=FILL_AREA_STYLE ('',( #17462 ) ) ;
#28661=FILL_AREA_STYLE_COLOUR ( '', #55151 ) ;
#28674=SURFACE_STYLE_FILL_AREA ( #17475 ) ;
#28677=DIRECTION ( 'NONE',  ( -1.000000000000000000, 0.000000000000000000, 0.000000000000000000 ) ) ;
#28686=FILL_AREA_STYLE ('',( #44243 ) ) ;
#28688=ORIENTED_EDGE ( 'NONE', *, *, #60809, .T. ) ;
#28693=DIRECTION ( 'NONE',  ( 1.300977106640434891E-16, -0.000000000000000000, 1.000000000000000000 ) ) ;
#28695=( NAMED_UNIT ( * ) PLANE_ANGLE_UNIT ( ) SI_UNIT ( $, .RADIAN. ) );
#28706=EDGE_LOOP ( 'NONE', ( #5193, #63478, #45032, #42707 ) ) ;
#28722=LINE ( 'NONE', #6243, #13236 ) ;
#28724=LINE ( 'NONE', #39329, #19126 ) ;
#28725=DIRECTION ( 'NONE',  ( 0.000000000000000000, 0.000000000000000000, 1.000000000000000000 ) ) ;
#28726=EDGE_CURVE ( 'NONE', #23486, #18241, #7194, .T. ) ;
#28734=FILL_AREA_STYLE_COLOUR ( '', #3443 ) ;
#28736=DIRECTION ( 'NONE',  ( -0.000000000000000000, -1.000000000000000000, 0.000000000000000000 ) ) ;
#28747=AXIS2_PLACEMENT_3D ( 'NONE', #44186, #23365, #65585 ) ;
#28748=ADVANCED_FACE ( 'NONE', ( #40967 ), #15277, .T. ) ;
#28751=FACE_OUTER_BOUND ( 'NONE', #47605, .T. ) ;
#28752=SURFACE_SIDE_STYLE ('',( #24177 ) ) ;
#28764=CARTESIAN_POINT ( 'NONE',  ( 29.00000000000000000, 34.36176364315826248, -80.00402776293826435 ) ) ;
#28766=ORIENTED_EDGE ( 'NONE', *, *, #45899, .F. ) ;
#28779=FACE_OUTER_BOUND ( 'NONE', #62603, .T. ) ;
#28789=ORIENTED_EDGE ( 'NONE', *, *, #871, .T. ) ;
#28790=ADVANCED_FACE ( 'NONE', ( #42024 ), #25779, .F. ) ;
#28797=CARTESIAN_POINT ( 'NONE',  ( 1.000000000000000000, 0.9999999999999991118, -79.00402776293826435 ) ) ;
#28803=( NAMED_UNIT ( * ) SI_UNIT ( $, .STERADIAN. ) SOLID_ANGLE_UNIT ( ) );
#28818=MECHANICAL_DESIGN_GEOMETRIC_PRESENTATION_REPRESENTATION('',(#35584),#56900);
#28824=FACE_OUTER_BOUND ( 'NONE', #66688, .T. ) ;
#28830=AXIS2_PLACEMENT_3D ( 'NONE', #56462, #28677, #34325 ) ;
#28864=ORIENTED_EDGE ( 'NONE', *, *, #31773, .T. ) ;
#28887=FILL_AREA_STYLE ('',( #18008 ) ) ;
#28891=EDGE_CURVE ( 'NONE', #62580, #5418, #62310, .T. ) ;
#28895=DIRECTION ( 'NONE',  ( -0.000000000000000000, -0.000000000000000000, 1.000000000000000000 ) ) ;
#28911=CARTESIAN_POINT ( 'NONE',  ( -4.167402100491157668E-16, 42.24290439781417916, 74.85424052902104108 ) ) ;
#28914=CARTESIAN_POINT ( 'NONE',  ( 4.000000000000030198, 38.70020753820971748, 89.00000000000000000 ) ) ;
#28930=FILL_AREA_STYLE ('',( #2143 ) ) ;
#28937=CARTESIAN_POINT ( 'NONE',  ( 6.330869393641158638, 43.00000000000000000, 28.38386403503541899 ) ) ;
#28946=CIRCLE ( 'NONE', #7626, 1.000000000000000888 ) ;
#28961=FILL_AREA_STYLE_COLOUR ( '', #68457 ) ;
#28962=VECTOR ( 'NONE', #61272, 1000.000000000000000 ) ;
#28965=FILL_AREA_STYLE_COLOUR ( '', #56087 ) ;
#28979=( NAMED_UNIT ( * ) PLANE_ANGLE_UNIT ( ) SI_UNIT ( $, .RADIAN. ) );
#28980=EDGE_CURVE ( 'NONE', #21181, #34757, #57592, .T. ) ;
#28983=SURFACE_STYLE_USAGE ( .BOTH. , #28646 ) ;
#28985=( NAMED_UNIT ( * ) SI_UNIT ( $, .STERADIAN. ) SOLID_ANGLE_UNIT ( ) );
#28998=SURFACE_STYLE_FILL_AREA ( #50158 ) ;
#29004=STYLED_ITEM ( 'NONE', ( #15632 ), #14500 ) ;
#29011=CARTESIAN_POINT ( 'NONE',  ( 3.000000000000030198, 38.93969262078591242, 89.65797985667433068 ) ) ;
#29018=FILL_AREA_STYLE ('',( #14613 ) ) ;
#29022=CIRCLE ( 'NONE', #9994, 5.000000000000000888 ) ;
#29028=PRESENTATION_STYLE_ASSIGNMENT (( #45282 ) ) ;
#29041=CARTESIAN_POINT ( 'NONE',  ( 0.3542424171060651328, 42.77450929379338618, 45.47201693779177134 ) ) ;
#29044=DIRECTION ( 'NONE',  ( 0.000000000000000000, 0.000000000000000000, -1.000000000000000000 ) ) ;
#29049=LINE ( 'NONE', #49860, #12246 ) ;
#29054=( GEOMETRIC_REPRESENTATION_CONTEXT ( 3 ) GLOBAL_UNCERTAINTY_ASSIGNED_CONTEXT ( ( #12881 ) ) GLOBAL_UNIT_ASSIGNED_CONTEXT ( ( #51486, #51853, #15283 ) ) REPRESENTATION_CONTEXT ( 'NONE', 'WORKASPACE' ) );
#29060=( GEOMETRIC_REPRESENTATION_CONTEXT ( 3 ) GLOBAL_UNCERTAINTY_ASSIGNED_CONTEXT ( ( #34704 ) ) GLOBAL_UNIT_ASSIGNED_CONTEXT ( ( #46340, #15011, #19900 ) ) REPRESENTATION_CONTEXT ( 'NONE', 'WORKASPACE' ) );
#29067=AXIS2_PLACEMENT_3D ( 'NONE', #39595, #56074, #55389 ) ;
#29077=STYLED_ITEM ( 'NONE', ( #40645 ), #33588 ) ;
#29078=ADVANCED_FACE ( 'NONE', ( #31312 ), #30265, .T. ) ;
#29082=ORIENTED_EDGE ( 'NONE', *, *, #56199, .T. ) ;
#29109=FILL_AREA_STYLE ('',( #44678 ) ) ;
#29115=COLOUR_RGB ( '', 0.09019608, 0.27058824, 0.51372549) ;
#29116=SURFACE_STYLE_USAGE ( .BOTH. , #7680 ) ;
#29120=CARTESIAN_POINT ( 'NONE',  ( 10.00000000000000178, 60.69879356856722552, -69.02971849933236115 ) ) ;
#29122=CARTESIAN_POINT ( 'NONE',  ( 22.00000000000000711, 50.00000000000000000, -60.00000000000000711 ) ) ;
#29131=DIRECTION ( 'NONE',  ( 0.000000000000000000, 0.000000000000000000, 1.000000000000000000 ) ) ;
#29138=SURFACE_STYLE_FILL_AREA ( #7699 ) ;
#29142=STYLED_ITEM ( 'NONE', ( #5735 ), #9473 ) ;
#29149=FACE_OUTER_BOUND ( 'NONE', #32955, .T. ) ;
#29150=CARTESIAN_POINT ( 'NONE',  ( 0.000000000000000000, 42.00000000000000000, -79.00402776293826435 ) ) ;
#29154=PRESENTATION_STYLE_ASSIGNMENT (( #39774 ) ) ;
#29165=CARTESIAN_POINT ( 'NONE',  ( 57.00000000000000000, 13.00000000000000178, 80.00402776293826435 ) ) ;
#29168=VERTEX_POINT ( 'NONE', #21119 ) ;
#29171=( GEOMETRIC_REPRESENTATION_CONTEXT ( 3 ) GLOBAL_UNCERTAINTY_ASSIGNED_CONTEXT ( ( #29875 ) ) GLOBAL_UNIT_ASSIGNED_CONTEXT ( ( #10568, #5259, #60794 ) ) REPRESENTATION_CONTEXT ( 'NONE', 'WORKASPACE' ) );
#29182=EDGE_LOOP ( 'NONE', ( #58550, #37735, #10717 ) ) ;
#29188=( NAMED_UNIT ( * ) SI_UNIT ( $, .STERADIAN. ) SOLID_ANGLE_UNIT ( ) );
#29189=MECHANICAL_DESIGN_GEOMETRIC_PRESENTATION_REPRESENTATION('',(#53908),#44967);
#29191=CARTESIAN_POINT ( 'NONE',  ( 35.99999999999999289, 5.000000000000000000, 72.00402776293825013 ) ) ;
#29200=DIRECTION ( 'NONE',  ( -0.000000000000000000, -1.000000000000000000, -0.000000000000000000 ) ) ;
#29202=STYLED_ITEM ( 'NONE', ( #36137 ), #51812 ) ;
#29208=COLOUR_RGB ( '', 0.66274510, 0.83137255, 0.94901961) ;
#29210=ORIENTED_EDGE ( 'NONE', *, *, #44874, .F. ) ;
#29216=VERTEX_POINT ( 'NONE', #17921 ) ;
#29218=UNCERTAINTY_MEASURE_WITH_UNIT (LENGTH_MEASURE( 1.000000000000000082E-05 ), #64266, 'distance_accuracy_value', 'NONE');
#29219=MECHANICAL_DESIGN_GEOMETRIC_PRESENTATION_REPRESENTATION('',(#6732),#20236);
#29228=EDGE_CURVE ( 'NONE', #29216, #14021, #61494, .T. ) ;
#29241=SURFACE_STYLE_FILL_AREA ( #19024 ) ;
#29242=DIRECTION ( 'NONE',  ( -1.000000000000000000, -0.000000000000000000, -0.000000000000000000 ) ) ;
#29252=COLOUR_RGB ( '', 0.31764706, 0.68627451, 0.89019608) ;
#29256=FACE_OUTER_BOUND ( 'NONE', #25873, .T. ) ;
#29257=( GEOMETRIC_REPRESENTATION_CONTEXT ( 3 ) GLOBAL_UNCERTAINTY_ASSIGNED_CONTEXT ( ( #5298 ) ) GLOBAL_UNIT_ASSIGNED_CONTEXT ( ( #1309, #10896, #48220 ) ) REPRESENTATION_CONTEXT ( 'NONE', 'WORKASPACE' ) );
#29259=ORIENTED_EDGE ( 'NONE', *, *, #32621, .T. ) ;
#29263=FILL_AREA_STYLE ('',( #19048 ) ) ;
#29282=DIRECTION ( 'NONE',  ( 0.000000000000000000, -1.000000000000000000, 0.000000000000000000 ) ) ;
#29293=SURFACE_STYLE_USAGE ( .BOTH. , #12773 ) ;
#29303=( LENGTH_UNIT ( ) NAMED_UNIT ( * ) SI_UNIT ( .MILLI., .METRE. ) );
#29307=FACE_OUTER_BOUND ( 'NONE', #3053, .T. ) ;
#29309=ADVANCED_FACE ( 'NONE', ( #2364 ), #18935, .F. ) ;
#29324=CARTESIAN_POINT ( 'NONE',  ( 6.000000000000017764, 43.00000000000000000, -35.50000000000000000 ) ) ;
#29329=CARTESIAN_POINT ( 'NONE',  ( 24.58168140846667526, 25.30925735143623356, -27.43541942659303956 ) ) ;
#29336=ORIENTED_EDGE ( 'NONE', *, *, #4864, .T. ) ;
#29345=LINE ( 'NONE', #23383, #49281 ) ;
#29349=( NAMED_UNIT ( * ) PLANE_ANGLE_UNIT ( ) SI_UNIT ( $, .RADIAN. ) );
#29356=UNCERTAINTY_MEASURE_WITH_UNIT (LENGTH_MEASURE( 1.000000000000000082E-05 ), #60467, 'distance_accuracy_value', 'NONE');
#29359=EDGE_CURVE ( 'NONE', #30684, #1198, #15899, .T. ) ;
#29383=DIRECTION ( 'NONE',  ( -0.000000000000000000, -1.000000000000000000, -0.000000000000000000 ) ) ;
#29421=DIRECTION ( 'NONE',  ( 0.000000000000000000, 1.000000000000000000, 0.000000000000000000 ) ) ;
#29426=SURFACE_SIDE_STYLE ('',( #62128 ) ) ;
#29440=EDGE_CURVE ( 'NONE', #41529, #49536, #11974, .T. ) ;
#29448=( GEOMETRIC_REPRESENTATION_CONTEXT ( 3 ) GLOBAL_UNCERTAINTY_ASSIGNED_CONTEXT ( ( #44029 ) ) GLOBAL_UNIT_ASSIGNED_CONTEXT ( ( #14697, #16708, #36171 ) ) REPRESENTATION_CONTEXT ( 'NONE', 'WORKASPACE' ) );
#29456=FACE_OUTER_BOUND ( 'NONE', #12509, .T. ) ;
#29457=AXIS2_PLACEMENT_3D ( 'NONE', #47291, #31394, #5022 ) ;
#29458=EDGE_CURVE ( 'NONE', #69192, #10939, #30660, .T. ) ;
#29465=PRESENTATION_STYLE_ASSIGNMENT (( #45692 ) ) ;
#29468=AXIS2_PLACEMENT_3D ( 'NONE', #28170, #27829, #59510 ) ;
#29477=DIRECTION ( 'NONE',  ( -1.239088197126290817E-16, 0.000000000000000000, -1.000000000000000000 ) ) ;
#29480=DIRECTION ( 'NONE',  ( 0.000000000000000000, 0.000000000000000000, -1.000000000000000000 ) ) ;
#29483=PRESENTATION_STYLE_ASSIGNMENT (( #39731 ) ) ;
#29490=DIRECTION ( 'NONE',  ( -1.000000000000000000, 0.000000000000000000, 0.000000000000000000 ) ) ;
#29497=( GEOMETRIC_REPRESENTATION_CONTEXT ( 3 ) GLOBAL_UNCERTAINTY_ASSIGNED_CONTEXT ( ( #33538 ) ) GLOBAL_UNIT_ASSIGNED_CONTEXT ( ( #49740, #3218, #28598 ) ) REPRESENTATION_CONTEXT ( 'NONE', 'WORKASPACE' ) );
#29509=FILL_AREA_STYLE_COLOUR ( '', #55423 ) ;
#29524=DIRECTION ( 'NONE',  ( 0.000000000000000000, 0.000000000000000000, 1.000000000000000000 ) ) ;
#29541=MECHANICAL_DESIGN_GEOMETRIC_PRESENTATION_REPRESENTATION('',(#54245),#65501);
#29550=ORIENTED_EDGE ( 'NONE', *, *, #32971, .T. ) ;
#29565=ORIENTED_EDGE ( 'NONE', *, *, #17680, .T. ) ;
#29581=( NAMED_UNIT ( * ) PLANE_ANGLE_UNIT ( ) SI_UNIT ( $, .RADIAN. ) );
#29587=VERTEX_POINT ( 'NONE', #53089 ) ;
#29595=STYLED_ITEM ( 'NONE', ( #27702 ), #61678 ) ;
#29607=LINE ( 'NONE', #35239, #55473 ) ;
#29609=AXIS2_PLACEMENT_3D ( 'NONE', #34417, #3395, #51296 ) ;
#29610=PRODUCT_DEFINITION ( 'UNKNOWN', '', #28138, #62047 ) ;
#29618=VECTOR ( 'NONE', #10201, 1000.000000000000000 ) ;
#29640=MECHANICAL_DESIGN_GEOMETRIC_PRESENTATION_REPRESENTATION('',(#28514),#36421);
#29645=COLOUR_RGB ( '', 0.31764706, 0.68627451, 0.89019608) ;
#29670=SURFACE_SIDE_STYLE ('',( #34250 ) ) ;
#29677=VERTEX_POINT ( 'NONE', #49197 ) ;
#29681=CIRCLE ( 'NONE', #8350, 5.000000000000004441 ) ;
#29686=AXIS2_PLACEMENT_3D ( 'NONE', #43126, #37508, #5412 ) ;
#29689=DIRECTION ( 'NONE',  ( 1.000000000000000000, -0.000000000000000000, -1.300977106640434891E-16 ) ) ;
#29701=SURFACE_STYLE_FILL_AREA ( #34614 ) ;
#29708=FILL_AREA_STYLE_COLOUR ( '', #64618 ) ;
#29712=ORIENTED_EDGE ( 'NONE', *, *, #42180, .T. ) ;
#29716=AXIS2_PLACEMENT_3D ( 'NONE', #11027, #32151, #64512 ) ;
#29730=TOROIDAL_SURFACE ( 'NONE', #58911, 24.00000000000001421, 1.000000000000000000 ) ;
#29732=DIRECTION ( 'NONE',  ( 0.000000000000000000, 0.000000000000000000, 1.000000000000000000 ) ) ;
#29743=EDGE_CURVE ( 'NONE', #54047, #1442, #58696, .T. ) ;
#29747=( LENGTH_UNIT ( ) NAMED_UNIT ( * ) SI_UNIT ( .MILLI., .METRE. ) );
#29754=ORIENTED_EDGE ( 'NONE', *, *, #4689, .F. ) ;
#29758=PLANE ( 'NONE',  #68390 ) ;
#29759=DIRECTION ( 'NONE',  ( 0.000000000000000000, -1.000000000000000000, 0.000000000000000000 ) ) ;
#29763=( GEOMETRIC_REPRESENTATION_CONTEXT ( 3 ) GLOBAL_UNCERTAINTY_ASSIGNED_CONTEXT ( ( #977 ) ) GLOBAL_UNIT_ASSIGNED_CONTEXT ( ( #63393, #67275, #61987 ) ) REPRESENTATION_CONTEXT ( 'NONE', 'WORKASPACE' ) );
#29770=CARTESIAN_POINT ( 'NONE',  ( 27.00000000000001776, 42.00000000000000000, -34.49999999999999289 ) ) ;
#29773=FILL_AREA_STYLE ('',( #56140 ) ) ;
#29781=STYLED_ITEM ( 'NONE', ( #46438 ), #27529 ) ;
#29790=EDGE_CURVE ( 'NONE', #52838, #26396, #31958, .T. ) ;
#29794=( NAMED_UNIT ( * ) SI_UNIT ( $, .STERADIAN. ) SOLID_ANGLE_UNIT ( ) );
#29796=CARTESIAN_POINT ( 'NONE',  ( 0.08961394468541557246, 42.48853604202995626, -45.29557250688775127 ) ) ;
#29797=DIRECTION ( 'NONE',  ( 0.000000000000000000, -1.000000000000000000, 0.000000000000000000 ) ) ;
#29804=EDGE_LOOP ( 'NONE', ( #5226, #16725, #11714, #64935 ) ) ;
#29805=CARTESIAN_POINT ( 'NONE',  ( 23.50000000000001776, 27.44010416289936316, -27.18999999999999417 ) ) ;
#29814=CARTESIAN_POINT ( 'NONE',  ( 3.000000000000000000, 0.000000000000000000, -72.00402776293822171 ) ) ;
#29821=ORIENTED_EDGE ( 'NONE', *, *, #48672, .T. ) ;
#29826=CARTESIAN_POINT ( 'NONE',  ( 73.01088739851488185, 0.000000000000000000, -65.71817553072278884 ) ) ;
#29830=STYLED_ITEM ( 'NONE', ( #55421 ), #49411 ) ;
#29850=PRESENTATION_STYLE_ASSIGNMENT (( #52026 ) ) ;
#29861=CIRCLE ( 'NONE', #34334, 1.000000000000000888 ) ;
#29864=FILL_AREA_STYLE ('',( #63610 ) ) ;
#29866=EDGE_CURVE ( 'NONE', #66133, #7763, #12739, .T. ) ;
#29871=DIRECTION ( 'NONE',  ( 1.084202172485504434E-16, 0.000000000000000000, 1.000000000000000000 ) ) ;
#29872=CYLINDRICAL_SURFACE ( 'NONE', #24713, 1.000000000000000888 ) ;
#29874=FILL_AREA_STYLE_COLOUR ( '', #48474 ) ;
#29875=UNCERTAINTY_MEASURE_WITH_UNIT (LENGTH_MEASURE( 1.000000000000000082E-05 ), #10568, 'distance_accuracy_value', 'NONE');
#29892=STYLED_ITEM ( 'NONE', ( #49551 ), #5776 ) ;
#29893=CARTESIAN_POINT ( 'NONE',  ( 11.00000000000001776, 26.00000000000000355, 23.99999999999999645 ) ) ;
#29900=VERTEX_POINT ( 'NONE', #34385 ) ;
#29901=DIRECTION ( 'NONE',  ( 1.000000000000000000, 0.000000000000000000, 0.000000000000000000 ) ) ;
#29909=DIRECTION ( 'NONE',  ( -0.000000000000000000, -1.000000000000000000, -0.000000000000000000 ) ) ;
#29915=ORIENTED_EDGE ( 'NONE', *, *, #36687, .F. ) ;
#29919=CARTESIAN_POINT ( 'NONE',  ( 1.000000000000000000, 14.00000000000000000, -80.00402776293826435 ) ) ;
#29924=LINE ( 'NONE', #2805, #21309 ) ;
#29946=EDGE_CURVE ( 'NONE', #60879, #53365, #45331, .T. ) ;
#29947=( NAMED_UNIT ( * ) PLANE_ANGLE_UNIT ( ) SI_UNIT ( $, .RADIAN. ) );
#29949=CARTESIAN_POINT ( 'NONE',  ( 23.32387453076606221, 27.44010416289935606, -27.18999999999999773 ) ) ;
#29956=UNCERTAINTY_MEASURE_WITH_UNIT (LENGTH_MEASURE( 1.000000000000000082E-05 ), #44897, 'distance_accuracy_value', 'NONE');
#29959=COLOUR_RGB ( '', 0.31764706, 0.68627451, 0.89019608) ;
#29966=CARTESIAN_POINT ( 'NONE',  ( 6.000000000000017764, 26.00000000000000355, -24.00000000000000355 ) ) ;
#29977=VERTEX_POINT ( 'NONE', #14673 ) ;
#29980=ORIENTED_EDGE ( 'NONE', *, *, #47319, .T. ) ;
#29982=SURFACE_STYLE_USAGE ( .BOTH. , #67992 ) ;
#29984=EDGE_CURVE ( 'NONE', #13573, #13184, #9406, .T. ) ;
#29990=EDGE_LOOP ( 'NONE', ( #42020, #33020, #55717, #37960 ) ) ;
#29992=UNCERTAINTY_MEASURE_WITH_UNIT (LENGTH_MEASURE( 1.000000000000000082E-05 ), #37368, 'distance_accuracy_value', 'NONE');
#30008=VERTEX_POINT ( 'NONE', #56522 ) ;
#30020=EDGE_CURVE ( 'NONE', #39120, #57229, #62201, .T. ) ;
#30021=SURFACE_SIDE_STYLE ('',( #30701 ) ) ;
#30024=CARTESIAN_POINT ( 'NONE',  ( 31.00000000000000000, 42.00000000000000000, -79.00402776293826435 ) ) ;
#30028=VECTOR ( 'NONE', #63325, 1000.000000000000000 ) ;
#30050=SURFACE_STYLE_USAGE ( .BOTH. , #30742 ) ;
#30052=ORIENTED_EDGE ( 'NONE', *, *, #53298, .F. ) ;
#30066=EDGE_LOOP ( 'NONE', ( #60342, #61148, #25632, #27875 ) ) ;
#30074=FILL_AREA_STYLE_COLOUR ( '', #49881 ) ;
#30085=ORIENTED_EDGE ( 'NONE', *, *, #35012, .F. ) ;
#30092=EDGE_CURVE ( 'NONE', #35716, #14824, #68141, .T. ) ;
#30094=ORIENTED_EDGE ( 'NONE', *, *, #22975, .T. ) ;
#30125=( NAMED_UNIT ( * ) SI_UNIT ( $, .STERADIAN. ) SOLID_ANGLE_UNIT ( ) );
#30127=DIRECTION ( 'NONE',  ( 0.000000000000000000, -1.000000000000000000, 0.000000000000000000 ) ) ;
#30128=VERTEX_POINT ( 'NONE', #7141 ) ;
#30130=ORIENTED_EDGE ( 'NONE', *, *, #65607, .T. ) ;
#30146=FACE_OUTER_BOUND ( 'NONE', #49478, .T. ) ;
#30147=EDGE_CURVE ( 'NONE', #26396, #38068, #391, .T. ) ;
#30154=EDGE_CURVE ( 'NONE', #31521, #21181, #55319, .T. ) ;
#30164=LINE ( 'NONE', #53389, #15160 ) ;
#30170=ORIENTED_EDGE ( 'NONE', *, *, #64312, .T. ) ;
#30175=EDGE_LOOP ( 'NONE', ( #48461, #42553, #8624, #25490 ) ) ;
#30178=SURFACE_STYLE_USAGE ( .BOTH. , #30524 ) ;
#30182=SURFACE_STYLE_USAGE ( .BOTH. , #61177 ) ;
#30186=( NAMED_UNIT ( * ) PLANE_ANGLE_UNIT ( ) SI_UNIT ( $, .RADIAN. ) );
#30193=( GEOMETRIC_REPRESENTATION_CONTEXT ( 3 ) GLOBAL_UNCERTAINTY_ASSIGNED_CONTEXT ( ( #63670 ) ) GLOBAL_UNIT_ASSIGNED_CONTEXT ( ( #57685, #21415, #37661 ) ) REPRESENTATION_CONTEXT ( 'NONE', 'WORKASPACE' ) );
#30202=SURFACE_STYLE_FILL_AREA ( #8779 ) ;
#30208=CYLINDRICAL_SURFACE ( 'NONE', #43004, 1.000000000000000888 ) ;
#30215=CARTESIAN_POINT ( 'NONE',  ( 27.99999999999999645, 5.000000000000000000, 24.00402776293821816 ) ) ;
#30217=EDGE_LOOP ( 'NONE', ( #66049, #15493, #9764, #52088 ) ) ;
#30228=SURFACE_STYLE_USAGE ( .BOTH. , #56988 ) ;
#30249=ADVANCED_FACE ( 'NONE', ( #49371 ), #6096, .F. ) ;
#30265=CYLINDRICAL_SURFACE ( 'NONE', #37470, 112.9999999999981526 ) ;
#30269=( NAMED_UNIT ( * ) SI_UNIT ( $, .STERADIAN. ) SOLID_ANGLE_UNIT ( ) );
#30270=AXIS2_PLACEMENT_3D ( 'NONE', #54168, #31066, #22170 ) ;
#30275=LINE ( 'NONE', #36319, #42715 ) ;
#30282=COLOUR_RGB ( '', 0.09019608, 0.27058824, 0.51372549) ;
#30295=ORIENTED_EDGE ( 'NONE', *, *, #47304, .F. ) ;
#30302=COLOUR_RGB ( '', 0.72549020, 0.75294118, 0.79215686) ;
#30306=CIRCLE ( 'NONE', #11258, 113.0000000000030127 ) ;
#30307=EDGE_CURVE ( 'NONE', #32128, #45031, #25201, .T. ) ;
#30315=( GEOMETRIC_REPRESENTATION_CONTEXT ( 3 ) GLOBAL_UNCERTAINTY_ASSIGNED_CONTEXT ( ( #62134 ) ) GLOBAL_UNIT_ASSIGNED_CONTEXT ( ( #66825, #61861, #45740 ) ) REPRESENTATION_CONTEXT ( 'NONE', 'WORKASPACE' ) );
#30332=( NAMED_UNIT ( * ) SI_UNIT ( $, .STERADIAN. ) SOLID_ANGLE_UNIT ( ) );
#30335=CARTESIAN_POINT ( 'NONE',  ( 109.0067032876572455, 13.00000000000000178, -19.20378738324562207 ) ) ;
#30339=COLOUR_RGB ( '', 0.09019608, 0.27058824, 0.51372549) ;
#30342=DIRECTION ( 'NONE',  ( -1.000000000000000000, 0.000000000000000000, 0.000000000000000000 ) ) ;
#30347=ORIENTED_EDGE ( 'NONE', *, *, #24553, .T. ) ;
#30351=DIRECTION ( 'NONE',  ( 1.000000000000000000, 0.000000000000000000, 0.000000000000000000 ) ) ;
#30355=CIRCLE ( 'NONE', #40552, 16.99999999999998579 ) ;
#30356=STYLED_ITEM ( 'NONE', ( #54083 ), #15754 ) ;
#30361=SURFACE_STYLE_USAGE ( .BOTH. , #56079 ) ;
#30365=FACE_OUTER_BOUND ( 'NONE', #61947, .T. ) ;
#30368=ORIENTED_EDGE ( 'NONE', *, *, #30092, .F. ) ;
#30374=COLOUR_RGB ( '', 0.66274510, 0.83137255, 0.94901961) ;
#30375=DIRECTION ( 'NONE',  ( -6.938893903907222856E-15, -0.000000000000000000, -1.000000000000000000 ) ) ;
#30383=AXIS2_PLACEMENT_3D ( 'NONE', #63111, #8960, #35353 ) ;
#30388=DIRECTION ( 'NONE',  ( 1.000000000000000000, 0.000000000000000000, 0.000000000000000000 ) ) ;
#30390=SURFACE_SIDE_STYLE ('',( #38680 ) ) ;
#30403=ORIENTED_EDGE ( 'NONE', *, *, #52082, .F. ) ;
#30408=ADVANCED_FACE ( 'NONE', ( #52846 ), #33441, .T. ) ;
#30416=ORIENTED_EDGE ( 'NONE', *, *, #36248, .T. ) ;
#30417=DIRECTION ( 'NONE',  ( 4.449603764765679692E-17, -0.9396926207859105373, 0.3420201433256630508 ) ) ;
#30421=( NAMED_UNIT ( * ) SI_UNIT ( $, .STERADIAN. ) SOLID_ANGLE_UNIT ( ) );
#30424=MECHANICAL_DESIGN_GEOMETRIC_PRESENTATION_REPRESENTATION('',(#58575),#67508);
#30426=TOROIDAL_SURFACE ( 'NONE', #2261, 17.00000000000000355, 1.000000000000000000 ) ;
#30427=CARTESIAN_POINT ( 'NONE',  ( 57.00000000000000000, 0.9999999999999991118, 80.00402776293826435 ) ) ;
#30434=DIRECTION ( 'NONE',  ( -0.000000000000000000, -1.000000000000000000, -0.000000000000000000 ) ) ;
#30443=DIRECTION ( 'NONE',  ( -0.000000000000000000, 1.000000000000000000, -0.000000000000000000 ) ) ;
#30444=DIRECTION ( 'NONE',  ( 1.000000000000000000, -0.000000000000000000, -1.300977106640434891E-16 ) ) ;
#30446=UNCERTAINTY_MEASURE_WITH_UNIT (LENGTH_MEASURE( 1.000000000000000082E-05 ), #6040, 'distance_accuracy_value', 'NONE');
#30459=CARTESIAN_POINT ( 'NONE',  ( 0.4644249260832968851, 42.85561104658234655, -45.52242297229210521 ) ) ;
#30463=CARTESIAN_POINT ( 'NONE',  ( 3.000000000000030198, 0.000000000000000000, 3.772833609257260986E-15 ) ) ;
#30466=FACE_OUTER_BOUND ( 'NONE', #29990, .T. ) ;
#30474=DIRECTION ( 'NONE',  ( 1.000000000000000000, 0.000000000000000000, 0.000000000000000000 ) ) ;
#30475=STYLED_ITEM ( 'NONE', ( #34931 ), #45982 ) ;
#30476=EDGE_CURVE ( 'NONE', #68708, #360, #33106, .T. ) ;
#30478=CARTESIAN_POINT ( 'NONE',  ( 10.00000000000002132, 50.00000000000000000, 60.00000000000000000 ) ) ;
#30489=FACE_OUTER_BOUND ( 'NONE', #13453, .T. ) ;
#30506=CARTESIAN_POINT ( 'NONE',  ( 179.4361977533490347, 5.000000000000000000, -103.7004518695263044 ) ) ;
#30511=VECTOR ( 'NONE', #13299, 1000.000000000000227 ) ;
#30524=SURFACE_SIDE_STYLE ('',( #3063 ) ) ;
#30528=( NAMED_UNIT ( * ) SI_UNIT ( $, .STERADIAN. ) SOLID_ANGLE_UNIT ( ) );
#30530=FILL_AREA_STYLE_COLOUR ( '', #25687 ) ;
#30534=LINE ( 'NONE', #67152, #62993 ) ;
#30536=CYLINDRICAL_SURFACE ( 'NONE', #17459, 1.000000000000000888 ) ;
#30539=FILL_AREA_STYLE_COLOUR ( '', #30302 ) ;
#30544=SURFACE_STYLE_FILL_AREA ( #8771 ) ;
#30546=FACE_OUTER_BOUND ( 'NONE', #19637, .T. ) ;
#30550=EDGE_CURVE ( 'NONE', #63380, #52516, #7413, .T. ) ;
#30555=STYLED_ITEM ( 'NONE', ( #4671 ), #28790 ) ;
#30563=STYLED_ITEM ( 'NONE', ( #42371 ), #25659 ) ;
#30568=CYLINDRICAL_SURFACE ( 'NONE', #362, 1.000000000000000888 ) ;
#30570=EDGE_LOOP ( 'NONE', ( #8232, #41223, #62195, #39799 ) ) ;
#30576=DIRECTION ( 'NONE',  ( 0.000000000000000000, 0.000000000000000000, -1.000000000000000000 ) ) ;
#30618=CARTESIAN_POINT ( 'NONE',  ( 57.00000000000000000, 13.00000000000000178, 60.00402776293827145 ) ) ;
#30623=PRESENTATION_STYLE_ASSIGNMENT (( #9205 ) ) ;
#30631=CARTESIAN_POINT ( 'NONE',  ( 57.00000000000000000, 16.00000000000000000, 60.00402776293825724 ) ) ;
#30648=ORIENTED_EDGE ( 'NONE', *, *, #33756, .F. ) ;
#30651=( GEOMETRIC_REPRESENTATION_CONTEXT ( 3 ) GLOBAL_UNCERTAINTY_ASSIGNED_CONTEXT ( ( #8076 ) ) GLOBAL_UNIT_ASSIGNED_CONTEXT ( ( #65736, #66070, #55528 ) ) REPRESENTATION_CONTEXT ( 'NONE', 'WORKASPACE' ) );
#30658=ORIENTED_EDGE ( 'NONE', *, *, #40160, .T. ) ;
#30660=CIRCLE ( 'NONE', #3672, 18.99999999999998934 ) ;
#30665=CYLINDRICAL_SURFACE ( 'NONE', #23666, 1.000000000000000888 ) ;
#30674=UNCERTAINTY_MEASURE_WITH_UNIT (LENGTH_MEASURE( 1.000000000000000082E-05 ), #49968, 'distance_accuracy_value', 'NONE');
#30684=VERTEX_POINT ( 'NONE', #56633 ) ;
#30690=SURFACE_SIDE_STYLE ('',( #2250 ) ) ;
#30700=CIRCLE ( 'NONE', #29609, 12.50000000000000178 ) ;
#30701=SURFACE_STYLE_FILL_AREA ( #51156 ) ;
#30706=SURFACE_STYLE_FILL_AREA ( #36406 ) ;
#30714=DIRECTION ( 'NONE',  ( -0.000000000000000000, -1.000000000000000000, 0.000000000000000000 ) ) ;
#30717=FACE_OUTER_BOUND ( 'NONE', #42954, .T. ) ;
#30723=CARTESIAN_POINT ( 'NONE',  ( 3.414213562373098032, 42.99999999999999289, -90.00000000000001421 ) ) ;
#30726=EDGE_CURVE ( 'NONE', #11361, #52535, #24093, .T. ) ;
#30728=DIRECTION ( 'NONE',  ( 0.000000000000000000, -0.000000000000000000, 1.000000000000000000 ) ) ;
#30731=DIRECTION ( 'NONE',  ( 0.000000000000000000, 1.000000000000000000, 0.000000000000000000 ) ) ;
#30733=ORIENTED_EDGE ( 'NONE', *, *, #4335, .F. ) ;
#30737=( LENGTH_UNIT ( ) NAMED_UNIT ( * ) SI_UNIT ( .MILLI., .METRE. ) );
#30740=EDGE_CURVE ( 'NONE', #57872, #7256, #8787, .T. ) ;
#30741=PRESENTATION_STYLE_ASSIGNMENT (( #57489 ) ) ;
#30742=SURFACE_SIDE_STYLE ('',( #4333 ) ) ;
#30757=UNCERTAINTY_MEASURE_WITH_UNIT (LENGTH_MEASURE( 1.000000000000000082E-05 ), #51067, 'distance_accuracy_value', 'NONE');
#30761=CARTESIAN_POINT ( 'NONE',  ( 4.000000000000002665, 38.00000000000000711, -90.00000000000000000 ) ) ;
#30774=STYLED_ITEM ( 'NONE', ( #10036 ), #7361 ) ;
#30778=COLOUR_RGB ( '', 0.66274510, 0.83137255, 0.94901961) ;
#30782=ORIENTED_EDGE ( 'NONE', *, *, #24450, .T. ) ;
#30796=SURFACE_STYLE_USAGE ( .BOTH. , #19556 ) ;
#30801=DIRECTION ( 'NONE',  ( 0.000000000000000000, 0.000000000000000000, -1.000000000000000000 ) ) ;
#30805=EDGE_LOOP ( 'NONE', ( #55091, #16114, #6367, #56969 ) ) ;
#30806=VECTOR ( 'NONE', #35221, 1000.000000000000000 ) ;
#30809=CARTESIAN_POINT ( 'NONE',  ( 26.00000000000001776, -3.148064030671221758, -29.68999999999999417 ) ) ;
#30811=CIRCLE ( 'NONE', #36496, 1.499999999999997780 ) ;
#30814=SURFACE_SIDE_STYLE ('',( #59531 ) ) ;
#30832=AXIS2_PLACEMENT_3D ( 'NONE', #9694, #41015, #56824 ) ;
#30833=CARTESIAN_POINT ( 'NONE',  ( -1.387778780781445676E-14, 17.78868675966041835, 1.540743955509788682E-30 ) ) ;
#30836=CARTESIAN_POINT ( 'NONE',  ( 23.50000000000041211, 24.55989583709592949, -27.18999999999997286 ) ) ;
#30846=DIRECTION ( 'NONE',  ( -1.982541115402068561E-16, 0.000000000000000000, 1.000000000000000000 ) ) ;
#30847=EDGE_LOOP ( 'NONE', ( #15483, #18393, #28575 ) ) ;
#30848=MECHANICAL_DESIGN_GEOMETRIC_PRESENTATION_REPRESENTATION('',(#15028),#64406);
#30852=CYLINDRICAL_SURFACE ( 'NONE', #62039, 1.000000000000000888 ) ;
#30853=EDGE_CURVE ( 'NONE', #15864, #62763, #52092, .T. ) ;
#30863=EDGE_LOOP ( 'NONE', ( #46503, #8424, #61078, #2963 ) ) ;
#30885=DIRECTION ( 'NONE',  ( -1.000000000000000000, 0.000000000000000000, 0.000000000000000000 ) ) ;
#30891=ORIENTED_EDGE ( 'NONE', *, *, #42173, .T. ) ;
#30896=( NAMED_UNIT ( * ) PLANE_ANGLE_UNIT ( ) SI_UNIT ( $, .RADIAN. ) );
#30902=CARTESIAN_POINT ( 'NONE',  ( 8.000000000000035527, 0.000000000000000000, -77.00402776293825013 ) ) ;
#30906=DIRECTION ( 'NONE',  ( 0.000000000000000000, 0.000000000000000000, 1.000000000000000000 ) ) ;
#30910=EDGE_LOOP ( 'NONE', ( #18888, #35529, #3950, #42574 ) ) ;
#30918=ORIENTED_EDGE ( 'NONE', *, *, #5312, .F. ) ;
#30929=ORIENTED_EDGE ( 'NONE', *, *, #27537, .T. ) ;
#30937=FILL_AREA_STYLE ('',( #51365 ) ) ;
#30948=DIRECTION ( 'NONE',  ( 0.000000000000000000, 0.000000000000000000, -1.000000000000000000 ) ) ;
#30954=VERTEX_POINT ( 'NONE', #5558 ) ;
#30957=LINE ( 'NONE', #47193, #52028 ) ;
#30969=CARTESIAN_POINT ( 'NONE',  ( 22.64869388986209486, 27.05257840322770591, 27.33874645186988417 ) ) ;
#30985=FILL_AREA_STYLE ('',( #13415 ) ) ;
#31001=DIRECTION ( 'NONE',  ( 0.000000000000000000, 0.000000000000000000, -1.000000000000000000 ) ) ;
#31005=SURFACE_STYLE_FILL_AREA ( #41596 ) ;
#31011=DIRECTION ( 'NONE',  ( 1.000000000000000000, 0.000000000000000000, -1.300977106640434891E-16 ) ) ;
#31015=ORIENTED_EDGE ( 'NONE', *, *, #53231, .T. ) ;
#31019=DIRECTION ( 'NONE',  ( 0.000000000000000000, -1.000000000000000000, 0.000000000000000000 ) ) ;
#31020=DIRECTION ( 'NONE',  ( 0.000000000000000000, 0.000000000000000000, -1.000000000000000000 ) ) ;
#31024=CARTESIAN_POINT ( 'NONE',  ( 22.99999999999998934, 5.000000000000000000, 37.00402776293825724 ) ) ;
#31034=ADVANCED_FACE ( 'NONE', ( #28751 ), #12735, .T. ) ;
#31035=VECTOR ( 'NONE', #60876, 1000.000000000000000 ) ;
#31044=DIRECTION ( 'NONE',  ( -1.000000000000000000, 0.000000000000000000, 0.000000000000000000 ) ) ;
#31054=SURFACE_SIDE_STYLE ('',( #62380 ) ) ;
#31066=DIRECTION ( 'NONE',  ( -0.000000000000000000, -1.000000000000000000, -0.000000000000000000 ) ) ;
#31069=CARTESIAN_POINT ( 'NONE',  ( 8.000000000000035527, 0.000000000000000000, 77.00402776293825013 ) ) ;
#31092=CARTESIAN_POINT ( 'NONE',  ( 29.00000000000000000, 38.70020753820971748, -89.00000000000000000 ) ) ;
#31099=ORIENTED_EDGE ( 'NONE', *, *, #56202, .F. ) ;
#31102=PRESENTATION_STYLE_ASSIGNMENT (( #35370 ) ) ;
#31103=ORIENTED_EDGE ( 'NONE', *, *, #26693, .F. ) ;
#31112=SURFACE_STYLE_USAGE ( .BOTH. , #42780 ) ;
#31141=CARTESIAN_POINT ( 'NONE',  ( 1.000000000000000000, 0.9999999999999991118, 79.00402776293826435 ) ) ;
#31146=CARTESIAN_POINT ( 'NONE',  ( 31.00000000000000711, 14.00000000000000000, -34.49999999999999289 ) ) ;
#31148=PRESENTATION_STYLE_ASSIGNMENT (( #37890 ) ) ;
#31152=DIRECTION ( 'NONE',  ( 0.000000000000000000, 0.000000000000000000, -1.000000000000000000 ) ) ;
#31160=AXIS2_PLACEMENT_3D ( 'NONE', #55179, #49945, #44694 ) ;
#31170=CARTESIAN_POINT ( 'NONE',  ( 22.65111520450740201, 24.94462592285371727, -27.33786404998805608 ) ) ;
#31171=AXIS2_PLACEMENT_3D ( 'NONE', #41762, #31495, #37182 ) ;
#31176=VECTOR ( 'NONE', #47738, 1000.000000000000000 ) ;
#31177=DIRECTION ( 'NONE',  ( -1.000000000000000000, 0.000000000000000000, -3.717264591378879477E-17 ) ) ;
#31186=EDGE_CURVE ( 'NONE', #13184, #18616, #49437, .T. ) ;
#31193=FACE_OUTER_BOUND ( 'NONE', #23265, .T. ) ;
#31203=SURFACE_STYLE_USAGE ( .BOTH. , #65923 ) ;
#31214=PRESENTATION_STYLE_ASSIGNMENT (( #36900 ) ) ;
#31217=ORIENTED_EDGE ( 'NONE', *, *, #32621, .F. ) ;
#31219=DIRECTION ( 'NONE',  ( -1.000000000000000000, -0.000000000000000000, 3.469446951953610639E-15 ) ) ;
#31230=STYLED_ITEM ( 'NONE', ( #19481 ), #67535 ) ;
#31242=ORIENTED_EDGE ( 'NONE', *, *, #39255, .T. ) ;
#31251=CARTESIAN_POINT ( 'NONE',  ( 3.000000000000002665, 42.00000000000000000, -80.00402776293826435 ) ) ;
#31253=STYLED_ITEM ( 'NONE', ( #18073 ), #50834 ) ;
#31260=EDGE_CURVE ( 'NONE', #60615, #56838, #29607, .T. ) ;
#31262=ADVANCED_FACE ( 'NONE', ( #19396 ), #56331, .T. ) ;
#31271=AXIS2_PLACEMENT_3D ( 'NONE', #48473, #37592, #4452 ) ;
#31280=DIRECTION ( 'NONE',  ( 1.000000000000000000, 0.000000000000000000, -1.300977106640435137E-16 ) ) ;
#31281=UNCERTAINTY_MEASURE_WITH_UNIT (LENGTH_MEASURE( 1.000000000000000082E-05 ), #62710, 'distance_accuracy_value', 'NONE');
#31284=CARTESIAN_POINT ( 'NONE',  ( 6.000000000000017764, 26.00000000000000355, -24.00000000000000355 ) ) ;
#31289=ORIENTED_EDGE ( 'NONE', *, *, #64740, .T. ) ;
#31291=LINE ( 'NONE', #52106, #30028 ) ;
#31298=LINE ( 'NONE', #59087, #24020 ) ;
#31299=EDGE_CURVE ( 'NONE', #4136, #3674, #49920, .T. ) ;
#31303=ORIENTED_EDGE ( 'NONE', *, *, #47807, .T. ) ;
#31311=AXIS2_PLACEMENT_3D ( 'NONE', #8468, #3106, #30576 ) ;
#31312=FACE_OUTER_BOUND ( 'NONE', #3473, .T. ) ;
#31319=AXIS2_PLACEMENT_3D ( 'NONE', #6068, #54924, #6751 ) ;
#31325=( GEOMETRIC_REPRESENTATION_CONTEXT ( 3 ) GLOBAL_UNCERTAINTY_ASSIGNED_CONTEXT ( ( #11582 ) ) GLOBAL_UNIT_ASSIGNED_CONTEXT ( ( #4760, #21635, #32196 ) ) REPRESENTATION_CONTEXT ( 'NONE', 'WORKASPACE' ) );
#31337=ORIENTED_EDGE ( 'NONE', *, *, #21944, .T. ) ;
#31338=VERTEX_POINT ( 'NONE', #53500 ) ;
#31343=SURFACE_STYLE_USAGE ( .BOTH. , #65084 ) ;
#31350=VERTEX_POINT ( 'NONE', #67961 ) ;
#31358=AXIS2_PLACEMENT_3D ( 'NONE', #59556, #5386, #42752 ) ;
#31360=DIRECTION ( 'NONE',  ( -1.000000000000000000, -0.000000000000000000, 4.625929269271505635E-16 ) ) ;
#31369=EDGE_CURVE ( 'NONE', #9217, #9855, #16920, .T. ) ;
#31372=VECTOR ( 'NONE', #15618, 1000.000000000000000 ) ;
#31380=ORIENTED_EDGE ( 'NONE', *, *, #54570, .T. ) ;
#31389=( LENGTH_UNIT ( ) NAMED_UNIT ( * ) SI_UNIT ( .MILLI., .METRE. ) );
#31391=STYLED_ITEM ( 'NONE', ( #11832 ), #1111 ) ;
#31393=AXIS2_PLACEMENT_3D ( 'NONE', #8651, #62781, #56479 ) ;
#31394=DIRECTION ( 'NONE',  ( -0.000000000000000000, -1.000000000000000000, -0.000000000000000000 ) ) ;
#31401=STYLED_ITEM ( 'NONE', ( #14540 ), #42953 ) ;
#31418=VERTEX_POINT ( 'NONE', #12285 ) ;
#31422=CYLINDRICAL_SURFACE ( 'NONE', #10266, 4.999999999999997335 ) ;
#31426=DIRECTION ( 'NONE',  ( -1.000000000000000000, 0.000000000000000000, 0.000000000000000000 ) ) ;
#31431=DIRECTION ( 'NONE',  ( 0.000000000000000000, 0.000000000000000000, -1.000000000000000000 ) ) ;
#31434=VERTEX_POINT ( 'NONE', #11266 ) ;
#31444=UNCERTAINTY_MEASURE_WITH_UNIT (LENGTH_MEASURE( 1.000000000000000082E-05 ), #21067, 'distance_accuracy_value', 'NONE');
#31448=EDGE_CURVE ( 'NONE', #59410, #44068, #21837, .T. ) ;
#31462=ORIENTED_EDGE ( 'NONE', *, *, #22553, .T. ) ;
#31466=( NAMED_UNIT ( * ) SI_UNIT ( $, .STERADIAN. ) SOLID_ANGLE_UNIT ( ) );
#31468=ORIENTED_EDGE ( 'NONE', *, *, #10953, .T. ) ;
#31477=EDGE_CURVE ( 'NONE', #4847, #32128, #43673, .T. ) ;
#31478=TOROIDAL_SURFACE ( 'NONE', #1082, 17.00000000000000355, 1.000000000000000000 ) ;
#31482=CARTESIAN_POINT ( 'NONE',  ( 27.00000000000001776, 15.00000000000000000, 34.49999999999999289 ) ) ;
#31484=( GEOMETRIC_REPRESENTATION_CONTEXT ( 3 ) GLOBAL_UNCERTAINTY_ASSIGNED_CONTEXT ( ( #68472 ) ) GLOBAL_UNIT_ASSIGNED_CONTEXT ( ( #20347, #30896, #47123 ) ) REPRESENTATION_CONTEXT ( 'NONE', 'WORKASPACE' ) );
#31495=DIRECTION ( 'NONE',  ( 1.000000000000000000, 0.000000000000000000, -1.300977106640434891E-16 ) ) ;
#31501=CARTESIAN_POINT ( 'NONE',  ( 4.000000000000030198, 37.76051491742381216, 89.34202014332566932 ) ) ;
#31512=DIRECTION ( 'NONE',  ( 1.000000000000000000, 0.000000000000000000, 0.000000000000000000 ) ) ;
#31516=VECTOR ( 'NONE', #6643, 1000.000000000000000 ) ;
#31519=DIRECTION ( 'NONE',  ( -0.000000000000000000, -1.000000000000000000, 0.000000000000000000 ) ) ;
#31521=VERTEX_POINT ( 'NONE', #27424 ) ;
#31527=EDGE_CURVE ( 'NONE', #27365, #25944, #45489, .T. ) ;
#31535=FACE_BOUND ( 'NONE', #16166, .T. ) ;
#31541=DIRECTION ( 'NONE',  ( 0.000000000000000000, 1.000000000000000000, -0.000000000000000000 ) ) ;
#31546=AXIS2_PLACEMENT_3D ( 'NONE', #36218, #25955, #42898 ) ;
#31566=VERTEX_POINT ( 'NONE', #56607 ) ;
#31576=AXIS2_PLACEMENT_3D ( 'NONE', #66073, #12605, #7353 ) ;
#31581=DIRECTION ( 'NONE',  ( -1.000000000000000000, 0.000000000000000000, 0.000000000000000000 ) ) ;
#31585=FILL_AREA_STYLE_COLOUR ( '', #38815 ) ;
#31594=DIRECTION ( 'NONE',  ( 0.000000000000000000, 0.000000000000000000, -1.000000000000000000 ) ) ;
#31599=ADVANCED_FACE ( 'NONE', ( #60827 ), #8072, .F. ) ;
#31604=ADVANCED_FACE ( 'NONE', ( #46084 ), #34455, .T. ) ;
#31607=DIRECTION ( 'NONE',  ( 0.000000000000000000, 0.000000000000000000, -1.000000000000000000 ) ) ;
#31611=ORIENTED_EDGE ( 'NONE', *, *, #45146, .F. ) ;
#31613=MECHANICAL_DESIGN_GEOMETRIC_PRESENTATION_REPRESENTATION('',(#61943),#9144);
#31617=SURFACE_STYLE_FILL_AREA ( #57674 ) ;
#31620=( NAMED_UNIT ( * ) SI_UNIT ( $, .STERADIAN. ) SOLID_ANGLE_UNIT ( ) );
#31629=MECHANICAL_DESIGN_GEOMETRIC_PRESENTATION_REPRESENTATION('',(#57495),#32798);
#31638=CARTESIAN_POINT ( 'NONE',  ( 32.00000000000001421, 43.00000000000000000, -36.50000000000000000 ) ) ;
#31641=LINE ( 'NONE', #20398, #59248 ) ;
#31656=EDGE_CURVE ( 'NONE', #18616, #62752, #69251, .T. ) ;
#31658=SURFACE_STYLE_USAGE ( .BOTH. , #21105 ) ;
#31660=SURFACE_SIDE_STYLE ('',( #21451 ) ) ;
#31662=VECTOR ( 'NONE', #12501, 1000.000000000000000 ) ;
#31696=EDGE_CURVE ( 'NONE', #22643, #56835, #30811, .T. ) ;
#31697=( NAMED_UNIT ( * ) SI_UNIT ( $, .STERADIAN. ) SOLID_ANGLE_UNIT ( ) );
#31705=CYLINDRICAL_SURFACE ( 'NONE', #28022, 1.000000000000000888 ) ;
#31708=ORIENTED_EDGE ( 'NONE', *, *, #28224, .F. ) ;
#31715=DIRECTION ( 'NONE',  ( 1.000000000000000000, -6.162975822039156098E-33, -1.300977106640435137E-16 ) ) ;
#31719=EDGE_LOOP ( 'NONE', ( #2801, #6193, #46115, #10068 ) ) ;
#31725=LINE ( 'NONE', #52866, #60224 ) ;
#31733=VERTEX_POINT ( 'NONE', #36597 ) ;
#31736=CARTESIAN_POINT ( 'NONE',  ( 33.00000000000002132, 15.00000000000000000, 79.00402776293826435 ) ) ;
#31738=CARTESIAN_POINT ( 'NONE',  ( 33.00000000000002132, 14.00000000000000000, 80.00402776293826435 ) ) ;
#31742=ORIENTED_EDGE ( 'NONE', *, *, #28726, .F. ) ;
#31749=COLOUR_RGB ( '', 0.40784314, 0.44705882, 0.49803922) ;
#31751=( NAMED_UNIT ( * ) SI_UNIT ( $, .STERADIAN. ) SOLID_ANGLE_UNIT ( ) );
#31754=CARTESIAN_POINT ( 'NONE',  ( 10.00000000000001954, 42.00000000000000000, 28.38386403503541899 ) ) ;
#31755=CARTESIAN_POINT ( 'NONE',  ( 31.00000000000000711, -60.04052944165106709, -35.50000000000000000 ) ) ;
#31773=EDGE_CURVE ( 'NONE', #65192, #39245, #28019, .T. ) ;
#31779=LINE ( 'NONE', #69091, #21142 ) ;
#31780=DIRECTION ( 'NONE',  ( 0.000000000000000000, 0.000000000000000000, 1.000000000000000000 ) ) ;
#31781=ORIENTED_EDGE ( 'NONE', *, *, #54570, .F. ) ;
#31786=COLOUR_RGB ( '', 0.72549020, 0.75294118, 0.79215686) ;
#31805=SURFACE_STYLE_FILL_AREA ( #57875 ) ;
#31818=CIRCLE ( 'NONE', #21740, 1.000000000000000888 ) ;
#31820=CARTESIAN_POINT ( 'NONE',  ( 4.000000000000002665, 43.00000000000000000, 0.000000000000000000 ) ) ;
#31840=CARTESIAN_POINT ( 'NONE',  ( 179.4361977533490347, 14.00000000000000000, -103.7004518695263044 ) ) ;
#31841=CARTESIAN_POINT ( 'NONE',  ( 3.000000000000002665, 35.42594141563417054, -80.00402776293826435 ) ) ;
#31848=MECHANICAL_DESIGN_GEOMETRIC_PRESENTATION_REPRESENTATION('',(#9383),#18370);
#31849=SURFACE_STYLE_FILL_AREA ( #57919 ) ;
#31854=ADVANCED_FACE ( 'NONE', ( #64300, #11526, #5202 ), #26647, .F. ) ;
#31862=PRESENTATION_STYLE_ASSIGNMENT (( #21660 ) ) ;
#31864=( NAMED_UNIT ( * ) PLANE_ANGLE_UNIT ( ) SI_UNIT ( $, .RADIAN. ) );
#31866=AXIS2_PLACEMENT_3D ( 'NONE', #68839, #20637, #20278 ) ;
#31872=DIRECTION ( 'NONE',  ( 0.000000000000000000, -0.6691306063588591257, -0.7431448254773933559 ) ) ;
#31878=PRESENTATION_STYLE_ASSIGNMENT (( #21319 ) ) ;
#31884=AXIS2_PLACEMENT_3D ( 'NONE', #5171, #48139, #69546 ) ;
#31889=MECHANICAL_DESIGN_GEOMETRIC_PRESENTATION_REPRESENTATION('',(#57729),#63342);
#31891=CARTESIAN_POINT ( 'NONE',  ( 179.4361977533490347, 13.00000000000000178, -103.7004518695263044 ) ) ;
#31897=EDGE_LOOP ( 'NONE', ( #21548, #57322, #12364, #8708, #3092, #54894, #2695, #23211 ) ) ;
#31900=PRESENTATION_STYLE_ASSIGNMENT (( #27293 ) ) ;
#31903=LINE ( 'NONE', #42185, #4900 ) ;
#31921=DIRECTION ( 'NONE',  ( 1.000000000000000000, -0.000000000000000000, -0.000000000000000000 ) ) ;
#31934=ORIENTED_EDGE ( 'NONE', *, *, #62379, .T. ) ;
#31943=VECTOR ( 'NONE', #16651, 1000.000000000000000 ) ;
#31951=UNCERTAINTY_MEASURE_WITH_UNIT (LENGTH_MEASURE( 1.000000000000000082E-05 ), #5223, 'distance_accuracy_value', 'NONE');
#31957=CYLINDRICAL_SURFACE ( 'NONE', #22484, 1.000000000000000888 ) ;
#31958=LINE ( 'NONE', #5212, #22911 ) ;
#31963=AXIS2_PLACEMENT_3D ( 'NONE', #10017, #26168, #30388 ) ;
#31965=( NAMED_UNIT ( * ) PLANE_ANGLE_UNIT ( ) SI_UNIT ( $, .RADIAN. ) );
#31969=EDGE_LOOP ( 'NONE', ( #36865, #37660, #51495, #57725 ) ) ;
#31975=CYLINDRICAL_SURFACE ( 'NONE', #21215, 3.499999999999999556 ) ;
#31981=MECHANICAL_DESIGN_GEOMETRIC_PRESENTATION_REPRESENTATION('',(#29781),#55584);
#31982=EDGE_LOOP ( 'NONE', ( #46215, #52793, #66252, #43991 ) ) ;
#31986=CARTESIAN_POINT ( 'NONE',  ( 27.99999999999998934, 0.000000000000000000, 37.00402776293829987 ) ) ;
#31997=ORIENTED_EDGE ( 'NONE', *, *, #16324, .F. ) ;
#32000=CARTESIAN_POINT ( 'NONE',  ( 27.99999999999998224, 0.000000000000000000, 72.00402776293822171 ) ) ;
#32001=COLOUR_RGB ( '', 0.40784314, 0.44705882, 0.49803922) ;
#32004=PRESENTATION_STYLE_ASSIGNMENT (( #21807 ) ) ;
#32013=CARTESIAN_POINT ( 'NONE',  ( 57.00000000000000000, 15.00000000000000000, -34.49999999999999289 ) ) ;
#32014=DIRECTION ( 'NONE',  ( -0.000000000000000000, -1.000000000000000000, -0.000000000000000000 ) ) ;
#32018=DIRECTION ( 'NONE',  ( 1.000000000000000000, 0.000000000000000000, 0.000000000000000000 ) ) ;
#32020=( NAMED_UNIT ( * ) PLANE_ANGLE_UNIT ( ) SI_UNIT ( $, .RADIAN. ) );
#32023=EDGE_CURVE ( 'NONE', #19539, #2934, #65685, .T. ) ;
#32030=( BOUNDED_CURVE ( )  B_SPLINE_CURVE ( 3, ( #15402, #36861, #47792, #69194 ),
 .UNSPECIFIED., .F., .F. ) 
 B_SPLINE_CURVE_WITH_KNOTS ( ( 4, 4 ),
 ( -7.105427357601001859E-15, 1.570796326794896558 ),
 .UNSPECIFIED. ) 
 CURVE ( )  GEOMETRIC_REPRESENTATION_ITEM ( )  RATIONAL_B_SPLINE_CURVE ( ( 1.000000000000000000, 0.8047378541243632721, 0.8047378541243632721, 1.000000000000000000 ) ) 
 REPRESENTATION_ITEM ( '' )  );
#32034=SURFACE_STYLE_FILL_AREA ( #49606 ) ;
#32035=( NAMED_UNIT ( * ) SI_UNIT ( $, .STERADIAN. ) SOLID_ANGLE_UNIT ( ) );
#32043=STYLED_ITEM ( 'NONE', ( #58658 ), #8442 ) ;
#32058=CARTESIAN_POINT ( 'NONE',  ( 31.00000000000000000, 42.00000000000000000, -80.00402776293826435 ) ) ;
#32060=( NAMED_UNIT ( * ) PLANE_ANGLE_UNIT ( ) SI_UNIT ( $, .RADIAN. ) );
#32062=( NAMED_UNIT ( * ) SI_UNIT ( $, .STERADIAN. ) SOLID_ANGLE_UNIT ( ) );
#32065=( GEOMETRIC_REPRESENTATION_CONTEXT ( 3 ) GLOBAL_UNCERTAINTY_ASSIGNED_CONTEXT ( ( #14420 ) ) GLOBAL_UNIT_ASSIGNED_CONTEXT ( ( #12066, #59911, #33196 ) ) REPRESENTATION_CONTEXT ( 'NONE', 'WORKASPACE' ) );
#32067=SURFACE_SIDE_STYLE ('',( #10617 ) ) ;
#32071=SURFACE_STYLE_USAGE ( .BOTH. , #37401 ) ;
#32103=( NAMED_UNIT ( * ) SI_UNIT ( $, .STERADIAN. ) SOLID_ANGLE_UNIT ( ) );
#32104=VECTOR ( 'NONE', #35246, 1000.000000000000000 ) ;
#32118=FILL_AREA_STYLE ('',( #37454 ) ) ;
#32128=VERTEX_POINT ( 'NONE', #31501 ) ;
#32133=SURFACE_SIDE_STYLE ('',( #20892 ) ) ;
#32143=CARTESIAN_POINT ( 'NONE',  ( 108.3664351561509420, 13.00000000000000178, -18.43563588791578667 ) ) ;
#32147=CYLINDRICAL_SURFACE ( 'NONE', #3258, 12.50000000000001066 ) ;
#32150=DIRECTION ( 'NONE',  ( 0.000000000000000000, -0.000000000000000000, -1.000000000000000000 ) ) ;
#32151=DIRECTION ( 'NONE',  ( 0.000000000000000000, -1.000000000000000000, 0.000000000000000000 ) ) ;
#32162=( LENGTH_UNIT ( ) NAMED_UNIT ( * ) SI_UNIT ( .MILLI., .METRE. ) );
#32168=ORIENTED_EDGE ( 'NONE', *, *, #44979, .T. ) ;
#32169=SURFACE_STYLE_FILL_AREA ( #10715 ) ;
#32171=EDGE_LOOP ( 'NONE', ( #14196, #50183, #34641, #48498 ) ) ;
#32175=( NAMED_UNIT ( * ) PLANE_ANGLE_UNIT ( ) SI_UNIT ( $, .RADIAN. ) );
#32177=CARTESIAN_POINT ( 'NONE',  ( 31.00000000000001776, 50.00000000000000000, 59.99999999999999289 ) ) ;
#32189=EDGE_CURVE ( 'NONE', #29900, #23421, #14302, .T. ) ;
#32192=ORIENTED_EDGE ( 'NONE', *, *, #15964, .T. ) ;
#32194=UNCERTAINTY_MEASURE_WITH_UNIT (LENGTH_MEASURE( 1.000000000000000082E-05 ), #45735, 'distance_accuracy_value', 'NONE');
#32196=( NAMED_UNIT ( * ) SI_UNIT ( $, .STERADIAN. ) SOLID_ANGLE_UNIT ( ) );
#32199=SURFACE_STYLE_USAGE ( .BOTH. , #10412 ) ;
#32201=CARTESIAN_POINT ( 'NONE',  ( 23.50000000000001776, 42.00000000000000000, -29.68999999999999417 ) ) ;
#32205=ORIENTED_EDGE ( 'NONE', *, *, #33504, .F. ) ;
#32207=SURFACE_SIDE_STYLE ('',( #31849 ) ) ;
#32223=FILL_AREA_STYLE ('',( #15720 ) ) ;
#32225=ORIENTED_EDGE ( 'NONE', *, *, #16085, .F. ) ;
#32226=SURFACE_STYLE_FILL_AREA ( #12144 ) ;
#32242=STYLED_ITEM ( 'NONE', ( #9951 ), #3494 ) ;
#32243=SURFACE_STYLE_FILL_AREA ( #21328 ) ;
#32250=FILL_AREA_STYLE_COLOUR ( '', #33554 ) ;
#32258=CARTESIAN_POINT ( 'NONE',  ( 57.00000000000000000, 5.000000000000000000, 55.00402776293825724 ) ) ;
#32262=DIRECTION ( 'NONE',  ( 0.000000000000000000, 0.3420201433256629953, -0.9396926207859104263 ) ) ;
#32267=LINE ( 'NONE', #22407, #46722 ) ;
#32285=CIRCLE ( 'NONE', #4191, 2.500000000000002220 ) ;
#32293=FILL_AREA_STYLE_COLOUR ( '', #19181 ) ;
#32303=ORIENTED_EDGE ( 'NONE', *, *, #57243, .F. ) ;
#32314=EDGE_LOOP ( 'NONE', ( #18924, #6484, #33474, #16887 ) ) ;
#32323=CARTESIAN_POINT ( 'NONE',  ( 22.99999999999999289, 0.000000000000000000, -37.00402776293825013 ) ) ;
#32336=ORIENTED_EDGE ( 'NONE', *, *, #20827, .T. ) ;
#32350=( LENGTH_UNIT ( ) NAMED_UNIT ( * ) SI_UNIT ( .MILLI., .METRE. ) );
#32352=CARTESIAN_POINT ( 'NONE',  ( 36.00000000000002842, 5.000000000000000000, 29.00402776293825724 ) ) ;
#32365=DIRECTION ( 'NONE',  ( 1.000000000000000000, 0.000000000000000000, 0.000000000000000000 ) ) ;
#32366=CARTESIAN_POINT ( 'NONE',  ( 4.000000000000001776, 43.00000000000000000, -90.00000000000000000 ) ) ;
#32368=VERTEX_POINT ( 'NONE', #1529 ) ;
#32375=EDGE_LOOP ( 'NONE', ( #14, #54186 ) ) ;
#32380=DIRECTION ( 'NONE',  ( 0.000000000000000000, 0.000000000000000000, -1.000000000000000000 ) ) ;
#32383=FACE_OUTER_BOUND ( 'NONE', #1664, .T. ) ;
#32389=LINE ( 'NONE', #20830, #21983 ) ;
#32412=STYLED_ITEM ( 'NONE', ( #4488 ), #19990 ) ;
#32424=MECHANICAL_DESIGN_GEOMETRIC_PRESENTATION_REPRESENTATION('',(#13345),#24581);
#32425=AXIS2_PLACEMENT_3D ( 'NONE', #19025, #29242, #50723 ) ;
#32427=PRESENTATION_STYLE_ASSIGNMENT (( #64461 ) ) ;
#32430=DIRECTION ( 'NONE',  ( 0.000000000000000000, 0.000000000000000000, -1.000000000000000000 ) ) ;
#32435=ORIENTED_EDGE ( 'NONE', *, *, #13825, .T. ) ;
#32436=FILL_AREA_STYLE ('',( #387 ) ) ;
#32437=MECHANICAL_DESIGN_GEOMETRIC_PRESENTATION_REPRESENTATION('',(#5456),#29060);
#32450=VECTOR ( 'NONE', #10419, 1000.000000000000000 ) ;
#32452=CARTESIAN_POINT ( 'NONE',  ( 96.10348817448819148, 5.000000000000000000, 27.38099488609881149 ) ) ;
#32468=ORIENTED_EDGE ( 'NONE', *, *, #64937, .F. ) ;
#32477=ORIENTED_EDGE ( 'NONE', *, *, #44832, .F. ) ;
#32479=ADVANCED_FACE ( 'NONE', ( #13873, #63451 ), #57840, .T. ) ;
#32482=DIRECTION ( 'NONE',  ( 0.000000000000000000, 1.000000000000000000, 0.000000000000000000 ) ) ;
#32483=ORIENTED_EDGE ( 'NONE', *, *, #10985, .T. ) ;
#32500=DIRECTION ( 'NONE',  ( -0.000000000000000000, -0.000000000000000000, 1.000000000000000000 ) ) ;
#32512=EDGE_CURVE ( 'NONE', #49909, #52976, #48946, .T. ) ;
#32513=( GEOMETRIC_REPRESENTATION_CONTEXT ( 3 ) GLOBAL_UNCERTAINTY_ASSIGNED_CONTEXT ( ( #10218 ) ) GLOBAL_UNIT_ASSIGNED_CONTEXT ( ( #37828, #27867, #33195 ) ) REPRESENTATION_CONTEXT ( 'NONE', 'WORKASPACE' ) );
#32515=EDGE_LOOP ( 'NONE', ( #64371, #27027 ) ) ;
#32523=CARTESIAN_POINT ( 'NONE',  ( 3.000000000000002665, 34.80256050929376954, -80.00402776293826435 ) ) ;
#32529=AXIS2_PLACEMENT_3D ( 'NONE', #16668, #49038, #46717 ) ;
#32533=UNCERTAINTY_MEASURE_WITH_UNIT (LENGTH_MEASURE( 1.000000000000000082E-05 ), #2335, 'distance_accuracy_value', 'NONE');
#32549=( NAMED_UNIT ( * ) SI_UNIT ( $, .STERADIAN. ) SOLID_ANGLE_UNIT ( ) );
#32551=ORIENTED_EDGE ( 'NONE', *, *, #57573, .F. ) ;
#32555=EDGE_LOOP ( 'NONE', ( #63977, #58234, #18506, #12120 ) ) ;
#32556=( NAMED_UNIT ( * ) PLANE_ANGLE_UNIT ( ) SI_UNIT ( $, .RADIAN. ) );
#32560=EDGE_CURVE ( 'NONE', #35304, #54767, #20887, .T. ) ;
#32564=EDGE_LOOP ( 'NONE', ( #35203, #27639, #58063 ) ) ;
#32565=CARTESIAN_POINT ( 'NONE',  ( 28.00000000000000000, 0.000000000000000000, -89.00000000000000000 ) ) ;
#32585=EDGE_LOOP ( 'NONE', ( #12086, #37257, #40743 ) ) ;
#32586=SURFACE_SIDE_STYLE ('',( #15760 ) ) ;
#32593=AXIS2_PLACEMENT_3D ( 'NONE', #26985, #10160, #31594 ) ;
#32597=EDGE_LOOP ( 'NONE', ( #66621, #56354, #31708, #21452 ) ) ;
#32607=( GEOMETRIC_REPRESENTATION_CONTEXT ( 3 ) GLOBAL_UNCERTAINTY_ASSIGNED_CONTEXT ( ( #56672 ) ) GLOBAL_UNIT_ASSIGNED_CONTEXT ( ( #53806, #20064, #4937 ) ) REPRESENTATION_CONTEXT ( 'NONE', 'WORKASPACE' ) );
#32618=DIRECTION ( 'NONE',  ( 0.000000000000000000, 0.000000000000000000, 1.000000000000000000 ) ) ;
#32621=EDGE_CURVE ( 'NONE', #39245, #42967, #11011, .T. ) ;
#32628=UNCERTAINTY_MEASURE_WITH_UNIT (LENGTH_MEASURE( 1.000000000000000082E-05 ), #1515, 'distance_accuracy_value', 'NONE');
#32629=MECHANICAL_DESIGN_GEOMETRIC_PRESENTATION_REPRESENTATION('',(#40515),#26988);
#32635=STYLED_ITEM ( 'NONE', ( #34618 ), #34624 ) ;
#32637=EDGE_CURVE ( 'NONE', #65035, #11384, #29861, .T. ) ;
#32648=AXIS2_PLACEMENT_3D ( 'NONE', #61857, #24563, #24922 ) ;
#32667=LINE ( 'NONE', #59385, #8608 ) ;
#32669=DIRECTION ( 'NONE',  ( 0.000000000000000000, 0.000000000000000000, 1.000000000000000000 ) ) ;
#32671=ORIENTED_EDGE ( 'NONE', *, *, #16237, .F. ) ;
#32687=UNCERTAINTY_MEASURE_WITH_UNIT (LENGTH_MEASURE( 1.000000000000000082E-05 ), #24936, 'distance_accuracy_value', 'NONE');
#32698=SURFACE_STYLE_USAGE ( .BOTH. , #12623 ) ;
#32700=SURFACE_STYLE_FILL_AREA ( #48940 ) ;
#32710=( NAMED_UNIT ( * ) PLANE_ANGLE_UNIT ( ) SI_UNIT ( $, .RADIAN. ) );
#32714=DIRECTION ( 'NONE',  ( 0.000000000000000000, 0.000000000000000000, 1.000000000000000000 ) ) ;
#32715=MECHANICAL_DESIGN_GEOMETRIC_PRESENTATION_REPRESENTATION('',(#7966),#17755);
#32721=CARTESIAN_POINT ( 'NONE',  ( 3.000000000000030198, 37.76051491742381216, 89.34202014332566932 ) ) ;
#32723=CARTESIAN_POINT ( 'NONE',  ( 3.000000000000002665, 42.58578643762690064, -89.58578643762690774 ) ) ;
#32724=UNCERTAINTY_MEASURE_WITH_UNIT (LENGTH_MEASURE( 1.000000000000000082E-05 ), #37859, 'distance_accuracy_value', 'NONE');
#32726=DIRECTION ( 'NONE',  ( 0.7681514953298231863, 0.000000000000000000, 0.6402681315062906942 ) ) ;
#32727=EDGE_LOOP ( 'NONE', ( #64411, #56637, #20992, #62269, #37587 ) ) ;
#32743=DIRECTION ( 'NONE',  ( -1.000000000000000000, 0.000000000000000000, -0.000000000000000000 ) ) ;
#32754=ORIENTED_EDGE ( 'NONE', *, *, #57522, .T. ) ;
#32755=DIRECTION ( 'NONE',  ( 0.000000000000000000, 0.000000000000000000, -1.000000000000000000 ) ) ;
#32759=CARTESIAN_POINT ( 'NONE',  ( 0.4644249260832968851, 42.85561104658234655, -74.47757702770792321 ) ) ;
#32760=ORIENTED_EDGE ( 'NONE', *, *, #7469, .T. ) ;
#32761=( GEOMETRIC_REPRESENTATION_CONTEXT ( 3 ) GLOBAL_UNCERTAINTY_ASSIGNED_CONTEXT ( ( #38914 ) ) GLOBAL_UNIT_ASSIGNED_CONTEXT ( ( #19441, #40231, #13826 ) ) REPRESENTATION_CONTEXT ( 'NONE', 'WORKASPACE' ) );
#32762=DIRECTION ( 'NONE',  ( 0.000000000000000000, -0.000000000000000000, -1.000000000000000000 ) ) ;
#32772=UNCERTAINTY_MEASURE_WITH_UNIT (LENGTH_MEASURE( 1.000000000000000082E-05 ), #62827, 'distance_accuracy_value', 'NONE');
#32773=CYLINDRICAL_SURFACE ( 'NONE', #19839, 12.50000000000001066 ) ;
#32784=ORIENTED_EDGE ( 'NONE', *, *, #19378, .F. ) ;
#32791=CARTESIAN_POINT ( 'NONE',  ( 10.00000000000001954, 42.00000000000000000, -29.68999999999999417 ) ) ;
#32798=( GEOMETRIC_REPRESENTATION_CONTEXT ( 3 ) GLOBAL_UNCERTAINTY_ASSIGNED_CONTEXT ( ( #61607 ) ) GLOBAL_UNIT_ASSIGNED_CONTEXT ( ( #37077, #59159, #32103 ) ) REPRESENTATION_CONTEXT ( 'NONE', 'WORKASPACE' ) );
#32799=ADVANCED_FACE ( 'NONE', ( #29256 ), #1792, .F. ) ;
#32805=LINE ( 'NONE', #59170, #60562 ) ;
#32826=ORIENTED_EDGE ( 'NONE', *, *, #50271, .F. ) ;
#32829=ORIENTED_EDGE ( 'NONE', *, *, #34384, .F. ) ;
#32851=CARTESIAN_POINT ( 'NONE',  ( 74.89452121010485541, 0.000000000000000000, 66.39042820928573008 ) ) ;
#32853=UNCERTAINTY_MEASURE_WITH_UNIT (LENGTH_MEASURE( 1.000000000000000082E-05 ), #15428, 'distance_accuracy_value', 'NONE');
#32855=DIRECTION ( 'NONE',  ( 0.000000000000000000, 0.000000000000000000, -1.000000000000000000 ) ) ;
#32861=ORIENTED_EDGE ( 'NONE', *, *, #34384, .T. ) ;
#32863=COLOUR_RGB ( '', 0.31764706, 0.68627451, 0.89019608) ;
#32864=PLANE ( 'NONE',  #34015 ) ;
#32873=FILL_AREA_STYLE ('',( #65215 ) ) ;
#32881=SURFACE_STYLE_FILL_AREA ( #59942 ) ;
#32886=SURFACE_STYLE_FILL_AREA ( #11413 ) ;
#32894=DIRECTION ( 'NONE',  ( 1.000000000000000000, 0.000000000000000000, 0.000000000000000000 ) ) ;
#32896=FACE_OUTER_BOUND ( 'NONE', #62796, .T. ) ;
#32898=FACE_BOUND ( 'NONE', #37604, .T. ) ;
#32906=CARTESIAN_POINT ( 'NONE',  ( 7.000000000000017764, 42.25685517452260598, -28.66913060635885913 ) ) ;
#32911=EDGE_LOOP ( 'NONE', ( #20031, #59310, #64261, #68924 ) ) ;
#32926=( NAMED_UNIT ( * ) SI_UNIT ( $, .STERADIAN. ) SOLID_ANGLE_UNIT ( ) );
#32933=AXIS2_PLACEMENT_3D ( 'NONE', #4200, #35904, #42282 ) ;
#32935=AXIS2_PLACEMENT_3D ( 'NONE', #64356, #26695, #48569 ) ;
#32936=LINE ( 'NONE', #49813, #13630 ) ;
#32950=ORIENTED_EDGE ( 'NONE', *, *, #21464, .T. ) ;
#32955=EDGE_LOOP ( 'NONE', ( #20561, #40215, #32671, #39324 ) ) ;
#32961=DIRECTION ( 'NONE',  ( 0.000000000000000000, -1.000000000000000000, 0.000000000000000000 ) ) ;
#32971=EDGE_CURVE ( 'NONE', #11604, #5288, #12326, .T. ) ;
#32988=EDGE_CURVE ( 'NONE', #20378, #11058, #25381, .T. ) ;
#32990=( GEOMETRIC_REPRESENTATION_CONTEXT ( 3 ) GLOBAL_UNCERTAINTY_ASSIGNED_CONTEXT ( ( #15251 ) ) GLOBAL_UNIT_ASSIGNED_CONTEXT ( ( #14851, #4967, #31697 ) ) REPRESENTATION_CONTEXT ( 'NONE', 'WORKASPACE' ) );
#32993=CARTESIAN_POINT ( 'NONE',  ( 24.58198306468035099, 25.31001116168506471, 27.43556691332571873 ) ) ;
#32996=SURFACE_STYLE_FILL_AREA ( #48517 ) ;
#33020=ORIENTED_EDGE ( 'NONE', *, *, #58546, .T. ) ;
#33021=FILL_AREA_STYLE_COLOUR ( '', #60226 ) ;
#33022=COLOUR_RGB ( '', 0.66274510, 0.83137255, 0.94901961) ;
#33025=CARTESIAN_POINT ( 'NONE',  ( 26.00000000000001776, 42.00000000000000000, -35.50000000000000000 ) ) ;
#33034=DIRECTION ( 'NONE',  ( -0.000000000000000000, -1.000000000000000000, -0.000000000000000000 ) ) ;
#33042=CARTESIAN_POINT ( 'NONE',  ( 26.00000000000001776, 15.00000000000000000, 29.68999999999999417 ) ) ;
#33047=ORIENTED_EDGE ( 'NONE', *, *, #39178, .F. ) ;
#33052=MECHANICAL_DESIGN_GEOMETRIC_PRESENTATION_REPRESENTATION('',(#24054),#35313);
#33069=CARTESIAN_POINT ( 'NONE',  ( 0.000000000000000000, 14.00000000000000000, 80.00402776293826435 ) ) ;
#33070=CARTESIAN_POINT ( 'NONE',  ( 32.00000000000000000, 43.00000000000000000, -79.00402776293826435 ) ) ;
#33071=EDGE_CURVE ( 'NONE', #18094, #50964, #43871, .T. ) ;
#33076=FILL_AREA_STYLE ('',( #11607 ) ) ;
#33097=CYLINDRICAL_SURFACE ( 'NONE', #51904, 1.000000000000000000 ) ;
#33100=CARTESIAN_POINT ( 'NONE',  ( 29.00000000000002842, 5.569094604152796002, -2.026984667724097466 ) ) ;
#33105=( NAMED_UNIT ( * ) PLANE_ANGLE_UNIT ( ) SI_UNIT ( $, .RADIAN. ) );
#33106=LINE ( 'NONE', #59826, #9510 ) ;
#33110=VERTEX_POINT ( 'NONE', #59352 ) ;
#33124=SURFACE_SIDE_STYLE ('',( #343 ) ) ;
#33136=CARTESIAN_POINT ( 'NONE',  ( 11.00000000000001776, 26.00000000000000355, 20.49999999999999645 ) ) ;
#33178=CARTESIAN_POINT ( 'NONE',  ( 2.000000000000008882, 50.00000000000000000, -59.99999999999999289 ) ) ;
#33185=TOROIDAL_SURFACE ( 'NONE', #8497, 3.499999999999998668, 1.000000000000000000 ) ;
#33186=CARTESIAN_POINT ( 'NONE',  ( 27.99999999999999645, 5.000000000000000000, -72.00402776293822171 ) ) ;
#33191=CARTESIAN_POINT ( 'NONE',  ( 30.99999999999999289, 5.000000000000000000, 24.00402776293822171 ) ) ;
#33195=( NAMED_UNIT ( * ) SI_UNIT ( $, .STERADIAN. ) SOLID_ANGLE_UNIT ( ) );
#33196=( NAMED_UNIT ( * ) SI_UNIT ( $, .STERADIAN. ) SOLID_ANGLE_UNIT ( ) );
#33205=PRESENTATION_STYLE_ASSIGNMENT (( #55337 ) ) ;
#33219=( NAMED_UNIT ( * ) PLANE_ANGLE_UNIT ( ) SI_UNIT ( $, .RADIAN. ) );
#33236=FACE_OUTER_BOUND ( 'NONE', #56311, .T. ) ;
#33250=TOROIDAL_SURFACE ( 'NONE', #1763, 17.00000000000000355, 1.000000000000000000 ) ;
#33252=CARTESIAN_POINT ( 'NONE',  ( 0.000000000000000000, 43.00000000000000000, 0.000000000000000000 ) ) ;
#33268=( LENGTH_UNIT ( ) NAMED_UNIT ( * ) SI_UNIT ( .MILLI., .METRE. ) );
#33269=CYLINDRICAL_SURFACE ( 'NONE', #7770, 1.000000000000000888 ) ;
#33271=( NAMED_UNIT ( * ) SI_UNIT ( $, .STERADIAN. ) SOLID_ANGLE_UNIT ( ) );
#33276=ORIENTED_EDGE ( 'NONE', *, *, #2902, .F. ) ;
#33277=SURFACE_SIDE_STYLE ('',( #32226 ) ) ;
#33287=FILL_AREA_STYLE ('',( #43878 ) ) ;
#33296=LINE ( 'NONE', #1901, #69325 ) ;
#33299=UNCERTAINTY_MEASURE_WITH_UNIT (LENGTH_MEASURE( 1.000000000000000082E-05 ), #65731, 'distance_accuracy_value', 'NONE');
#33304=EDGE_CURVE ( 'NONE', #22147, #25561, #20979, .T. ) ;
#33306=ORIENTED_EDGE ( 'NONE', *, *, #21368, .T. ) ;
#33311=LINE ( 'NONE', #854, #14453 ) ;
#33319=DIRECTION ( 'NONE',  ( -0.000000000000000000, -1.000000000000000000, -0.000000000000000000 ) ) ;
#33334=DIRECTION ( 'NONE',  ( 0.000000000000000000, 0.000000000000000000, -1.000000000000000000 ) ) ;
#33336=AXIS2_PLACEMENT_3D ( 'NONE', #38533, #26843, #64164 ) ;
#33348=MECHANICAL_DESIGN_GEOMETRIC_PRESENTATION_REPRESENTATION('',(#32242),#44638);
#33355=ADVANCED_FACE ( 'NONE', ( #14668 ), #62489, .F. ) ;
#33364=SURFACE_STYLE_USAGE ( .BOTH. , #11551 ) ;
#33372=DIRECTION ( 'NONE',  ( -0.000000000000000000, -0.000000000000000000, -1.000000000000000000 ) ) ;
#33374=VERTEX_POINT ( 'NONE', #42474 ) ;
#33379=VERTEX_POINT ( 'NONE', #20632 ) ;
#33398=ORIENTED_EDGE ( 'NONE', *, *, #29458, .F. ) ;
#33400=SURFACE_SIDE_STYLE ('',( #17598 ) ) ;
#33409=ORIENTED_EDGE ( 'NONE', *, *, #55351, .T. ) ;
#33429=ADVANCED_FACE ( 'NONE', ( #69504 ), #33269, .T. ) ;
#33430=EDGE_CURVE ( 'NONE', #5489, #59091, #18020, .T. ) ;
#33431=CARTESIAN_POINT ( 'NONE',  ( 10.00000000000001954, 50.00000000000000000, 46.00000000000000000 ) ) ;
#33441=SPHERICAL_SURFACE ( 'NONE', #437, 1.000000000000000000 ) ;
#33451=EDGE_CURVE ( 'NONE', #18424, #56002, #1126, .T. ) ;
#33464=ORIENTED_EDGE ( 'NONE', *, *, #56199, .F. ) ;
#33467=UNCERTAINTY_MEASURE_WITH_UNIT (LENGTH_MEASURE( 1.000000000000000082E-05 ), #55590, 'distance_accuracy_value', 'NONE');
#33468=AXIS2_PLACEMENT_3D ( 'NONE', #8259, #24076, #8601 ) ;
#33474=ORIENTED_EDGE ( 'NONE', *, *, #21944, .F. ) ;
#33480=CARTESIAN_POINT ( 'NONE',  ( 28.00000000000002132, 43.00000000000000000, 90.00000000000000000 ) ) ;
#33485=ORIENTED_EDGE ( 'NONE', *, *, #9062, .F. ) ;
#33492=ORIENTED_EDGE ( 'NONE', *, *, #55595, .F. ) ;
#33498=DIRECTION ( 'NONE',  ( 0.000000000000000000, 0.000000000000000000, -1.000000000000000000 ) ) ;
#33504=EDGE_CURVE ( 'NONE', #40178, #52535, #14666, .T. ) ;
#33518=DIRECTION ( 'NONE',  ( 0.000000000000000000, 0.000000000000000000, 1.000000000000000000 ) ) ;
#33522=PRESENTATION_STYLE_ASSIGNMENT (( #44131 ) ) ;
#33526=AXIS2_PLACEMENT_3D ( 'NONE', #57626, #25588, #62876 ) ;
#33527=ORIENTED_EDGE ( 'NONE', *, *, #50524, .F. ) ;
#33538=UNCERTAINTY_MEASURE_WITH_UNIT (LENGTH_MEASURE( 1.000000000000000082E-05 ), #49740, 'distance_accuracy_value', 'NONE');
#33541=COLOUR_RGB ( '', 0.72549020, 0.75294118, 0.79215686) ;
#33545=CYLINDRICAL_SURFACE ( 'NONE', #49711, 0.9999999999999974465 ) ;
#33554=COLOUR_RGB ( '', 0.66274510, 0.83137255, 0.94901961) ;
#33562=ORIENTED_EDGE ( 'NONE', *, *, #25271, .F. ) ;
#33568=CARTESIAN_POINT ( 'NONE',  ( 2.000000000000023093, 50.00000000000000000, 65.00000000000000000 ) ) ;
#33575=AXIS2_PLACEMENT_3D ( 'NONE', #22329, #63840, #15686 ) ;
#33580=FACE_OUTER_BOUND ( 'NONE', #53799, .T. ) ;
#33588=ADVANCED_FACE ( 'NONE', ( #51514 ), #47328, .F. ) ;
#33591=FILL_AREA_STYLE_COLOUR ( '', #34907 ) ;
#33594=DIRECTION ( 'NONE',  ( 1.000000000000000000, 0.000000000000000000, 0.000000000000000000 ) ) ;
#33600=STYLED_ITEM ( 'NONE', ( #34782 ), #19852 ) ;
#33607=DIRECTION ( 'NONE',  ( 0.000000000000000000, 0.000000000000000000, -1.000000000000000000 ) ) ;
#33616=CIRCLE ( 'NONE', #42656, 2.000000000000001776 ) ;
#33617=EDGE_LOOP ( 'NONE', ( #5114, #64421, #32826, #37947 ) ) ;
#33625=ADVANCED_FACE ( 'NONE', ( #26159 ), #36775, .F. ) ;
#33647=DIRECTION ( 'NONE',  ( -0.000000000000000000, 1.000000000000000000, -0.000000000000000000 ) ) ;
#33648=LINE ( 'NONE', #59680, #7046 ) ;
#33677=CYLINDRICAL_SURFACE ( 'NONE', #34855, 1.000000000000000888 ) ;
#33679=EDGE_CURVE ( 'NONE', #57515, #17308, #23531, .T. ) ;
#33686=CARTESIAN_POINT ( 'NONE',  ( 22.99999999999995381, 0.000000000000000000, 32.00402776293825724 ) ) ;
#33690=AXIS2_PLACEMENT_3D ( 'NONE', #28464, #2385, #11623 ) ;
#33702=DIRECTION ( 'NONE',  ( 0.000000000000000000, 0.000000000000000000, 1.000000000000000000 ) ) ;
#33703=PRESENTATION_STYLE_ASSIGNMENT (( #37666 ) ) ;
#33722=FILL_AREA_STYLE ('',( #55879 ) ) ;
#33728=ORIENTED_EDGE ( 'NONE', *, *, #63830, .F. ) ;
#33738=PRESENTATION_STYLE_ASSIGNMENT (( #50973 ) ) ;
#33746=SURFACE_STYLE_USAGE ( .BOTH. , #44366 ) ;
#33749=SURFACE_STYLE_USAGE ( .BOTH. , #66100 ) ;
#33752=EDGE_CURVE ( 'NONE', #49909, #60879, #5537, .T. ) ;
#33756=EDGE_CURVE ( 'NONE', #1567, #27344, #49363, .T. ) ;
#33761=SURFACE_SIDE_STYLE ('',( #980 ) ) ;
#33769=DIRECTION ( 'NONE',  ( -0.000000000000000000, -1.000000000000000000, -0.000000000000000000 ) ) ;
#33773=ORIENTED_EDGE ( 'NONE', *, *, #67119, .T. ) ;
#33776=MECHANICAL_DESIGN_GEOMETRIC_PRESENTATION_REPRESENTATION('',(#67473),#9096);
#33782=ORIENTED_EDGE ( 'NONE', *, *, #40301, .F. ) ;
#33783=ORIENTED_EDGE ( 'NONE', *, *, #28980, .T. ) ;
#33785=DIRECTION ( 'NONE',  ( 0.000000000000000000, -0.000000000000000000, -1.000000000000000000 ) ) ;
#33789=CARTESIAN_POINT ( 'NONE',  ( 22.00000000000002132, 43.00000000000000000, 29.68999999999999417 ) ) ;
#33802=CARTESIAN_POINT ( 'NONE',  ( 179.4361977533476136, 5.000000000000000000, 103.7004518695250823 ) ) ;
#33810=MECHANICAL_DESIGN_GEOMETRIC_PRESENTATION_REPRESENTATION('',(#67505),#50643);
#33813=CARTESIAN_POINT ( 'NONE',  ( 22.99999999999996447, 0.000000000000000000, -29.00402776293825369 ) ) ;
#33814=AXIS2_PLACEMENT_3D ( 'NONE', #64240, #53016, #53686 ) ;
#33815=COLOUR_RGB ( '', 0.66274510, 0.83137255, 0.94901961) ;
#33835=MECHANICAL_DESIGN_GEOMETRIC_PRESENTATION_REPRESENTATION('',(#47348),#52942);
#33851=DIRECTION ( 'NONE',  ( 0.000000000000000000, 0.000000000000000000, 1.000000000000000000 ) ) ;
#33862=DIRECTION ( 'NONE',  ( -0.000000000000000000, -1.000000000000000000, -0.000000000000000000 ) ) ;
#33867=ORIENTED_EDGE ( 'NONE', *, *, #40101, .F. ) ;
#33868=DIRECTION ( 'NONE',  ( 1.000000000000000000, 0.000000000000000000, -1.300977106640435137E-16 ) ) ;
#33874=( NAMED_UNIT ( * ) PLANE_ANGLE_UNIT ( ) SI_UNIT ( $, .RADIAN. ) );
#33875=CARTESIAN_POINT ( 'NONE',  ( 73.01088739851485343, 5.000000000000000000, 65.71817553072288831 ) ) ;
#33886=CARTESIAN_POINT ( 'NONE',  ( 22.00000000000002132, 43.00000000000000000, 90.00000000000000000 ) ) ;
#33888=VERTEX_POINT ( 'NONE', #23313 ) ;
#33895=DIRECTION ( 'NONE',  ( 0.000000000000000000, 0.000000000000000000, -1.000000000000000000 ) ) ;
#33912=CARTESIAN_POINT ( 'NONE',  ( 30.99999999999999289, 5.000000000000000000, -37.00402776293829277 ) ) ;
#33917=DIRECTION ( 'NONE',  ( -0.000000000000000000, -1.000000000000000000, 0.000000000000000000 ) ) ;
#33932=COLOUR_RGB ( '', 0.66274510, 0.83137255, 0.94901961) ;
#33933=CARTESIAN_POINT ( 'NONE',  ( 11.00000000000001776, 16.44305403005404287, 6.465863758942333782E-16 ) ) ;
#33948=VERTEX_POINT ( 'NONE', #18727 ) ;
#33949=SURFACE_SIDE_STYLE ('',( #23070 ) ) ;
#33955=MECHANICAL_DESIGN_GEOMETRIC_PRESENTATION_REPRESENTATION('',(#8172),#10432);
#33956=FILL_AREA_STYLE_COLOUR ( '', #28173 ) ;
#33963=VERTEX_POINT ( 'NONE', #34553 ) ;
#33975=( NAMED_UNIT ( * ) PLANE_ANGLE_UNIT ( ) SI_UNIT ( $, .RADIAN. ) );
#33982=ORIENTED_EDGE ( 'NONE', *, *, #28062, .T. ) ;
#33995=DIRECTION ( 'NONE',  ( 0.000000000000000000, 0.000000000000000000, -1.000000000000000000 ) ) ;
#34000=( NAMED_UNIT ( * ) SI_UNIT ( $, .STERADIAN. ) SOLID_ANGLE_UNIT ( ) );
#34014=DIRECTION ( 'NONE',  ( 0.000000000000000000, -1.000000000000000000, 0.000000000000000000 ) ) ;
#34015=AXIS2_PLACEMENT_3D ( 'NONE', #13832, #60959, #51462 ) ;
#34016=SURFACE_SIDE_STYLE ('',( #22426 ) ) ;
#34022=CIRCLE ( 'NONE', #3659, 2.499999999999998668 ) ;
#34024=EDGE_CURVE ( 'NONE', #1286, #66425, #56160, .T. ) ;
#34027=( NAMED_UNIT ( * ) PLANE_ANGLE_UNIT ( ) SI_UNIT ( $, .RADIAN. ) );
#34035=CARTESIAN_POINT ( 'NONE',  ( 32.00000000000001421, 42.00000000000000000, 36.49999999999999289 ) ) ;
#34038=CARTESIAN_POINT ( 'NONE',  ( 0.000000000000000000, 13.00000000000000178, -36.49999999999999289 ) ) ;
#34039=CARTESIAN_POINT ( 'NONE',  ( 36.00000000000002842, 5.000000000000000000, -29.00402776293825724 ) ) ;
#34044=ORIENTED_EDGE ( 'NONE', *, *, #40221, .F. ) ;
#34047=SURFACE_STYLE_FILL_AREA ( #66047 ) ;
#34048=EDGE_LOOP ( 'NONE', ( #17865, #26911, #12214, #54800 ) ) ;
#34059=SURFACE_STYLE_USAGE ( .BOTH. , #12590 ) ;
#34074=FILL_AREA_STYLE ('',( #18604 ) ) ;
#34079=DIRECTION ( 'NONE',  ( 0.000000000000000000, 1.000000000000000000, 0.000000000000000000 ) ) ;
#34100=AXIS2_PLACEMENT_3D ( 'NONE', #6183, #5132, #38238 ) ;
#34102=( LENGTH_UNIT ( ) NAMED_UNIT ( * ) SI_UNIT ( .MILLI., .METRE. ) );
#34109=STYLED_ITEM ( 'NONE', ( #63638 ), #61675 ) ;
#34116=VERTEX_POINT ( 'NONE', #57768 ) ;
#34120=( NAMED_UNIT ( * ) SI_UNIT ( $, .STERADIAN. ) SOLID_ANGLE_UNIT ( ) );
#34123=ORIENTED_EDGE ( 'NONE', *, *, #20567, .T. ) ;
#34140=CARTESIAN_POINT ( 'NONE',  ( 16.00000000000001776, 43.00000000000000000, 29.68999999999999417 ) ) ;
#34141=VERTEX_POINT ( 'NONE', #9594 ) ;
#34147=SURFACE_SIDE_STYLE ('',( #7429 ) ) ;
#34150=AXIS2_PLACEMENT_3D ( 'NONE', #64173, #47012, #26189 ) ;
#34151=PRESENTATION_STYLE_ASSIGNMENT (( #18985 ) ) ;
#34158=UNCERTAINTY_MEASURE_WITH_UNIT (LENGTH_MEASURE( 1.000000000000000082E-05 ), #46903, 'distance_accuracy_value', 'NONE');
#34159=EDGE_CURVE ( 'NONE', #53011, #37678, #13485, .T. ) ;
#34161=CIRCLE ( 'NONE', #66695, 1.000000000000000888 ) ;
#34162=SURFACE_STYLE_USAGE ( .BOTH. , #12690 ) ;
#34169=( NAMED_UNIT ( * ) PLANE_ANGLE_UNIT ( ) SI_UNIT ( $, .RADIAN. ) );
#34175=ADVANCED_FACE ( 'NONE', ( #42654 ), #31705, .T. ) ;
#34183=ORIENTED_EDGE ( 'NONE', *, *, #51331, .F. ) ;
#34185=( NAMED_UNIT ( * ) SI_UNIT ( $, .STERADIAN. ) SOLID_ANGLE_UNIT ( ) );
#34188=VERTEX_POINT ( 'NONE', #64764 ) ;
#34211=COLOUR_RGB ( '', 0.31764706, 0.68627451, 0.89019608) ;
#34224=ORIENTED_EDGE ( 'NONE', *, *, #25336, .F. ) ;
#34226=FILL_AREA_STYLE_COLOUR ( '', #64606 ) ;
#34227=EDGE_CURVE ( 'NONE', #1278, #48365, #42329, .T. ) ;
#34229=FACE_OUTER_BOUND ( 'NONE', #62981, .T. ) ;
#34236=COLOUR_RGB ( '', 0.31764706, 0.68627451, 0.89019608) ;
#34243=ADVANCED_FACE ( 'NONE', ( #43012 ), #54542, .T. ) ;
#34250=SURFACE_STYLE_FILL_AREA ( #13470 ) ;
#34253=DIRECTION ( 'NONE',  ( 0.000000000000000000, 1.000000000000000000, -0.000000000000000000 ) ) ;
#34270=DIRECTION ( 'NONE',  ( 0.000000000000000000, 0.000000000000000000, -1.000000000000000000 ) ) ;
#34273=DIRECTION ( 'NONE',  ( 2.168404344971007882E-16, 0.000000000000000000, 1.000000000000000000 ) ) ;
#34275=FACE_OUTER_BOUND ( 'NONE', #32585, .T. ) ;
#34288=DIRECTION ( 'NONE',  ( 1.000000000000000000, 0.000000000000000000, -1.300977106640434891E-16 ) ) ;
#34291=( NAMED_UNIT ( * ) PLANE_ANGLE_UNIT ( ) SI_UNIT ( $, .RADIAN. ) );
#34292=CARTESIAN_POINT ( 'NONE',  ( 27.00000000000001776, 15.00000000000000000, 34.49999999999999289 ) ) ;
#34299=SURFACE_SIDE_STYLE ('',( #61363 ) ) ;
#34307=MECHANICAL_DESIGN_GEOMETRIC_PRESENTATION_REPRESENTATION('',(#44457),#46718);
#34313=ORIENTED_EDGE ( 'NONE', *, *, #12952, .T. ) ;
#34325=DIRECTION ( 'NONE',  ( 0.000000000000000000, 0.000000000000000000, 1.000000000000000000 ) ) ;
#34326=CARTESIAN_POINT ( 'NONE',  ( 7.000000000000017764, 42.74314482547740113, 27.71473342867655987 ) ) ;
#34332=DIRECTION ( 'NONE',  ( 1.000000000000000000, -0.000000000000000000, 0.000000000000000000 ) ) ;
#34334=AXIS2_PLACEMENT_3D ( 'NONE', #15628, #5719, #15987 ) ;
#34342=CARTESIAN_POINT ( 'NONE',  ( 93.00000000000000000, 0.9999999999999991118, 0.000000000000000000 ) ) ;
#34349=VECTOR ( 'NONE', #64560, 1000.000000000000000 ) ;
#34353=CARTESIAN_POINT ( 'NONE',  ( 0.4644257559287154891, 42.85561152959480324, 45.52242327283500600 ) ) ;
#34371=( NAMED_UNIT ( * ) PLANE_ANGLE_UNIT ( ) SI_UNIT ( $, .RADIAN. ) );
#34375=CARTESIAN_POINT ( 'NONE',  ( 27.99999999999998934, 5.000000000000000000, -37.00402776293828566 ) ) ;
#34376=VECTOR ( 'NONE', #57088, 1000.000000000000000 ) ;
#34377=CARTESIAN_POINT ( 'NONE',  ( 29.00000000000002842, 42.00000000000000000, 80.00402776293826435 ) ) ;
#34379=EDGE_CURVE ( 'NONE', #35471, #16364, #35171, .T. ) ;
#34384=EDGE_CURVE ( 'NONE', #65503, #39245, #64009, .T. ) ;
#34385=CARTESIAN_POINT ( 'NONE',  ( 3.000000000000002665, 38.70020753820971748, -89.00000000000000000 ) ) ;
#34401=ORIENTED_EDGE ( 'NONE', *, *, #57909, .T. ) ;
#34402=COLOUR_RGB ( '', 0.31764706, 0.68627451, 0.89019608) ;
#34413=FACE_OUTER_BOUND ( 'NONE', #8029, .T. ) ;
#34414=AXIS2_PLACEMENT_3D ( 'NONE', #55427, #7250, #51204 ) ;
#34417=CARTESIAN_POINT ( 'NONE',  ( 98.00000000000000000, 16.00000000000000000, 0.000000000000000000 ) ) ;
#34428=DIRECTION ( 'NONE',  ( 0.000000000000000000, -0.6691306063588591257, -0.7431448254773933559 ) ) ;
#34436=EDGE_LOOP ( 'NONE', ( #47895, #47984, #7329, #31015, #42290, #66940 ) ) ;
#34448=SURFACE_SIDE_STYLE ('',( #56601 ) ) ;
#34449=DIRECTION ( 'NONE',  ( 1.000000000000000000, 0.000000000000000000, 0.000000000000000000 ) ) ;
#34455=CYLINDRICAL_SURFACE ( 'NONE', #431, 1.000000000000000888 ) ;
#34464=CARTESIAN_POINT ( 'NONE',  ( 32.00000000000000711, 42.00000000000000000, -45.00000000000000000 ) ) ;
#34480=ORIENTED_EDGE ( 'NONE', *, *, #44972, .F. ) ;
#34482=ORIENTED_EDGE ( 'NONE', *, *, #13711, .F. ) ;
#34483=EDGE_LOOP ( 'NONE', ( #41678, #25981 ) ) ;
#34488=( NAMED_UNIT ( * ) PLANE_ANGLE_UNIT ( ) SI_UNIT ( $, .RADIAN. ) );
#34492=( NAMED_UNIT ( * ) PLANE_ANGLE_UNIT ( ) SI_UNIT ( $, .RADIAN. ) );
#34495=CARTESIAN_POINT ( 'NONE',  ( 30.99999999999999289, 5.000000000000000000, -37.00402776293829277 ) ) ;
#34518=CIRCLE ( 'NONE', #16583, 19.99999999999998934 ) ;
#34522=( NAMED_UNIT ( * ) SI_UNIT ( $, .STERADIAN. ) SOLID_ANGLE_UNIT ( ) );
#34539=( GEOMETRIC_REPRESENTATION_CONTEXT ( 3 ) GLOBAL_UNCERTAINTY_ASSIGNED_CONTEXT ( ( #3082 ) ) GLOBAL_UNIT_ASSIGNED_CONTEXT ( ( #5851, #57968, #15756 ) ) REPRESENTATION_CONTEXT ( 'NONE', 'WORKASPACE' ) );
#34550=ADVANCED_FACE ( 'NONE', ( #42247 ), #53761, .T. ) ;
#34551=DIRECTION ( 'NONE',  ( 1.982541115402069054E-16, 0.000000000000000000, -1.000000000000000000 ) ) ;
#34553=CARTESIAN_POINT ( 'NONE',  ( 108.3664351561509278, 14.00000000000000000, 18.43563588791581154 ) ) ;
#34563=DIRECTION ( 'NONE',  ( 0.000000000000000000, 1.000000000000000000, 0.000000000000000000 ) ) ;
#34570=( NAMED_UNIT ( * ) SI_UNIT ( $, .STERADIAN. ) SOLID_ANGLE_UNIT ( ) );
#34574=VERTEX_POINT ( 'NONE', #6593 ) ;
#34580=CARTESIAN_POINT ( 'NONE',  ( 82.09357085539566867, 0.000000000000000000, -37.00402776293823592 ) ) ;
#34606=DIRECTION ( 'NONE',  ( -0.000000000000000000, -1.000000000000000000, 0.000000000000000000 ) ) ;
#34614=FILL_AREA_STYLE ('',( #7891 ) ) ;
#34618=PRESENTATION_STYLE_ASSIGNMENT (( #28983 ) ) ;
#34620=EDGE_CURVE ( 'NONE', #49461, #1044, #68592, .T. ) ;
#34621=ADVANCED_FACE ( 'NONE', ( #59736 ), #49202, .T. ) ;
#34622=DIRECTION ( 'NONE',  ( 1.000000000000000000, 0.000000000000000000, -1.300977106640434891E-16 ) ) ;
#34624=ADVANCED_BREP_SHAPE_REPRESENTATION ( '', ( #50492, #42840 ), #53979 ) ;
#34626=AXIS2_PLACEMENT_3D ( 'NONE', #54879, #23577, #59834 ) ;
#34632=SURFACE_STYLE_USAGE ( .BOTH. , #34299 ) ;
#34641=ORIENTED_EDGE ( 'NONE', *, *, #13990, .F. ) ;
#34643=MECHANICAL_DESIGN_GEOMETRIC_PRESENTATION_REPRESENTATION('',(#29004),#6511);
#34645=AXIS2_PLACEMENT_3D ( 'NONE', #68871, #41814, #63231 ) ;
#34646=( NAMED_UNIT ( * ) SI_UNIT ( $, .STERADIAN. ) SOLID_ANGLE_UNIT ( ) );
#34648=VERTEX_POINT ( 'NONE', #4342 ) ;
#34649=FILL_AREA_STYLE_COLOUR ( '', #7354 ) ;
#34659=UNCERTAINTY_MEASURE_WITH_UNIT (LENGTH_MEASURE( 1.000000000000000082E-05 ), #17556, 'distance_accuracy_value', 'NONE');
#34671=CARTESIAN_POINT ( 'NONE',  ( 27.99999999999999645, 5.000000000000000000, -72.00402776293822171 ) ) ;
#34672=CIRCLE ( 'NONE', #31311, 4.999999999999997335 ) ;
#34680=CARTESIAN_POINT ( 'NONE',  ( 16.00000000000001776, 15.00000000000000000, 29.68999999999999417 ) ) ;
#34688=CARTESIAN_POINT ( 'NONE',  ( 28.00000000000002842, 38.00000000000000711, 90.00000000000000000 ) ) ;
#34692=EDGE_LOOP ( 'NONE', ( #54639, #46229 ) ) ;
#34695=DIRECTION ( 'NONE',  ( -1.000000000000000000, -0.000000000000000000, -0.000000000000000000 ) ) ;
#34702=DIRECTION ( 'NONE',  ( -0.000000000000000000, -1.000000000000000000, -0.000000000000000000 ) ) ;
#34703=ADVANCED_FACE ( 'NONE', ( #4083 ), #28121, .F. ) ;
#34704=UNCERTAINTY_MEASURE_WITH_UNIT (LENGTH_MEASURE( 1.000000000000000082E-05 ), #46340, 'distance_accuracy_value', 'NONE');
#34705=FACE_OUTER_BOUND ( 'NONE', #11532, .T. ) ;
#34708=SURFACE_STYLE_FILL_AREA ( #19919 ) ;
#34715=( NAMED_UNIT ( * ) PLANE_ANGLE_UNIT ( ) SI_UNIT ( $, .RADIAN. ) );
#34720=EDGE_LOOP ( 'NONE', ( #11479, #38852, #47297, #5305 ) ) ;
#34721=ORIENTED_EDGE ( 'NONE', *, *, #28980, .F. ) ;
#34731=VERTEX_POINT ( 'NONE', #12309 ) ;
#34743=VECTOR ( 'NONE', #18456, 1000.000000000000000 ) ;
#34745=ORIENTED_EDGE ( 'NONE', *, *, #55340, .F. ) ;
#34748=PRESENTATION_STYLE_ASSIGNMENT (( #66788 ) ) ;
#34757=VERTEX_POINT ( 'NONE', #58270 ) ;
#34775=( GEOMETRIC_REPRESENTATION_CONTEXT ( 3 ) GLOBAL_UNCERTAINTY_ASSIGNED_CONTEXT ( ( #46998 ) ) GLOBAL_UNIT_ASSIGNED_CONTEXT ( ( #45069, #62574, #34120 ) ) REPRESENTATION_CONTEXT ( 'NONE', 'WORKASPACE' ) );
#34777=DIRECTION ( 'NONE',  ( -1.000000000000000000, 0.000000000000000000, -4.625929269271509580E-16 ) ) ;
#34781=ORIENTED_EDGE ( 'NONE', *, *, #59955, .F. ) ;
#34782=PRESENTATION_STYLE_ASSIGNMENT (( #30182 ) ) ;
#34786=SURFACE_SIDE_STYLE ('',( #50979 ) ) ;
#34788=DIRECTION ( 'NONE',  ( 2.478176394252586564E-16, 0.000000000000000000, 1.000000000000000000 ) ) ;
#34794=DIRECTION ( 'NONE',  ( 0.000000000000000000, -1.000000000000000000, 0.000000000000000000 ) ) ;
#34796=UNCERTAINTY_MEASURE_WITH_UNIT (LENGTH_MEASURE( 1.000000000000000082E-05 ), #67458, 'distance_accuracy_value', 'NONE');
#34803=SURFACE_STYLE_FILL_AREA ( #40127 ) ;
#34823=DIRECTION ( 'NONE',  ( 0.000000000000000000, 0.000000000000000000, 1.000000000000000000 ) ) ;
#34826=STYLED_ITEM ( 'NONE', ( #54154 ), #11347 ) ;
#34827=DIRECTION ( 'NONE',  ( -0.000000000000000000, -1.000000000000000000, -0.000000000000000000 ) ) ;
#34828=CARTESIAN_POINT ( 'NONE',  ( 23.50000000000001776, 15.00000000000000000, -29.68999999999999417 ) ) ;
#34829=COLOUR_RGB ( '', 0.31764706, 0.68627451, 0.89019608) ;
#34842=( GEOMETRIC_REPRESENTATION_CONTEXT ( 3 ) GLOBAL_UNCERTAINTY_ASSIGNED_CONTEXT ( ( #15887 ) ) GLOBAL_UNIT_ASSIGNED_CONTEXT ( ( #33268, #55045, #32926 ) ) REPRESENTATION_CONTEXT ( 'NONE', 'WORKASPACE' ) );
#34845=AXIS2_PLACEMENT_3D ( 'NONE', #5268, #48939, #27745 ) ;
#34854=UNCERTAINTY_MEASURE_WITH_UNIT (LENGTH_MEASURE( 1.000000000000000082E-05 ), #64770, 'distance_accuracy_value', 'NONE');
#34855=AXIS2_PLACEMENT_3D ( 'NONE', #55826, #55120, #55484 ) ;
#34875=FACE_OUTER_BOUND ( 'NONE', #56825, .T. ) ;
#34877=PLANE ( 'NONE',  #12408 ) ;
#34879=DIRECTION ( 'NONE',  ( 1.000000000000000000, 0.000000000000000000, 4.625929269271509580E-16 ) ) ;
#34884=DIRECTION ( 'NONE',  ( -0.000000000000000000, 0.000000000000000000, 1.000000000000000000 ) ) ;
#34896=EDGE_CURVE ( 'NONE', #11361, #63620, #32936, .T. ) ;
#34902=( NAMED_UNIT ( * ) SI_UNIT ( $, .STERADIAN. ) SOLID_ANGLE_UNIT ( ) );
#34907=COLOUR_RGB ( '', 0.31764706, 0.68627451, 0.89019608) ;
#34908=CARTESIAN_POINT ( 'NONE',  ( 29.00000000000000000, 0.000000000000000000, 3.902931319921305165E-16 ) ) ;
#34916=PRESENTATION_STYLE_ASSIGNMENT (( #51114 ) ) ;
#34919=ORIENTED_EDGE ( 'NONE', *, *, #50920, .T. ) ;
#34929=CYLINDRICAL_SURFACE ( 'NONE', #27604, 4.999999999999997335 ) ;
#34931=PRESENTATION_STYLE_ASSIGNMENT (( #67291 ) ) ;
#34932=ADVANCED_FACE ( 'NONE', ( #6190 ), #65278, .F. ) ;
#34942=SURFACE_STYLE_USAGE ( .BOTH. , #29670 ) ;
#34943=DIRECTION ( 'NONE',  ( -0.000000000000000000, -1.000000000000000000, -0.000000000000000000 ) ) ;
#34944=PLANE ( 'NONE',  #5992 ) ;
#34949=VECTOR ( 'NONE', #36146, 1000.000000000000000 ) ;
#34962=CARTESIAN_POINT ( 'NONE',  ( 6.000000000000017764, 26.00000000000000355, -20.50000000000000355 ) ) ;
#35006=FACE_OUTER_BOUND ( 'NONE', #29182, .T. ) ;
#35012=EDGE_CURVE ( 'NONE', #55787, #1416, #24778, .T. ) ;
#35016=EDGE_LOOP ( 'NONE', ( #5761, #59907, #5929, #48064 ) ) ;
#35020=FILL_AREA_STYLE ('',( #30074 ) ) ;
#35057=CARTESIAN_POINT ( 'NONE',  ( 36.00000000000002842, 0.000000000000000000, 77.00402776293825013 ) ) ;
#35059=DIRECTION ( 'NONE',  ( -1.000000000000000000, 0.000000000000000000, -0.000000000000000000 ) ) ;
#35065=FILL_AREA_STYLE_COLOUR ( '', #27843 ) ;
#35077=DIRECTION ( 'NONE',  ( 0.000000000000000000, 0.000000000000000000, 1.000000000000000000 ) ) ;
#35079=( NAMED_UNIT ( * ) PLANE_ANGLE_UNIT ( ) SI_UNIT ( $, .RADIAN. ) );
#35080=MECHANICAL_DESIGN_GEOMETRIC_PRESENTATION_REPRESENTATION('',(#38508),#3560);
#35089=CIRCLE ( 'NONE', #58694, 17.00000000000000000 ) ;
#35106=DIRECTION ( 'NONE',  ( 1.000000000000000000, -0.000000000000000000, -1.300977106640434891E-16 ) ) ;
#35113=SURFACE_STYLE_FILL_AREA ( #34074 ) ;
#35118=LINE ( 'NONE', #18918, #59700 ) ;
#35121=AXIS2_PLACEMENT_3D ( 'NONE', #62607, #52448, #20402 ) ;
#35134=AXIS2_PLACEMENT_3D ( 'NONE', #47889, #59063, #15491 ) ;
#35143=( NAMED_UNIT ( * ) SI_UNIT ( $, .STERADIAN. ) SOLID_ANGLE_UNIT ( ) );
#35147=COLOUR_RGB ( '', 0.40784314, 0.44705882, 0.49803922) ;
#35153=FILL_AREA_STYLE ('',( #61189 ) ) ;
#35169=DIRECTION ( 'NONE',  ( 1.000000000000000000, 0.000000000000000000, -3.932039878880752229E-15 ) ) ;
#35170=DIRECTION ( 'NONE',  ( -0.000000000000000000, -0.000000000000000000, -1.000000000000000000 ) ) ;
#35171=LINE ( 'NONE', #20016, #68543 ) ;
#35178=CYLINDRICAL_SURFACE ( 'NONE', #20771, 12.50000000000000178 ) ;
#35181=ORIENTED_EDGE ( 'NONE', *, *, #46091, .F. ) ;
#35184=VERTEX_POINT ( 'NONE', #58541 ) ;
#35201=DIRECTION ( 'NONE',  ( -0.000000000000000000, 0.000000000000000000, 1.000000000000000000 ) ) ;
#35203=ORIENTED_EDGE ( 'NONE', *, *, #32637, .F. ) ;
#35216=EDGE_CURVE ( 'NONE', #19853, #56811, #25828, .T. ) ;
#35221=DIRECTION ( 'NONE',  ( -0.000000000000000000, -1.000000000000000000, -0.000000000000000000 ) ) ;
#35223=DIRECTION ( 'NONE',  ( 1.300977106640434891E-16, -0.000000000000000000, 1.000000000000000000 ) ) ;
#35228=DIRECTION ( 'NONE',  ( -1.000000000000000000, -0.000000000000000000, -0.000000000000000000 ) ) ;
#35231=FACE_OUTER_BOUND ( 'NONE', #27635, .T. ) ;
#35233=( NAMED_UNIT ( * ) PLANE_ANGLE_UNIT ( ) SI_UNIT ( $, .RADIAN. ) );
#35239=CARTESIAN_POINT ( 'NONE',  ( 1.000000000000000000, 43.00000000000000000, 45.61250543006183733 ) ) ;
#35240=COLOUR_RGB ( '', 0.08235294, 0.09019608, 0.10196078) ;
#35245=MECHANICAL_DESIGN_GEOMETRIC_PRESENTATION_REPRESENTATION('',(#19469),#32990);
#35246=DIRECTION ( 'NONE',  ( 1.000000000000000000, 0.000000000000000000, 0.000000000000000000 ) ) ;
#35248=CIRCLE ( 'NONE', #39798, 12.50000000000001066 ) ;
#35251=( LENGTH_UNIT ( ) NAMED_UNIT ( * ) SI_UNIT ( .MILLI., .METRE. ) );
#35255=EDGE_LOOP ( 'NONE', ( #41002, #27538, #65555, #18174 ) ) ;
#35263=ORIENTED_EDGE ( 'NONE', *, *, #24758, .F. ) ;
#35265=ADVANCED_FACE ( 'NONE', ( #64850, #44148 ), #60271, .T. ) ;
#35270=CARTESIAN_POINT ( 'NONE',  ( 27.99999999999998224, 5.000000000000000000, 72.00402776293822171 ) ) ;
#35287=SPHERICAL_SURFACE ( 'NONE', #56346, 1.000000000000000000 ) ;
#35292=AXIS2_PLACEMENT_3D ( 'NONE', #44599, #29759, #6910 ) ;
#35297=PRESENTATION_STYLE_ASSIGNMENT (( #65911 ) ) ;
#35301=SPHERICAL_SURFACE ( 'NONE', #59918, 1.000000000000000000 ) ;
#35304=VERTEX_POINT ( 'NONE', #32851 ) ;
#35306=CARTESIAN_POINT ( 'NONE',  ( 4.000000000000002665, 38.93969262078591242, -89.65797985667433068 ) ) ;
#35313=( GEOMETRIC_REPRESENTATION_CONTEXT ( 3 ) GLOBAL_UNCERTAINTY_ASSIGNED_CONTEXT ( ( #51545 ) ) GLOBAL_UNIT_ASSIGNED_CONTEXT ( ( #11998, #5319, #10626 ) ) REPRESENTATION_CONTEXT ( 'NONE', 'WORKASPACE' ) );
#35319=MECHANICAL_DESIGN_GEOMETRIC_PRESENTATION_REPRESENTATION('',(#30774),#64488);
#35321=CARTESIAN_POINT ( 'NONE',  ( 11.00000000000001776, 26.00000000000000355, 27.49999999999999645 ) ) ;
#35322=DIRECTION ( 'NONE',  ( 0.000000000000000000, 0.000000000000000000, -1.000000000000000000 ) ) ;
#35326=CARTESIAN_POINT ( 'NONE',  ( 23.85435327029094665, 24.60286873851424261, -27.21019326824331230 ) ) ;
#35334=FACE_OUTER_BOUND ( 'NONE', #4123, .T. ) ;
#35342=DIRECTION ( 'NONE',  ( 0.000000000000000000, 1.000000000000000000, -0.000000000000000000 ) ) ;
#35343=CARTESIAN_POINT ( 'NONE',  ( 22.00000000000000355, 43.00000000000000000, -90.00000000000000000 ) ) ;
#35347=AXIS2_PLACEMENT_3D ( 'NONE', #20199, #52253, #36058 ) ;
#35351=STYLED_ITEM ( 'NONE', ( #51336 ), #31604 ) ;
#35353=DIRECTION ( 'NONE',  ( 0.000000000000000000, -0.000000000000000000, 1.000000000000000000 ) ) ;
#35359=CARTESIAN_POINT ( 'NONE',  ( 31.00000000000000711, 42.00000000000000000, -36.50000000000000000 ) ) ;
#35362=CYLINDRICAL_SURFACE ( 'NONE', #29716, 1.000000000000000888 ) ;
#35370=SURFACE_STYLE_USAGE ( .BOTH. , #44574 ) ;
#35372=CARTESIAN_POINT ( 'NONE',  ( 10.00000000000000533, 50.00000000000000000, -46.00000000000000000 ) ) ;
#35377=AXIS2_PLACEMENT_3D ( 'NONE', #26259, #31177, #10103 ) ;
#35380=ORIENTED_EDGE ( 'NONE', *, *, #18682, .T. ) ;
#35384=ORIENTED_EDGE ( 'NONE', *, *, #667, .F. ) ;
#35389=AXIS2_PLACEMENT_3D ( 'NONE', #54451, #7571, #13181 ) ;
#35410=DIRECTION ( 'NONE',  ( 1.000000000000000000, -0.000000000000000000, -0.000000000000000000 ) ) ;
#35414=ORIENTED_EDGE ( 'NONE', *, *, #44036, .F. ) ;
#35422=( NAMED_UNIT ( * ) SI_UNIT ( $, .STERADIAN. ) SOLID_ANGLE_UNIT ( ) );
#35428=AXIS2_PLACEMENT_3D ( 'NONE', #6970, #28393, #60761 ) ;
#35432=( BOUNDED_CURVE ( )  B_SPLINE_CURVE ( 3, ( #34326, #13544, #39987, #45264 ),
 .UNSPECIFIED., .F., .F. ) 
 B_SPLINE_CURVE_WITH_KNOTS ( ( 4, 4 ),
 ( 4.712388980384687898, 5.445427266222307772 ),
 .UNSPECIFIED. ) 
 CURVE ( )  GEOMETRIC_REPRESENTATION_ITEM ( )  RATIONAL_B_SPLINE_CURVE ( ( 1.000000000000000000, 0.9557202843314677176, 0.9557202843314677176, 1.000000000000000000 ) ) 
 REPRESENTATION_ITEM ( '' )  );
#35433=CARTESIAN_POINT ( 'NONE',  ( 1.000000000000000888, 43.00000000000000000, -45.61250543006183733 ) ) ;
#35436=PLANE ( 'NONE',  #42876 ) ;
#35440=CARTESIAN_POINT ( 'NONE',  ( 26.00000000000001776, 14.00000000000000000, -34.49999999999999289 ) ) ;
#35442=VERTEX_POINT ( 'NONE', #923 ) ;
#35446=( LENGTH_UNIT ( ) NAMED_UNIT ( * ) SI_UNIT ( .MILLI., .METRE. ) );
#35447=EDGE_CURVE ( 'NONE', #2934, #25731, #42921, .T. ) ;
#35453=ADVANCED_FACE ( 'NONE', ( #53775 ), #16877, .F. ) ;
#35457=ORIENTED_EDGE ( 'NONE', *, *, #29790, .T. ) ;
#35471=VERTEX_POINT ( 'NONE', #18588 ) ;
#35488=DIRECTION ( 'NONE',  ( 0.000000000000000000, 1.000000000000000000, 0.000000000000000000 ) ) ;
#35497=ORIENTED_EDGE ( 'NONE', *, *, #35216, .F. ) ;
#35500=( GEOMETRIC_REPRESENTATION_CONTEXT ( 3 ) GLOBAL_UNCERTAINTY_ASSIGNED_CONTEXT ( ( #69378 ) ) GLOBAL_UNIT_ASSIGNED_CONTEXT ( ( #7476, #11711, #54938 ) ) REPRESENTATION_CONTEXT ( 'NONE', 'WORKASPACE' ) );
#35501=FILL_AREA_STYLE ('',( #55904 ) ) ;
#35505=( NAMED_UNIT ( * ) PLANE_ANGLE_UNIT ( ) SI_UNIT ( $, .RADIAN. ) );
#35511=FACE_OUTER_BOUND ( 'NONE', #36568, .T. ) ;
#35516=CARTESIAN_POINT ( 'NONE',  ( 4.000000000000002665, 38.70020753820971748, -89.00000000000000000 ) ) ;
#35526=CARTESIAN_POINT ( 'NONE',  ( 57.00000000000000000, 0.000000000000000000, 60.00402776293825724 ) ) ;
#35529=ORIENTED_EDGE ( 'NONE', *, *, #49747, .T. ) ;
#35541=VECTOR ( 'NONE', #23841, 1000.000000000000000 ) ;
#35544=CYLINDRICAL_SURFACE ( 'NONE', #44871, 4.999999999999990230 ) ;
#35546=ORIENTED_EDGE ( 'NONE', *, *, #14538, .T. ) ;
#35547=AXIS2_PLACEMENT_3D ( 'NONE', #1836, #25768, #62695 ) ;
#35552=CARTESIAN_POINT ( 'NONE',  ( 27.99999999999998934, 0.000000000000000000, -37.00402776293828566 ) ) ;
#35577=DIRECTION ( 'NONE',  ( 0.000000000000000000, 0.000000000000000000, 1.000000000000000000 ) ) ;
#35579=DIRECTION ( 'NONE',  ( 0.000000000000000000, 0.000000000000000000, 1.000000000000000000 ) ) ;
#35582=ORIENTED_EDGE ( 'NONE', *, *, #40221, .T. ) ;
#35584=STYLED_ITEM ( 'NONE', ( #22829 ), #3109 ) ;
#35585=DIRECTION ( 'NONE',  ( 0.000000000000000000, -1.000000000000000000, 0.000000000000000000 ) ) ;
#35589=FILL_AREA_STYLE_COLOUR ( '', #67451 ) ;
#35591=( NAMED_UNIT ( * ) PLANE_ANGLE_UNIT ( ) SI_UNIT ( $, .RADIAN. ) );
#35613=SURFACE_STYLE_FILL_AREA ( #29263 ) ;
#35614=ADVANCED_FACE ( 'NONE', ( #30146 ), #67681, .T. ) ;
#35629=DIRECTION ( 'NONE',  ( 0.9418169057949938860, 0.000000000000000000, -0.3361263392814427542 ) ) ;
#35641=CARTESIAN_POINT ( 'NONE',  ( 3.000000000000002665, 42.00000000000000000, -80.00402776293826435 ) ) ;
#35647=LINE ( 'NONE', #57797, #26113 ) ;
#35650=DIRECTION ( 'NONE',  ( 0.000000000000000000, -1.000000000000000000, 0.000000000000000000 ) ) ;
#35654=FACE_OUTER_BOUND ( 'NONE', #50168, .T. ) ;
#35660=SURFACE_STYLE_FILL_AREA ( #69401 ) ;
#35665=( NAMED_UNIT ( * ) PLANE_ANGLE_UNIT ( ) SI_UNIT ( $, .RADIAN. ) );
#35670=DIRECTION ( 'NONE',  ( 1.000000000000000000, -0.000000000000000000, -1.300977106640434891E-16 ) ) ;
#35699=FILL_AREA_STYLE ('',( #68064 ) ) ;
#35700=CARTESIAN_POINT ( 'NONE',  ( 26.00000000000001776, 42.00000000000000000, -29.68999999999999417 ) ) ;
#35708=( LENGTH_UNIT ( ) NAMED_UNIT ( * ) SI_UNIT ( .MILLI., .METRE. ) );
#35714=SURFACE_STYLE_FILL_AREA ( #52601 ) ;
#35716=VERTEX_POINT ( 'NONE', #28231 ) ;
#35718=FACE_OUTER_BOUND ( 'NONE', #38994, .T. ) ;
#35725=( NAMED_UNIT ( * ) PLANE_ANGLE_UNIT ( ) SI_UNIT ( $, .RADIAN. ) );
#35750=SURFACE_STYLE_FILL_AREA ( #24821 ) ;
#35753=CARTESIAN_POINT ( 'NONE',  ( 0.000000000000000000, 42.00000000000000000, -75.00000000000001421 ) ) ;
#35758=( LENGTH_UNIT ( ) NAMED_UNIT ( * ) SI_UNIT ( .MILLI., .METRE. ) );
#35772=SURFACE_STYLE_USAGE ( .BOTH. , #14312 ) ;
#35775=CARTESIAN_POINT ( 'NONE',  ( 11.00000000000001776, -3.148064030671221758, 29.68999999999999417 ) ) ;
#35782=SURFACE_STYLE_FILL_AREA ( #24860 ) ;
#35786=AXIS2_PLACEMENT_3D ( 'NONE', #36566, #68528, #67226 ) ;
#35789=ORIENTED_EDGE ( 'NONE', *, *, #23293, .T. ) ;
#35800=EDGE_LOOP ( 'NONE', ( #19372, #20639, #62749, #39038 ) ) ;
#35821=EDGE_LOOP ( 'NONE', ( #522, #35865, #4239, #21609, #25337, #4605, #41784, #48295, #68352, #22753, #41870, #826, #38640, #63235, #40098, #47890 ) ) ;
#35827=( NAMED_UNIT ( * ) PLANE_ANGLE_UNIT ( ) SI_UNIT ( $, .RADIAN. ) );
#35831=FILL_AREA_STYLE ('',( #8417 ) ) ;
#35836=PRESENTATION_STYLE_ASSIGNMENT (( #5435 ) ) ;
#35838=CARTESIAN_POINT ( 'NONE',  ( 82.09357085539578236, 5.000000000000000000, 32.00402776293825724 ) ) ;
#35844=CARTESIAN_POINT ( 'NONE',  ( 57.00000000000000000, 0.9999999999999991118, 80.00402776293826435 ) ) ;
#35860=( NAMED_UNIT ( * ) SI_UNIT ( $, .STERADIAN. ) SOLID_ANGLE_UNIT ( ) );
#35865=ORIENTED_EDGE ( 'NONE', *, *, #47063, .T. ) ;
#35870=CARTESIAN_POINT ( 'NONE',  ( 82.09357085539566867, 5.000000000000000000, -37.00402776293823592 ) ) ;
#35884=ORIENTED_EDGE ( 'NONE', *, *, #5911, .T. ) ;
#35904=DIRECTION ( 'NONE',  ( 1.000000000000000000, -0.000000000000000000, -1.300977106640434891E-16 ) ) ;
#35911=( GEOMETRIC_REPRESENTATION_CONTEXT ( 3 ) GLOBAL_UNCERTAINTY_ASSIGNED_CONTEXT ( ( #41918 ) ) GLOBAL_UNIT_ASSIGNED_CONTEXT ( ( #63468, #42413, #10010 ) ) REPRESENTATION_CONTEXT ( 'NONE', 'WORKASPACE' ) );
#35918=VECTOR ( 'NONE', #68137, 1000.000000000000000 ) ;
#35936=SURFACE_SIDE_STYLE ('',( #14458 ) ) ;
#35937=MECHANICAL_DESIGN_GEOMETRIC_PRESENTATION_REPRESENTATION('',(#28037),#66233);
#35938=CARTESIAN_POINT ( 'NONE',  ( 57.00000000000000000, 16.00000000000000000, 72.50402776293826435 ) ) ;
#35942=CARTESIAN_POINT ( 'NONE',  ( 4.000000000000030198, 38.93969262078591242, 89.65797985667433068 ) ) ;
#35954=VERTEX_POINT ( 'NONE', #12016 ) ;
#35960=AXIS2_PLACEMENT_3D ( 'NONE', #29966, #3906, #31001 ) ;
#35973=CARTESIAN_POINT ( 'NONE',  ( 1.000000000000000888, 43.00000000000000000, 74.38749456993816978 ) ) ;
#35982=VERTEX_POINT ( 'NONE', #46501 ) ;
#35994=DIRECTION ( 'NONE',  ( -0.000000000000000000, -1.000000000000000000, -0.000000000000000000 ) ) ;
#35996=CARTESIAN_POINT ( 'NONE',  ( 27.00000000000001776, 42.00000000000000000, 35.50000000000000000 ) ) ;
#36003=SURFACE_SIDE_STYLE ('',( #36389 ) ) ;
#36007=( GEOMETRIC_REPRESENTATION_CONTEXT ( 3 ) GLOBAL_UNCERTAINTY_ASSIGNED_CONTEXT ( ( #4725 ) ) GLOBAL_UNIT_ASSIGNED_CONTEXT ( ( #40644, #9676, #20188 ) ) REPRESENTATION_CONTEXT ( 'NONE', 'WORKASPACE' ) );
#36008=EDGE_CURVE ( 'NONE', #29977, #26396, #34022, .T. ) ;
#36021=DIRECTION ( 'NONE',  ( 0.000000000000000000, -0.7431448254773944662, 0.6691306063588580155 ) ) ;
#36048=STYLED_ITEM ( 'NONE', ( #23890 ), #12423 ) ;
#36056=ORIENTED_EDGE ( 'NONE', *, *, #4602, .T. ) ;
#36058=DIRECTION ( 'NONE',  ( 0.000000000000000000, 0.000000000000000000, -1.000000000000000000 ) ) ;
#36090=DIRECTION ( 'NONE',  ( 0.000000000000000000, -0.3420201433256629953, -0.9396926207859104263 ) ) ;
#36100=EDGE_CURVE ( 'NONE', #29677, #25215, #43078, .T. ) ;
#36117=STYLED_ITEM ( 'NONE', ( #17120 ), #54231 ) ;
#36124=AXIS2_PLACEMENT_3D ( 'NONE', #21217, #53590, #31780 ) ;
#36125=( LENGTH_UNIT ( ) NAMED_UNIT ( * ) SI_UNIT ( .MILLI., .METRE. ) );
#36130=CARTESIAN_POINT ( 'NONE',  ( 36.00000000000002132, 5.000000000000000000, -77.00402776293825013 ) ) ;
#36136=AXIS2_PLACEMENT_3D ( 'NONE', #22938, #44769, #45470 ) ;
#36137=PRESENTATION_STYLE_ASSIGNMENT (( #9403 ) ) ;
#36140=DIRECTION ( 'NONE',  ( 0.000000000000000000, 0.000000000000000000, -1.000000000000000000 ) ) ;
#36146=DIRECTION ( 'NONE',  ( 1.000000000000000000, -0.000000000000000000, 0.000000000000000000 ) ) ;
#36148=MECHANICAL_DESIGN_GEOMETRIC_PRESENTATION_REPRESENTATION('',(#30475),#32761);
#36152=CARTESIAN_POINT ( 'NONE',  ( 22.84135002011590387, 24.77014762460473563, -27.27734489800906914 ) ) ;
#36159=CYLINDRICAL_SURFACE ( 'NONE', #10671, 19.99999999999998934 ) ;
#36167=( GEOMETRIC_REPRESENTATION_CONTEXT ( 3 ) GLOBAL_UNCERTAINTY_ASSIGNED_CONTEXT ( ( #65112 ) ) GLOBAL_UNIT_ASSIGNED_CONTEXT ( ( #59386, #8385, #67449 ) ) REPRESENTATION_CONTEXT ( 'NONE', 'WORKASPACE' ) );
#36170=VERTEX_POINT ( 'NONE', #32000 ) ;
#36171=( NAMED_UNIT ( * ) SI_UNIT ( $, .STERADIAN. ) SOLID_ANGLE_UNIT ( ) );
#36173=FILL_AREA_STYLE_COLOUR ( '', #46371 ) ;
#36207=EDGE_CURVE ( 'NONE', #25561, #55142, #39679, .T. ) ;
#36213=( LENGTH_UNIT ( ) NAMED_UNIT ( * ) SI_UNIT ( .MILLI., .METRE. ) );
#36216=VECTOR ( 'NONE', #19482, 1000.000000000000000 ) ;
#36218=CARTESIAN_POINT ( 'NONE',  ( 57.00000000000000000, 15.00000000000000000, 34.49999999999998579 ) ) ;
#36221=AXIS2_PLACEMENT_3D ( 'NONE', #68164, #41105, #13994 ) ;
#36225=DIRECTION ( 'NONE',  ( 0.000000000000000000, 1.000000000000000000, 0.000000000000000000 ) ) ;
#36237=CYLINDRICAL_SURFACE ( 'NONE', #49459, 1.000000000000000888 ) ;
#36238=MECHANICAL_DESIGN_GEOMETRIC_PRESENTATION_REPRESENTATION('',(#12541),#39608);
#36240=DIRECTION ( 'NONE',  ( 0.000000000000000000, 0.000000000000000000, -1.000000000000000000 ) ) ;
#36241=CARTESIAN_POINT ( 'NONE',  ( 4.000000000000002665, 43.00000000000000000, -79.00402776293826435 ) ) ;
#36248=EDGE_CURVE ( 'NONE', #44275, #4197, #30957, .T. ) ;
#36249=FILL_AREA_STYLE_COLOUR ( '', #1221 ) ;
#36250=DIRECTION ( 'NONE',  ( -1.734723475976803545E-15, 0.7431448254773944662, 0.6691306063588580155 ) ) ;
#36253=SURFACE_SIDE_STYLE ('',( #47518 ) ) ;
#36254=ORIENTED_EDGE ( 'NONE', *, *, #28495, .F. ) ;
#36266=ORIENTED_EDGE ( 'NONE', *, *, #21472, .T. ) ;
#36267=VECTOR ( 'NONE', #41905, 1000.000000000000000 ) ;
#36277=CIRCLE ( 'NONE', #4740, 4.000000000000003553 ) ;
#36294=PLANE ( 'NONE',  #28355 ) ;
#36298=ORIENTED_EDGE ( 'NONE', *, *, #12007, .F. ) ;
#36300=CARTESIAN_POINT ( 'NONE',  ( 22.39276236906906448, 26.60476906391062002, 27.44839360434220410 ) ) ;
#36302=COLOUR_RGB ( '', 0.66274510, 0.83137255, 0.94901961) ;
#36310=STYLED_ITEM ( 'NONE', ( #16647 ), #25798 ) ;
#36314=PRESENTATION_STYLE_ASSIGNMENT (( #40185 ) ) ;
#36319=CARTESIAN_POINT ( 'NONE',  ( 26.00000000000001776, -3.148064030671221758, 34.49999999999999289 ) ) ;
#36320=UNCERTAINTY_MEASURE_WITH_UNIT (LENGTH_MEASURE( 1.000000000000000082E-05 ), #14261, 'distance_accuracy_value', 'NONE');
#36327=SURFACE_STYLE_USAGE ( .BOTH. , #2573 ) ;
#36332=VERTEX_POINT ( 'NONE', #1311 ) ;
#36334=VERTEX_POINT ( 'NONE', #38368 ) ;
#36355=CARTESIAN_POINT ( 'NONE',  ( 22.99999999999998224, 0.000000000000000000, 72.00402776293825013 ) ) ;
#36361=DIRECTION ( 'NONE',  ( 0.000000000000000000, -1.000000000000000000, 0.000000000000000000 ) ) ;
#36371=CARTESIAN_POINT ( 'NONE',  ( 27.00000000000001776, 42.00000000000000000, 36.50000000000000000 ) ) ;
#36375=CYLINDRICAL_SURFACE ( 'NONE', #14269, 1.000000000000000888 ) ;
#36389=SURFACE_STYLE_FILL_AREA ( #40246 ) ;
#36393=CARTESIAN_POINT ( 'NONE',  ( 27.99999999999998224, 5.000000000000000000, 72.00402776293822171 ) ) ;
#36397=SURFACE_STYLE_USAGE ( .BOTH. , #4296 ) ;
#36400=AXIS2_PLACEMENT_3D ( 'NONE', #61816, #41456, #68177 ) ;
#36406=FILL_AREA_STYLE ('',( #69074 ) ) ;
#36407=CIRCLE ( 'NONE', #6012, 12.50000000000001066 ) ;
#36416=AXIS2_PLACEMENT_3D ( 'NONE', #60334, #1184, #49804 ) ;
#36421=( GEOMETRIC_REPRESENTATION_CONTEXT ( 3 ) GLOBAL_UNCERTAINTY_ASSIGNED_CONTEXT ( ( #37633 ) ) GLOBAL_UNIT_ASSIGNED_CONTEXT ( ( #17828, #16810, #39307 ) ) REPRESENTATION_CONTEXT ( 'NONE', 'WORKASPACE' ) );
#36428=ORIENTED_EDGE ( 'NONE', *, *, #40101, .T. ) ;
#36434=FILL_AREA_STYLE_COLOUR ( '', #30339 ) ;
#36435=( NAMED_UNIT ( * ) SI_UNIT ( $, .STERADIAN. ) SOLID_ANGLE_UNIT ( ) );
#36447=ORIENTED_EDGE ( 'NONE', *, *, #15041, .T. ) ;
#36452=FILL_AREA_STYLE_COLOUR ( '', #58927 ) ;
#36454=MECHANICAL_DESIGN_GEOMETRIC_PRESENTATION_REPRESENTATION('',(#57753),#11697);
#36471=DIRECTION ( 'NONE',  ( 1.000000000000000000, 0.000000000000000000, -1.300977106640434891E-16 ) ) ;
#36473=MECHANICAL_DESIGN_GEOMETRIC_PRESENTATION_REPRESENTATION('',(#3803),#38677);
#36477=ADVANCED_FACE ( 'NONE', ( #43639 ), #16891, .F. ) ;
#36487=CARTESIAN_POINT ( 'NONE',  ( 4.000000000000001776, 34.36176364315826248, -80.00402776293826435 ) ) ;
#36492=AXIS2_PLACEMENT_3D ( 'NONE', #14440, #46153, #35577 ) ;
#36496=AXIS2_PLACEMENT_3D ( 'NONE', #14379, #36225, #42547 ) ;
#36506=CIRCLE ( 'NONE', #39866, 4.999999999999997335 ) ;
#36509=EDGE_CURVE ( 'NONE', #35442, #38534, #47659, .T. ) ;
#36510=CARTESIAN_POINT ( 'NONE',  ( 86.21825843581756033, 0.000000000000000000, 39.83014742847163348 ) ) ;
#36511=DIRECTION ( 'NONE',  ( 1.000000000000000000, -0.000000000000000000, -1.300977106640434891E-16 ) ) ;
#36518=( GEOMETRIC_REPRESENTATION_CONTEXT ( 3 ) GLOBAL_UNCERTAINTY_ASSIGNED_CONTEXT ( ( #41763 ) ) GLOBAL_UNIT_ASSIGNED_CONTEXT ( ( #18974, #12403, #20022 ) ) REPRESENTATION_CONTEXT ( 'NONE', 'WORKASPACE' ) );
#36519=EDGE_LOOP ( 'NONE', ( #39451, #47916, #58438, #62937 ) ) ;
#36520=( GEOMETRIC_REPRESENTATION_CONTEXT ( 3 ) GLOBAL_UNCERTAINTY_ASSIGNED_CONTEXT ( ( #28372 ) ) GLOBAL_UNIT_ASSIGNED_CONTEXT ( ( #52259, #8635, #51531 ) ) REPRESENTATION_CONTEXT ( 'NONE', 'WORKASPACE' ) );
#36521=PRESENTATION_STYLE_ASSIGNMENT (( #15047 ) ) ;
#36522=CARTESIAN_POINT ( 'NONE',  ( 3.000000000000030198, 43.00000000000000000, 79.00402776293826435 ) ) ;
#36525=FILL_AREA_STYLE_COLOUR ( '', #3554 ) ;
#36534=ORIENTED_EDGE ( 'NONE', *, *, #19378, .T. ) ;
#36536=CARTESIAN_POINT ( 'NONE',  ( 27.99999999999999645, 0.000000000000000000, -72.00402776293822171 ) ) ;
#36539=AXIS2_PLACEMENT_3D ( 'NONE', #12745, #66207, #39176 ) ;
#36549=SURFACE_STYLE_FILL_AREA ( #53698 ) ;
#36560=( NAMED_UNIT ( * ) SI_UNIT ( $, .STERADIAN. ) SOLID_ANGLE_UNIT ( ) );
#36564=DIRECTION ( 'NONE',  ( 0.000000000000000000, 0.6449798928094537809, 0.7641995406119435064 ) ) ;
#36566=CARTESIAN_POINT ( 'NONE',  ( 7.999999999999992895, 5.000000000000000000, 24.00402776293826079 ) ) ;
#36568=EDGE_LOOP ( 'NONE', ( #38348, #45396, #28487, #67539 ) ) ;
#36570=CYLINDRICAL_SURFACE ( 'NONE', #24206, 1.000000000000000000 ) ;
#36575=CARTESIAN_POINT ( 'NONE',  ( 3.000000000000030198, 42.58578643762690064, 89.58578643762690774 ) ) ;
#36578=CARTESIAN_POINT ( 'NONE',  ( 25.00000000000001421, 42.00000000000000000, 0.000000000000000000 ) ) ;
#36597=CARTESIAN_POINT ( 'NONE',  ( 23.50000000000001776, 43.00000000000000000, -28.18999999999999773 ) ) ;
#36612=PRESENTATION_STYLE_ASSIGNMENT (( #51699 ) ) ;
#36615=ORIENTED_EDGE ( 'NONE', *, *, #3838, .T. ) ;
#36629=EDGE_CURVE ( 'NONE', #43704, #46026, #3399, .T. ) ;
#36640=EDGE_LOOP ( 'NONE', ( #37344, #27535, #61933, #68600 ) ) ;
#36650=VECTOR ( 'NONE', #42395, 1000.000000000000000 ) ;
#36657=FILL_AREA_STYLE ('',( #42611 ) ) ;
#36669=CARTESIAN_POINT ( 'NONE',  ( 35.99999999999999289, 0.000000000000000000, 37.00402776293825724 ) ) ;
#36687=EDGE_CURVE ( 'NONE', #62990, #50964, #40894, .T. ) ;
#36690=VECTOR ( 'NONE', #64100, 1000.000000000000000 ) ;
#36700=FILL_AREA_STYLE ('',( #9595 ) ) ;
#36704=CARTESIAN_POINT ( 'NONE',  ( 30.99999999999998579, 5.000000000000000000, -72.00402776293822171 ) ) ;
#36707=DIRECTION ( 'NONE',  ( -1.000000000000000000, 0.000000000000000000, 0.000000000000000000 ) ) ;
#36735=DIRECTION ( 'NONE',  ( 1.239088197126290324E-16, 0.000000000000000000, 1.000000000000000000 ) ) ;
#36736=AXIS2_PLACEMENT_3D ( 'NONE', #53689, #25229, #46748 ) ;
#36737=FILL_AREA_STYLE_COLOUR ( '', #15580 ) ;
#36741=DIRECTION ( 'NONE',  ( 1.000000000000000000, 0.000000000000000000, 0.000000000000000000 ) ) ;
#36743=DIRECTION ( 'NONE',  ( 0.000000000000000000, 0.000000000000000000, 1.000000000000000000 ) ) ;
#36747=PLANE ( 'NONE',  #67619 ) ;
#36749=DIRECTION ( 'NONE',  ( 0.000000000000000000, 0.000000000000000000, -1.000000000000000000 ) ) ;
#36765=COLOUR_RGB ( '', 0.40784314, 0.44705882, 0.49803922) ;
#36774=DIRECTION ( 'NONE',  ( 0.000000000000000000, 0.000000000000000000, 1.000000000000000000 ) ) ;
#36775=PLANE ( 'NONE',  #53861 ) ;
#36776=CIRCLE ( 'NONE', #7554, 1.000000000000000888 ) ;
#36778=ORIENTED_EDGE ( 'NONE', *, *, #11292, .F. ) ;
#36785=( NAMED_UNIT ( * ) SI_UNIT ( $, .STERADIAN. ) SOLID_ANGLE_UNIT ( ) );
#36789=ORIENTED_EDGE ( 'NONE', *, *, #68383, .F. ) ;
#36793=FILL_AREA_STYLE_COLOUR ( '', #16249 ) ;
#36795=CARTESIAN_POINT ( 'NONE',  ( 21.00000000000001776, 42.00000000000000000, 29.68999999999999417 ) ) ;
#36797=EDGE_LOOP ( 'NONE', ( #36534, #27483, #31781 ) ) ;
#36800=FACE_OUTER_BOUND ( 'NONE', #30910, .T. ) ;
#36801=ORIENTED_EDGE ( 'NONE', *, *, #7932, .F. ) ;
#36803=CARTESIAN_POINT ( 'NONE',  ( 4.000000000000002665, 38.70020753820971748, -89.00000000000000000 ) ) ;
#36808=SURFACE_SIDE_STYLE ('',( #47021 ) ) ;
#36810=LINE ( 'NONE', #3677, #15401 ) ;
#36821=( LENGTH_UNIT ( ) NAMED_UNIT ( * ) SI_UNIT ( .MILLI., .METRE. ) );
#36832=( NAMED_UNIT ( * ) PLANE_ANGLE_UNIT ( ) SI_UNIT ( $, .RADIAN. ) );
#36843=DIRECTION ( 'NONE',  ( -8.705236002253083981E-17, -0.7431448254773934670, -0.6691306063588592368 ) ) ;
#36844=AXIS2_PLACEMENT_3D ( 'NONE', #20442, #37010, #9568 ) ;
#36846=CIRCLE ( 'NONE', #49183, 1.000000000000000888 ) ;
#36855=EDGE_CURVE ( 'NONE', #17287, #54496, #7222, .T. ) ;
#36861=CARTESIAN_POINT ( 'NONE',  ( 28.58578643762690419, 43.00000000000000711, -89.99999999999998579 ) ) ;
#36863=PLANE ( 'NONE',  #35377 ) ;
#36865=ORIENTED_EDGE ( 'NONE', *, *, #8032, .T. ) ;
#36876=CARTESIAN_POINT ( 'NONE',  ( 57.00000000000000000, 14.00000000000000000, 47.50402776293824303 ) ) ;
#36880=LINE ( 'NONE', #53035, #6005 ) ;
#36888=FILL_AREA_STYLE_COLOUR ( '', #62007 ) ;
#36889=LINE ( 'NONE', #26947, #402 ) ;
#36895=ORIENTED_EDGE ( 'NONE', *, *, #44467, .F. ) ;
#36900=SURFACE_STYLE_USAGE ( .BOTH. , #9102 ) ;
#36903=EDGE_LOOP ( 'NONE', ( #15565, #32950, #61127, #39366, #748, #17522, #31303 ) ) ;
#36935=EDGE_LOOP ( 'NONE', ( #48765, #16895, #65622, #30347, #43559, #68739 ) ) ;
#36941=FILL_AREA_STYLE ('',( #10179 ) ) ;
#36943=VECTOR ( 'NONE', #58145, 1000.000000000000000 ) ;
#36946=( LENGTH_UNIT ( ) NAMED_UNIT ( * ) SI_UNIT ( .MILLI., .METRE. ) );
#36953=CARTESIAN_POINT ( 'NONE',  ( 57.00000000000000000, 1.000000000000000000, -79.00402776293826435 ) ) ;
#36959=( GEOMETRIC_REPRESENTATION_CONTEXT ( 3 ) GLOBAL_UNCERTAINTY_ASSIGNED_CONTEXT ( ( #65646 ) ) GLOBAL_UNIT_ASSIGNED_CONTEXT ( ( #64620, #58292, #25573 ) ) REPRESENTATION_CONTEXT ( 'NONE', 'WORKASPACE' ) );
#36970=STYLED_ITEM ( 'NONE', ( #29850 ), #68163 ) ;
#36971=CARTESIAN_POINT ( 'NONE',  ( 82.09357085539578236, 5.000000000000000000, 37.00402776293825724 ) ) ;
#36972=EDGE_CURVE ( 'NONE', #11136, #11113, #9005, .T. ) ;
#36980=FACE_OUTER_BOUND ( 'NONE', #68456, .T. ) ;
#36983=AXIS2_PLACEMENT_3D ( 'NONE', #26303, #47847, #69244 ) ;
#36990=CARTESIAN_POINT ( 'NONE',  ( 23.32315385395093799, 24.57035872801869658, 27.19478135492500925 ) ) ;
#36999=( GEOMETRIC_REPRESENTATION_CONTEXT ( 3 ) GLOBAL_UNCERTAINTY_ASSIGNED_CONTEXT ( ( #46866 ) ) GLOBAL_UNIT_ASSIGNED_CONTEXT ( ( #43961, #60091, #11553 ) ) REPRESENTATION_CONTEXT ( 'NONE', 'WORKASPACE' ) );
#37010=DIRECTION ( 'NONE',  ( 1.000000000000000000, 0.000000000000000000, -1.300977106640434891E-16 ) ) ;
#37020=DIRECTION ( 'NONE',  ( -0.000000000000000000, 1.000000000000000000, -0.000000000000000000 ) ) ;
#37035=DIRECTION ( 'NONE',  ( -0.000000000000000000, 1.000000000000000000, -0.000000000000000000 ) ) ;
#37059=CARTESIAN_POINT ( 'NONE',  ( 27.99999999999999645, 5.000000000000000000, 24.00402776293821816 ) ) ;
#37063=( NAMED_UNIT ( * ) PLANE_ANGLE_UNIT ( ) SI_UNIT ( $, .RADIAN. ) );
#37067=CARTESIAN_POINT ( 'NONE',  ( 27.99999999999998934, 5.000000000000000000, 37.00402776293829277 ) ) ;
#37070=CARTESIAN_POINT ( 'NONE',  ( 10.00000000000000178, 43.00000000000000000, -90.00000000000000000 ) ) ;
#37072=CARTESIAN_POINT ( 'NONE',  ( 28.00000000000000000, 37.76051491742381216, -89.34202014332566932 ) ) ;
#37077=( LENGTH_UNIT ( ) NAMED_UNIT ( * ) SI_UNIT ( .MILLI., .METRE. ) );
#37080=( NAMED_UNIT ( * ) PLANE_ANGLE_UNIT ( ) SI_UNIT ( $, .RADIAN. ) );
#37084=PRESENTATION_STYLE_ASSIGNMENT (( #36397 ) ) ;
#37087=CIRCLE ( 'NONE', #8974, 1.000000000000000888 ) ;
#37092=CARTESIAN_POINT ( 'NONE',  ( 98.00000000000000000, 5.000000000000000000, 0.000000000000000000 ) ) ;
#37095=EDGE_CURVE ( 'NONE', #30008, #31521, #16242, .T. ) ;
#37101=COLOUR_RGB ( '', 0.08235294, 0.09019608, 0.10196078) ;
#37104=COLOUR_RGB ( '', 0.09019608, 0.27058824, 0.51372549) ;
#37110=AXIS2_PLACEMENT_3D ( 'NONE', #64738, #42628, #32714 ) ;
#37118=CARTESIAN_POINT ( 'NONE',  ( 20.00000000000001776, 14.00000000000000000, -29.68999999999999417 ) ) ;
#37121=CARTESIAN_POINT ( 'NONE',  ( 22.00000000000000711, 50.00000000000000000, -59.99999999999999289 ) ) ;
#37125=CARTESIAN_POINT ( 'NONE',  ( 2.000000000000022649, 50.00000000000000000, 60.00000000000000711 ) ) ;
#37136=ORIENTED_EDGE ( 'NONE', *, *, #29946, .T. ) ;
#37139=( NAMED_UNIT ( * ) PLANE_ANGLE_UNIT ( ) SI_UNIT ( $, .RADIAN. ) );
#37149=ORIENTED_EDGE ( 'NONE', *, *, #11431, .T. ) ;
#37150=FILL_AREA_STYLE_COLOUR ( '', #46070 ) ;
#37160=DIRECTION ( 'NONE',  ( 0.000000000000000000, 0.000000000000000000, -1.000000000000000000 ) ) ;
#37172=CARTESIAN_POINT ( 'NONE',  ( 57.00000000000000000, 0.000000000000000000, -60.00402776293827145 ) ) ;
#37182=DIRECTION ( 'NONE',  ( -1.084202172485504434E-16, 0.000000000000000000, -1.000000000000000000 ) ) ;
#37194=AXIS2_PLACEMENT_3D ( 'NONE', #67088, #40368, #36140 ) ;
#37201=DIRECTION ( 'NONE',  ( 0.000000000000000000, 0.000000000000000000, -1.000000000000000000 ) ) ;
#37203=VERTEX_POINT ( 'NONE', #48757 ) ;
#37214=DIRECTION ( 'NONE',  ( -0.000000000000000000, -1.000000000000000000, -0.000000000000000000 ) ) ;
#37257=ORIENTED_EDGE ( 'NONE', *, *, #26051, .F. ) ;
#37262=( GEOMETRIC_REPRESENTATION_CONTEXT ( 3 ) GLOBAL_UNCERTAINTY_ASSIGNED_CONTEXT ( ( #2492 ) ) GLOBAL_UNIT_ASSIGNED_CONTEXT ( ( #53386, #28695, #62699 ) ) REPRESENTATION_CONTEXT ( 'NONE', 'WORKASPACE' ) );
#37266=VERTEX_POINT ( 'NONE', #65925 ) ;
#37280=COLOUR_RGB ( '', 0.40784314, 0.44705882, 0.49803922) ;
#37283=( GEOMETRIC_REPRESENTATION_CONTEXT ( 3 ) GLOBAL_UNCERTAINTY_ASSIGNED_CONTEXT ( ( #43841 ) ) GLOBAL_UNIT_ASSIGNED_CONTEXT ( ( #32162, #37139, #48733 ) ) REPRESENTATION_CONTEXT ( 'NONE', 'WORKASPACE' ) );
#37287=MECHANICAL_DESIGN_GEOMETRIC_PRESENTATION_REPRESENTATION('',(#50757),#2379);
#37297=( GEOMETRIC_REPRESENTATION_CONTEXT ( 3 ) GLOBAL_UNCERTAINTY_ASSIGNED_CONTEXT ( ( #13786 ) ) GLOBAL_UNIT_ASSIGNED_CONTEXT ( ( #5457, #26907, #64913 ) ) REPRESENTATION_CONTEXT ( 'NONE', 'WORKASPACE' ) );
#37298=( NAMED_UNIT ( * ) SI_UNIT ( $, .STERADIAN. ) SOLID_ANGLE_UNIT ( ) );
#37301=DIRECTION ( 'NONE',  ( 0.000000000000000000, 0.000000000000000000, -1.000000000000000000 ) ) ;
#37311=( LENGTH_UNIT ( ) NAMED_UNIT ( * ) SI_UNIT ( .MILLI., .METRE. ) );
#37314=CYLINDRICAL_SURFACE ( 'NONE', #4794, 1.000000000000000888 ) ;
#37321=DIRECTION ( 'NONE',  ( 0.000000000000000000, 1.000000000000000000, 0.000000000000000000 ) ) ;
#37331=ORIENTED_EDGE ( 'NONE', *, *, #43039, .F. ) ;
#37336=CARTESIAN_POINT ( 'NONE',  ( 28.00000000000002842, 38.70020753820971748, 89.00000000000000000 ) ) ;
#37337=CARTESIAN_POINT ( 'NONE',  ( 7.000000000000017764, 42.74314482547740113, -27.71473342867655987 ) ) ;
#37338=COLOUR_RGB ( '', 0.66274510, 0.83137255, 0.94901961) ;
#37341=SURFACE_STYLE_USAGE ( .BOTH. , #31660 ) ;
#37344=ORIENTED_EDGE ( 'NONE', *, *, #32560, .T. ) ;
#37346=STYLED_ITEM ( 'NONE', ( #27152 ), #11833 ) ;
#37368=( LENGTH_UNIT ( ) NAMED_UNIT ( * ) SI_UNIT ( .MILLI., .METRE. ) );
#37370=( GEOMETRIC_REPRESENTATION_CONTEXT ( 3 ) GLOBAL_UNCERTAINTY_ASSIGNED_CONTEXT ( ( #44151 ) ) GLOBAL_UNIT_ASSIGNED_CONTEXT ( ( #5018, #3589, #57810 ) ) REPRESENTATION_CONTEXT ( 'NONE', 'WORKASPACE' ) );
#37382=( LENGTH_UNIT ( ) NAMED_UNIT ( * ) SI_UNIT ( .MILLI., .METRE. ) );
#37385=MECHANICAL_DESIGN_GEOMETRIC_PRESENTATION_REPRESENTATION('',(#12609),#53060);
#37386=DIRECTION ( 'NONE',  ( 0.000000000000000000, 0.000000000000000000, 1.000000000000000000 ) ) ;
#37396=FILL_AREA_STYLE_COLOUR ( '', #1967 ) ;
#37401=SURFACE_SIDE_STYLE ('',( #15921 ) ) ;
#37418=( LENGTH_UNIT ( ) NAMED_UNIT ( * ) SI_UNIT ( .MILLI., .METRE. ) );
#37425=LINE ( 'NONE', #4276, #22103 ) ;
#37437=PRESENTATION_STYLE_ASSIGNMENT (( #47651 ) ) ;
#37440=EDGE_LOOP ( 'NONE', ( #19955, #28600, #52143, #26919 ) ) ;
#37454=FILL_AREA_STYLE_COLOUR ( '', #7728 ) ;
#37463=FILL_AREA_STYLE ('',( #53579 ) ) ;
#37470=AXIS2_PLACEMENT_3D ( 'NONE', #60141, #54160, #54508 ) ;
#37471=EDGE_CURVE ( 'NONE', #42847, #67099, #49633, .T. ) ;
#37474=( NAMED_UNIT ( * ) PLANE_ANGLE_UNIT ( ) SI_UNIT ( $, .RADIAN. ) );
#37475=DIRECTION ( 'NONE',  ( 0.000000000000000000, 0.6449798928094537809, 0.7641995406119435064 ) ) ;
#37485=SURFACE_STYLE_USAGE ( .BOTH. , #15646 ) ;
#37494=DIRECTION ( 'NONE',  ( 0.000000000000000000, 0.7431448254773929118, -0.6691306063588596809 ) ) ;
#37506=CIRCLE ( 'NONE', #63263, 1.000000000000000888 ) ;
#37508=DIRECTION ( 'NONE',  ( -4.449603764765679692E-17, -0.9396926207859105373, -0.3420201433256630508 ) ) ;
#37512=VECTOR ( 'NONE', #27437, 1000.000000000000114 ) ;
#37514=CARTESIAN_POINT ( 'NONE',  ( 1.000000000000000000, 0.000000000000000000, 79.00402776293826435 ) ) ;
#37530=DIRECTION ( 'NONE',  ( 0.000000000000000000, -0.000000000000000000, -1.000000000000000000 ) ) ;
#37536=FILL_AREA_STYLE ('',( #62893 ) ) ;
#37537=ADVANCED_FACE ( 'NONE', ( #32383 ), #1373, .F. ) ;
#37544=( NAMED_UNIT ( * ) SI_UNIT ( $, .STERADIAN. ) SOLID_ANGLE_UNIT ( ) );
#37547=LINE ( 'NONE', #9385, #102 ) ;
#37559=CIRCLE ( 'NONE', #36400, 12.50000000000001066 ) ;
#37573=AXIS2_PLACEMENT_3D ( 'NONE', #31141, #35410, #41396 ) ;
#37578=DIRECTION ( 'NONE',  ( 0.000000000000000000, -1.000000000000000000, 0.000000000000000000 ) ) ;
#37579=COLOUR_RGB ( '', 0.66274510, 0.83137255, 0.94901961) ;
#37587=ORIENTED_EDGE ( 'NONE', *, *, #14378, .F. ) ;
#37589=CARTESIAN_POINT ( 'NONE',  ( 11.00000000000001776, 42.00000000000000000, 29.69000000000000128 ) ) ;
#37592=DIRECTION ( 'NONE',  ( -1.000000000000000000, 0.000000000000000000, 1.300977106640434891E-16 ) ) ;
#37595=LINE ( 'NONE', #5490, #11346 ) ;
#37596=DIRECTION ( 'NONE',  ( 3.717264591378879477E-17, 0.000000000000000000, -1.000000000000000000 ) ) ;
#37597=DIRECTION ( 'NONE',  ( 0.000000000000000000, 1.000000000000000000, 0.000000000000000000 ) ) ;
#37601=CARTESIAN_POINT ( 'NONE',  ( 6.000000000000017764, -60.04052944165106709, 35.50000000000000000 ) ) ;
#37604=EDGE_LOOP ( 'NONE', ( #56345, #1080, #49046, #55320, #47905, #44135, #14910, #5867 ) ) ;
#37621=CIRCLE ( 'NONE', #60053, 1.000000000000000888 ) ;
#37622=PRESENTATION_STYLE_ASSIGNMENT (( #9815 ) ) ;
#37626=ADVANCED_FACE ( 'NONE', ( #40285 ), #45593, .F. ) ;
#37631=DIRECTION ( 'NONE',  ( 0.000000000000000000, 0.000000000000000000, -1.000000000000000000 ) ) ;
#37633=UNCERTAINTY_MEASURE_WITH_UNIT (LENGTH_MEASURE( 1.000000000000000082E-05 ), #17828, 'distance_accuracy_value', 'NONE');
#37635=FILL_AREA_STYLE ('',( #32293 ) ) ;
#37655=ORIENTED_EDGE ( 'NONE', *, *, #9112, .F. ) ;
#37660=ORIENTED_EDGE ( 'NONE', *, *, #58608, .F. ) ;
#37661=( NAMED_UNIT ( * ) SI_UNIT ( $, .STERADIAN. ) SOLID_ANGLE_UNIT ( ) );
#37664=DIRECTION ( 'NONE',  ( -0.000000000000000000, -1.000000000000000000, -0.000000000000000000 ) ) ;
#37666=SURFACE_STYLE_USAGE ( .BOTH. , #21421 ) ;
#37678=VERTEX_POINT ( 'NONE', #4328 ) ;
#37695=LINE ( 'NONE', #38025, #59747 ) ;
#37701=FACE_OUTER_BOUND ( 'NONE', #38242, .T. ) ;
#37723=UNCERTAINTY_MEASURE_WITH_UNIT (LENGTH_MEASURE( 1.000000000000000082E-05 ), #14252, 'distance_accuracy_value', 'NONE');
#37726=ORIENTED_EDGE ( 'NONE', *, *, #25115, .T. ) ;
#37734=DIRECTION ( 'NONE',  ( -1.000000000000000000, -0.000000000000000000, -0.000000000000000000 ) ) ;
#37735=ORIENTED_EDGE ( 'NONE', *, *, #42538, .T. ) ;
#37757=EDGE_CURVE ( 'NONE', #27240, #39729, #316, .T. ) ;
#37766=DIRECTION ( 'NONE',  ( -0.000000000000000000, 0.000000000000000000, 1.000000000000000000 ) ) ;
#37781=ORIENTED_EDGE ( 'NONE', *, *, #69514, .F. ) ;
#37782=FACE_OUTER_BOUND ( 'NONE', #11249, .T. ) ;
#37789=SURFACE_STYLE_FILL_AREA ( #5020 ) ;
#37790=( GEOMETRIC_REPRESENTATION_CONTEXT ( 3 ) GLOBAL_UNCERTAINTY_ASSIGNED_CONTEXT ( ( #48254 ) ) GLOBAL_UNIT_ASSIGNED_CONTEXT ( ( #27628, #64926, #65973 ) ) REPRESENTATION_CONTEXT ( 'NONE', 'WORKASPACE' ) );
#37795=ORIENTED_EDGE ( 'NONE', *, *, #27688, .F. ) ;
#37796=DIRECTION ( 'NONE',  ( 4.625929269271505635E-16, -0.000000000000000000, 1.000000000000000000 ) ) ;
#37826=COLOUR_RGB ( '', 0.31764706, 0.68627451, 0.89019608) ;
#37828=( LENGTH_UNIT ( ) NAMED_UNIT ( * ) SI_UNIT ( .MILLI., .METRE. ) );
#37839=DIRECTION ( 'NONE',  ( -1.000000000000000000, -0.000000000000000000, 1.300977106640434891E-16 ) ) ;
#37842=CARTESIAN_POINT ( 'NONE',  ( 22.99999999999996447, 5.000000000000000000, 29.00402776293825369 ) ) ;
#37844=DIRECTION ( 'NONE',  ( 0.000000000000000000, 0.000000000000000000, 1.000000000000000000 ) ) ;
#37846=SURFACE_STYLE_USAGE ( .BOTH. , #6805 ) ;
#37855=CARTESIAN_POINT ( 'NONE',  ( 1.000000000000000000, 0.9999999999999991118, 79.00402776293826435 ) ) ;
#37859=( LENGTH_UNIT ( ) NAMED_UNIT ( * ) SI_UNIT ( .MILLI., .METRE. ) );
#37862=ORIENTED_EDGE ( 'NONE', *, *, #54494, .F. ) ;
#37876=EDGE_CURVE ( 'NONE', #48050, #10014, #66573, .T. ) ;
#37879=CIRCLE ( 'NONE', #1802, 12.50000000000001066 ) ;
#37880=CARTESIAN_POINT ( 'NONE',  ( 1.000000000000000888, 14.00000000000000533, -35.50000000000000000 ) ) ;
#37890=SURFACE_STYLE_USAGE ( .BOTH. , #32207 ) ;
#37898=ADVANCED_FACE ( 'NONE', ( #28201 ), #44807, .F. ) ;
#37905=CARTESIAN_POINT ( 'NONE',  ( 10.00000000000001954, 50.00000000000000000, 60.00000000000000000 ) ) ;
#37912=VERTEX_POINT ( 'NONE', #17710 ) ;
#37926=EDGE_CURVE ( 'NONE', #65056, #28347, #39518, .T. ) ;
#37939=FACE_OUTER_BOUND ( 'NONE', #45700, .T. ) ;
#37941=DIRECTION ( 'NONE',  ( -0.000000000000000000, -1.000000000000000000, -0.000000000000000000 ) ) ;
#37943=DIRECTION ( 'NONE',  ( 0.000000000000000000, -0.000000000000000000, -1.000000000000000000 ) ) ;
#37947=ORIENTED_EDGE ( 'NONE', *, *, #35216, .T. ) ;
#37952=FILL_AREA_STYLE ('',( #48497 ) ) ;
#37953=ORIENTED_EDGE ( 'NONE', *, *, #55798, .T. ) ;
#37960=ORIENTED_EDGE ( 'NONE', *, *, #23356, .T. ) ;
#37962=SURFACE_STYLE_FILL_AREA ( #20705 ) ;
#37967=CARTESIAN_POINT ( 'NONE',  ( 7.999999999999989342, 0.000000000000000000, 37.00402776293825724 ) ) ;
#38000=COLOUR_RGB ( '', 0.40784314, 0.44705882, 0.49803922) ;
#38001=CARTESIAN_POINT ( 'NONE',  ( 22.99999999999995026, 5.000000000000000000, -32.00402776293824303 ) ) ;
#38012=DIRECTION ( 'NONE',  ( 0.000000000000000000, 1.000000000000000000, 0.000000000000000000 ) ) ;
#38013=FILL_AREA_STYLE ('',( #11576 ) ) ;
#38025=CARTESIAN_POINT ( 'NONE',  ( 31.00000000000001421, 43.00000000000000000, 35.50000000000000000 ) ) ;
#38029=ORIENTED_EDGE ( 'NONE', *, *, #24686, .F. ) ;
#38034=ORIENTED_EDGE ( 'NONE', *, *, #7085, .T. ) ;
#38037=SURFACE_STYLE_FILL_AREA ( #58168 ) ;
#38043=VECTOR ( 'NONE', #9932, 1000.000000000000000 ) ;
#38047=CARTESIAN_POINT ( 'NONE',  ( 16.00000000000001776, 42.00000000000000000, 35.68999999999999062 ) ) ;
#38061=MECHANICAL_DESIGN_GEOMETRIC_PRESENTATION_REPRESENTATION('',(#40299),#66080);
#38067=DIRECTION ( 'NONE',  ( -0.000000000000000000, -1.000000000000000000, -0.000000000000000000 ) ) ;
#38068=VERTEX_POINT ( 'NONE', #25046 ) ;
#38070=ORIENTED_EDGE ( 'NONE', *, *, #64937, .T. ) ;
#38078=CARTESIAN_POINT ( 'NONE',  ( 12.00000000000001776, 14.00000000000000000, 29.68999999999999417 ) ) ;
#38079=ADVANCED_FACE ( 'NONE', ( #24002 ), #51100, .T. ) ;
#38094=EDGE_CURVE ( 'NONE', #39120, #34141, #21144, .T. ) ;
#38095=AXIS2_PLACEMENT_3D ( 'NONE', #7702, #62550, #8425 ) ;
#38098=COLOUR_RGB ( '', 0.08235294, 0.09019608, 0.10196078) ;
#38112=CIRCLE ( 'NONE', #53819, 4.999999999999997335 ) ;
#38117=CYLINDRICAL_SURFACE ( 'NONE', #4773, 5.000000000000004441 ) ;
#38127=COLOUR_RGB ( '', 0.66274510, 0.83137255, 0.94901961) ;
#38146=CYLINDRICAL_SURFACE ( 'NONE', #58457, 16.99999999999998579 ) ;
#38149=AXIS2_PLACEMENT_3D ( 'NONE', #66118, #50311, #18647 ) ;
#38153=VERTEX_POINT ( 'NONE', #58791 ) ;
#38160=CIRCLE ( 'NONE', #65070, 16.99999999999998579 ) ;
#38174=( NAMED_UNIT ( * ) PLANE_ANGLE_UNIT ( ) SI_UNIT ( $, .RADIAN. ) );
#38182=EDGE_LOOP ( 'NONE', ( #67429, #7731, #14616, #47073 ) ) ;
#38183=SURFACE_SIDE_STYLE ('',( #54658 ) ) ;
#38185=LINE ( 'NONE', #15516, #42756 ) ;
#38188=CARTESIAN_POINT ( 'NONE',  ( 3.000000000000030198, 43.00000000000000000, 90.00000000000000000 ) ) ;
#38216=DIRECTION ( 'NONE',  ( 1.000000000000000000, -0.000000000000000000, -1.300977106640434644E-16 ) ) ;
#38233=PRESENTATION_STYLE_ASSIGNMENT (( #17119 ) ) ;
#38238=DIRECTION ( 'NONE',  ( 0.000000000000000000, 0.000000000000000000, -1.000000000000000000 ) ) ;
#38242=EDGE_LOOP ( 'NONE', ( #67631, #6598, #39024, #9800 ) ) ;
#38269=ORIENTED_EDGE ( 'NONE', *, *, #45481, .T. ) ;
#38274=PLANE ( 'NONE',  #16825 ) ;
#38281=DIRECTION ( 'NONE',  ( 0.000000000000000000, 1.000000000000000000, 0.000000000000000000 ) ) ;
#38283=CARTESIAN_POINT ( 'NONE',  ( 4.000000000000030198, 38.70020753820971748, 89.00000000000000000 ) ) ;
#38302=COLOUR_RGB ( '', 0.31764706, 0.68627451, 0.89019608) ;
#38309=COLOUR_RGB ( '', 0.40784314, 0.44705882, 0.49803922) ;
#38310=UNCERTAINTY_MEASURE_WITH_UNIT (LENGTH_MEASURE( 1.000000000000000082E-05 ), #36946, 'distance_accuracy_value', 'NONE');
#38313=SURFACE_STYLE_USAGE ( .BOTH. , #49879 ) ;
#38325=COLOUR_RGB ( '', 0.66274510, 0.83137255, 0.94901961) ;
#38326=EDGE_CURVE ( 'NONE', #57943, #11591, #51065, .T. ) ;
#38329=DIRECTION ( 'NONE',  ( 0.000000000000000000, 0.000000000000000000, -1.000000000000000000 ) ) ;
#38333=EDGE_LOOP ( 'NONE', ( #56984, #33867, #50032, #47762, #30403, #30733, #12587, #16354 ) ) ;
#38334=CIRCLE ( 'NONE', #12470, 5.000000000000004441 ) ;
#38341=CARTESIAN_POINT ( 'NONE',  ( 179.4361977533490347, 0.000000000000000000, 103.7004518695263044 ) ) ;
#38345=MECHANICAL_DESIGN_GEOMETRIC_PRESENTATION_REPRESENTATION('',(#48440),#55105);
#38348=ORIENTED_EDGE ( 'NONE', *, *, #12206, .F. ) ;
#38354=LINE ( 'NONE', #31638, #61096 ) ;
#38355=ORIENTED_EDGE ( 'NONE', *, *, #38497, .F. ) ;
#38368=CARTESIAN_POINT ( 'NONE',  ( 26.00000000000001776, 15.00000000000000000, 29.68999999999999417 ) ) ;
#38373=UNCERTAINTY_MEASURE_WITH_UNIT (LENGTH_MEASURE( 1.000000000000000082E-05 ), #61862, 'distance_accuracy_value', 'NONE');
#38375=( GEOMETRIC_REPRESENTATION_CONTEXT ( 3 ) GLOBAL_UNCERTAINTY_ASSIGNED_CONTEXT ( ( #59361 ) ) GLOBAL_UNIT_ASSIGNED_CONTEXT ( ( #10081, #20628, #42140 ) ) REPRESENTATION_CONTEXT ( 'NONE', 'WORKASPACE' ) );
#38387=PRESENTATION_STYLE_ASSIGNMENT (( #42975 ) ) ;
#38403=EDGE_CURVE ( 'NONE', #31418, #1731, #45760, .T. ) ;
#38412=EDGE_CURVE ( 'NONE', #54537, #44052, #53327, .T. ) ;
#38423=DIRECTION ( 'NONE',  ( 1.000000000000000000, 0.000000000000000000, -0.000000000000000000 ) ) ;
#38431=ORIENTED_EDGE ( 'NONE', *, *, #5383, .F. ) ;
#38443=AXIS2_PLACEMENT_3D ( 'NONE', #26841, #69118, #20927 ) ;
#38449=DIRECTION ( 'NONE',  ( 1.000000000000000000, -0.000000000000000000, -1.300977106640434891E-16 ) ) ;
#38471=ORIENTED_EDGE ( 'NONE', *, *, #60809, .F. ) ;
#38473=VECTOR ( 'NONE', #32262, 1000.000000000000000 ) ;
#38476=SURFACE_STYLE_USAGE ( .BOTH. , #16986 ) ;
#38477=AXIS2_PLACEMENT_3D ( 'NONE', #32013, #25682, #20784 ) ;
#38486=( NAMED_UNIT ( * ) SI_UNIT ( $, .STERADIAN. ) SOLID_ANGLE_UNIT ( ) );
#38487=CYLINDRICAL_SURFACE ( 'NONE', #1030, 5.000000000000004441 ) ;
#38497=EDGE_CURVE ( 'NONE', #8099, #48634, #24953, .T. ) ;
#38498=SURFACE_STYLE_USAGE ( .BOTH. , #66198 ) ;
#38499=EDGE_CURVE ( 'NONE', #55142, #30954, #66491, .T. ) ;
#38503=( LENGTH_UNIT ( ) NAMED_UNIT ( * ) SI_UNIT ( .MILLI., .METRE. ) );
#38508=STYLED_ITEM ( 'NONE', ( #18754 ), #54771 ) ;
#38509=EDGE_CURVE ( 'NONE', #15308, #21029, #14067, .T. ) ;
#38517=ORIENTED_EDGE ( 'NONE', *, *, #42722, .F. ) ;
#38526=CARTESIAN_POINT ( 'NONE',  ( 22.00000000000002132, 50.00000000000000000, 59.99999999999999289 ) ) ;
#38528=UNCERTAINTY_MEASURE_WITH_UNIT (LENGTH_MEASURE( 1.000000000000000082E-05 ), #6453, 'distance_accuracy_value', 'NONE');
#38533=CARTESIAN_POINT ( 'NONE',  ( 2.000000000000008882, 50.00000000000000000, -59.99999999999999289 ) ) ;
#38534=VERTEX_POINT ( 'NONE', #68929 ) ;
#38536=VECTOR ( 'NONE', #31519, 1000.000000000000000 ) ;
#38542=ORIENTED_EDGE ( 'NONE', *, *, #53086, .T. ) ;
#38544=( LENGTH_UNIT ( ) NAMED_UNIT ( * ) SI_UNIT ( .MILLI., .METRE. ) );
#38553=CARTESIAN_POINT ( 'NONE',  ( 16.00000000000001776, 43.00000000000000000, -29.68999999999999417 ) ) ;
#38562=SURFACE_STYLE_USAGE ( .BOTH. , #22333 ) ;
#38577=SURFACE_STYLE_FILL_AREA ( #44881 ) ;
#38592=EDGE_CURVE ( 'NONE', #25561, #51395, #12825, .T. ) ;
#38594=( LENGTH_UNIT ( ) NAMED_UNIT ( * ) SI_UNIT ( .MILLI., .METRE. ) );
#38596=FACE_OUTER_BOUND ( 'NONE', #35016, .T. ) ;
#38623=CARTESIAN_POINT ( 'NONE',  ( 3.000000000000030198, 38.70020753820971748, 89.00000000000000000 ) ) ;
#38624=ORIENTED_EDGE ( 'NONE', *, *, #1447, .T. ) ;
#38625=FILL_AREA_STYLE ('',( #16472 ) ) ;
#38632=CIRCLE ( 'NONE', #64456, 5.000000000000004441 ) ;
#38635=EDGE_LOOP ( 'NONE', ( #3051, #12741, #8219, #36895 ) ) ;
#38639=SURFACE_SIDE_STYLE ('',( #17167 ) ) ;
#38640=ORIENTED_EDGE ( 'NONE', *, *, #6655, .T. ) ;
#38642=VECTOR ( 'NONE', #6775, 1000.000000000000000 ) ;
#38644=ADVANCED_FACE ( 'NONE', ( #59360 ), #902, .T. ) ;
#38648=VECTOR ( 'NONE', #62529, 1000.000000000000000 ) ;
#38660=VECTOR ( 'NONE', #47866, 1000.000000000000000 ) ;
#38663=( NAMED_UNIT ( * ) PLANE_ANGLE_UNIT ( ) SI_UNIT ( $, .RADIAN. ) );
#38668=AXIS2_PLACEMENT_3D ( 'NONE', #18133, #61024, #33607 ) ;
#38675=MECHANICAL_DESIGN_GEOMETRIC_PRESENTATION_REPRESENTATION('',(#50988),#10525);
#38676=EDGE_LOOP ( 'NONE', ( #25051, #31742, #48931, #39397 ) ) ;
#38677=( GEOMETRIC_REPRESENTATION_CONTEXT ( 3 ) GLOBAL_UNCERTAINTY_ASSIGNED_CONTEXT ( ( #5205 ) ) GLOBAL_UNIT_ASSIGNED_CONTEXT ( ( #10100, #53010, #19231 ) ) REPRESENTATION_CONTEXT ( 'NONE', 'WORKASPACE' ) );
#38680=SURFACE_STYLE_FILL_AREA ( #17215 ) ;
#38681=SURFACE_SIDE_STYLE ('',( #53441 ) ) ;
#38689=SURFACE_STYLE_FILL_AREA ( #22463 ) ;
#38694=DIRECTION ( 'NONE',  ( 0.000000000000000000, 0.000000000000000000, -1.000000000000000000 ) ) ;
#38704=CARTESIAN_POINT ( 'NONE',  ( 57.00000000000000000, 1.000000000000000000, 79.00402776293826435 ) ) ;
#38705=DIRECTION ( 'NONE',  ( 0.000000000000000000, 0.000000000000000000, -1.000000000000000000 ) ) ;
#38709=ORIENTED_EDGE ( 'NONE', *, *, #27092, .F. ) ;
#38710=ORIENTED_EDGE ( 'NONE', *, *, #34024, .F. ) ;
#38730=FACE_OUTER_BOUND ( 'NONE', #37440, .T. ) ;
#38733=( GEOMETRIC_REPRESENTATION_CONTEXT ( 3 ) GLOBAL_UNCERTAINTY_ASSIGNED_CONTEXT ( ( #59258 ) ) GLOBAL_UNIT_ASSIGNED_CONTEXT ( ( #23074, #28300, #1550 ) ) REPRESENTATION_CONTEXT ( 'NONE', 'WORKASPACE' ) );
#38764=( LENGTH_UNIT ( ) NAMED_UNIT ( * ) SI_UNIT ( .MILLI., .METRE. ) );
#38768=TOROIDAL_SURFACE ( 'NONE', #56709, 1.499999999999998668, 1.000000000000000000 ) ;
#38773=AXIS2_PLACEMENT_3D ( 'NONE', #14969, #19160, #8292 ) ;
#38798=LINE ( 'NONE', #47988, #56444 ) ;
#38811=( LENGTH_UNIT ( ) NAMED_UNIT ( * ) SI_UNIT ( .MILLI., .METRE. ) );
#38815=COLOUR_RGB ( '', 0.09019608, 0.27058824, 0.51372549) ;
#38821=SURFACE_STYLE_USAGE ( .BOTH. , #54925 ) ;
#38834=DIRECTION ( 'NONE',  ( -8.673617379884015751E-17, 0.000000000000000000, -1.000000000000000000 ) ) ;
#38839=ORIENTED_EDGE ( 'NONE', *, *, #46016, .F. ) ;
#38846=DIRECTION ( 'NONE',  ( -0.000000000000000000, -1.000000000000000000, -0.000000000000000000 ) ) ;
#38847=DIRECTION ( 'NONE',  ( 0.000000000000000000, 1.000000000000000000, 0.000000000000000000 ) ) ;
#38852=ORIENTED_EDGE ( 'NONE', *, *, #26825, .T. ) ;
#38858=EDGE_LOOP ( 'NONE', ( #12942, #48978, #61120, #44331 ) ) ;
#38859=SURFACE_STYLE_FILL_AREA ( #17395 ) ;
#38861=( NAMED_UNIT ( * ) SI_UNIT ( $, .STERADIAN. ) SOLID_ANGLE_UNIT ( ) );
#38864=SURFACE_STYLE_FILL_AREA ( #60277 ) ;
#38868=( GEOMETRIC_REPRESENTATION_CONTEXT ( 3 ) GLOBAL_UNCERTAINTY_ASSIGNED_CONTEXT ( ( #37723 ) ) GLOBAL_UNIT_ASSIGNED_CONTEXT ( ( #14252, #24434, #67723 ) ) REPRESENTATION_CONTEXT ( 'NONE', 'WORKASPACE' ) );
#38872=FILL_AREA_STYLE_COLOUR ( '', #2483 ) ;
#38913=PLANE ( 'NONE',  #64230 ) ;
#38914=UNCERTAINTY_MEASURE_WITH_UNIT (LENGTH_MEASURE( 1.000000000000000082E-05 ), #19441, 'distance_accuracy_value', 'NONE');
#38929=SURFACE_SIDE_STYLE ('',( #44893 ) ) ;
#38935=SURFACE_STYLE_FILL_AREA ( #13180 ) ;
#38939=AXIS2_PLACEMENT_3D ( 'NONE', #6799, #39548, #49734 ) ;
#38946=( LENGTH_UNIT ( ) NAMED_UNIT ( * ) SI_UNIT ( .MILLI., .METRE. ) );
#38953=ADVANCED_FACE ( 'NONE', ( #39530 ), #49721, .T. ) ;
#38954=DIRECTION ( 'NONE',  ( 0.000000000000000000, 0.4705882352941173075, 0.8823529411764708952 ) ) ;
#38957=SURFACE_STYLE_USAGE ( .BOTH. , #17488 ) ;
#38961=( NAMED_UNIT ( * ) SI_UNIT ( $, .STERADIAN. ) SOLID_ANGLE_UNIT ( ) );
#38964=( LENGTH_UNIT ( ) NAMED_UNIT ( * ) SI_UNIT ( .MILLI., .METRE. ) );
#38968=SURFACE_SIDE_STYLE ('',( #43898 ) ) ;
#38978=FILL_AREA_STYLE ('',( #27653 ) ) ;
#38982=VERTEX_POINT ( 'NONE', #67990 ) ;
#38985=CARTESIAN_POINT ( 'NONE',  ( 23.50000000000001776, 15.00000000000000000, -29.68999999999999417 ) ) ;
#38994=EDGE_LOOP ( 'NONE', ( #35380, #68939 ) ) ;
#38995=CARTESIAN_POINT ( 'NONE',  ( 8.000000000000024869, 0.000000000000000000, 32.00402776293825724 ) ) ;
#39004=CARTESIAN_POINT ( 'NONE',  ( 22.99999999999999289, 5.000000000000000000, -37.00402776293825013 ) ) ;
#39024=ORIENTED_EDGE ( 'NONE', *, *, #25712, .F. ) ;
#39037=CARTESIAN_POINT ( 'NONE',  ( 0.000000000000000000, 42.00000000000000000, 74.38749456993816978 ) ) ;
#39038=ORIENTED_EDGE ( 'NONE', *, *, #15018, .F. ) ;
#39041=DIRECTION ( 'NONE',  ( -0.000000000000000000, -1.000000000000000000, -0.000000000000000000 ) ) ;
#39044=ORIENTED_EDGE ( 'NONE', *, *, #37876, .T. ) ;
#39046=EDGE_CURVE ( 'NONE', #38153, #36170, #45524, .T. ) ;
#39050=( NAMED_UNIT ( * ) PLANE_ANGLE_UNIT ( ) SI_UNIT ( $, .RADIAN. ) );
#39054=CYLINDRICAL_SURFACE ( 'NONE', #1248, 1.000000000000000888 ) ;
#39055=ORIENTED_EDGE ( 'NONE', *, *, #57111, .T. ) ;
#39064=( NAMED_UNIT ( * ) PLANE_ANGLE_UNIT ( ) SI_UNIT ( $, .RADIAN. ) );
#39075=FILL_AREA_STYLE_COLOUR ( '', #33815 ) ;
#39086=CARTESIAN_POINT ( 'NONE',  ( 3.000000000000030198, 43.00000000000000000, 90.00000000000000000 ) ) ;
#39109=ORIENTED_EDGE ( 'NONE', *, *, #32023, .T. ) ;
#39117=( LENGTH_UNIT ( ) NAMED_UNIT ( * ) SI_UNIT ( .MILLI., .METRE. ) );
#39120=VERTEX_POINT ( 'NONE', #51443 ) ;
#39176=DIRECTION ( 'NONE',  ( 0.000000000000000000, 0.000000000000000000, -1.000000000000000000 ) ) ;
#39178=EDGE_CURVE ( 'NONE', #17013, #11331, #32389, .T. ) ;
#39190=CARTESIAN_POINT ( 'NONE',  ( 179.4361977533490347, 0.9999999999999991118, 103.7004518695263044 ) ) ;
#39191=VECTOR ( 'NONE', #8876, 1000.000000000000000 ) ;
#39207=DIRECTION ( 'NONE',  ( -0.000000000000000000, -1.000000000000000000, 0.000000000000000000 ) ) ;
#39212=ORIENTED_EDGE ( 'NONE', *, *, #42803, .T. ) ;
#39229=DIRECTION ( 'NONE',  ( 1.000000000000000000, -0.000000000000000000, -1.300977106640434891E-16 ) ) ;
#39235=DIRECTION ( 'NONE',  ( -1.000000000000000000, 0.000000000000000000, 1.300977106640434891E-16 ) ) ;
#39245=VERTEX_POINT ( 'NONE', #28492 ) ;
#39248=CARTESIAN_POINT ( 'NONE',  ( 31.00000000000002132, 14.00000000000000000, 80.00402776293826435 ) ) ;
#39253=( NAMED_UNIT ( * ) SI_UNIT ( $, .STERADIAN. ) SOLID_ANGLE_UNIT ( ) );
#39255=EDGE_CURVE ( 'NONE', #22411, #25215, #47900, .T. ) ;
#39261=FACE_OUTER_BOUND ( 'NONE', #3215, .T. ) ;
#39264=CARTESIAN_POINT ( 'NONE',  ( 8.000000000000000000, 0.000000000000000000, -72.00402776293825013 ) ) ;
#39270=( LENGTH_UNIT ( ) NAMED_UNIT ( * ) SI_UNIT ( .MILLI., .METRE. ) );
#39273=CARTESIAN_POINT ( 'NONE',  ( 1.000000000000000000, 42.00000000000000000, 0.000000000000000000 ) ) ;
#39282=B_SPLINE_CURVE_WITH_KNOTS ( 'NONE', 3,
 ( #60621, #6822, #21988, #90, #48399, #16388, #6142, #59943 ),
 .UNSPECIFIED., .F., .F.,
 ( 4, 2, 2, 4 ),
 ( -6.733023926842405106E-06, 0.0008427316310560229676, 0.001267463958547459645, 0.001692196286038896540 ),
 .UNSPECIFIED. ) ;
#39295=FILL_AREA_STYLE_COLOUR ( '', #29115 ) ;
#39297=FACE_OUTER_BOUND ( 'NONE', #21500, .T. ) ;
#39299=EDGE_LOOP ( 'NONE', ( #43288, #26859 ) ) ;
#39300=FILL_AREA_STYLE ('',( #44250 ) ) ;
#39307=( NAMED_UNIT ( * ) SI_UNIT ( $, .STERADIAN. ) SOLID_ANGLE_UNIT ( ) );
#39319=FILL_AREA_STYLE ('',( #6556 ) ) ;
#39323=STYLED_ITEM ( 'NONE', ( #20940 ), #58971 ) ;
#39324=ORIENTED_EDGE ( 'NONE', *, *, #23206, .F. ) ;
#39326=STYLED_ITEM ( 'NONE', ( #8521 ), #44302 ) ;
#39329=CARTESIAN_POINT ( 'NONE',  ( 57.00000000000000000, 16.00000000000000000, 72.50402776293826435 ) ) ;
#39336=PLANE ( 'NONE',  #16666 ) ;
#39337=AXIS2_PLACEMENT_3D ( 'NONE', #996, #18314, #66128 ) ;
#39343=AXIS2_PLACEMENT_3D ( 'NONE', #62419, #19498, #25131 ) ;
#39346=EDGE_CURVE ( 'NONE', #1416, #16364, #61219, .T. ) ;
#39359=VERTEX_POINT ( 'NONE', #7745 ) ;
#39364=CARTESIAN_POINT ( 'NONE',  ( 23.50000000000001776, 15.00000000000000000, 29.68999999999999417 ) ) ;
#39366=ORIENTED_EDGE ( 'NONE', *, *, #19689, .T. ) ;
#39379=DIRECTION ( 'NONE',  ( -1.239088197126290817E-16, 0.000000000000000000, -1.000000000000000000 ) ) ;
#39383=CYLINDRICAL_SURFACE ( 'NONE', #43124, 0.9999999999999992228 ) ;
#39384=VERTEX_POINT ( 'NONE', #56643 ) ;
#39397=ORIENTED_EDGE ( 'NONE', *, *, #67923, .T. ) ;
#39405=LINE ( 'NONE', #55547, #31516 ) ;
#39409=COLOUR_RGB ( '', 0.66274510, 0.83137255, 0.94901961) ;
#39424=( NAMED_UNIT ( * ) PLANE_ANGLE_UNIT ( ) SI_UNIT ( $, .RADIAN. ) );
#39426=DIRECTION ( 'NONE',  ( 0.3361263392814427542, 0.000000000000000000, 0.9418169057949938860 ) ) ;
#39428=DIRECTION ( 'NONE',  ( 1.000000000000000000, 0.000000000000000000, -1.300977106640435137E-16 ) ) ;
#39451=ORIENTED_EDGE ( 'NONE', *, *, #23217, .F. ) ;
#39461=FILL_AREA_STYLE_COLOUR ( '', #67677 ) ;
#39463=ORIENTED_EDGE ( 'NONE', *, *, #9253, .T. ) ;
#39484=LINE ( 'NONE', #49677, #41778 ) ;
#39492=COLOUR_RGB ( '', 0.40784314, 0.44705882, 0.49803922) ;
#39506=DIRECTION ( 'NONE',  ( -1.300977106640434891E-16, 0.000000000000000000, -1.000000000000000000 ) ) ;
#39513=( NAMED_UNIT ( * ) SI_UNIT ( $, .STERADIAN. ) SOLID_ANGLE_UNIT ( ) );
#39518=LINE ( 'NONE', #33186, #66833 ) ;
#39525=SURFACE_STYLE_USAGE ( .BOTH. , #50399 ) ;
#39530=FACE_OUTER_BOUND ( 'NONE', #36797, .T. ) ;
#39544=CIRCLE ( 'NONE', #36124, 1.000000000000000888 ) ;
#39545=FACE_OUTER_BOUND ( 'NONE', #57587, .T. ) ;
#39548=DIRECTION ( 'NONE',  ( -0.000000000000000000, -1.000000000000000000, -0.000000000000000000 ) ) ;
#39551=ORIENTED_EDGE ( 'NONE', *, *, #19634, .F. ) ;
#39557=CARTESIAN_POINT ( 'NONE',  ( 57.00000000000000000, 16.00000000000000000, -55.00402776293825724 ) ) ;
#39560=( NAMED_UNIT ( * ) PLANE_ANGLE_UNIT ( ) SI_UNIT ( $, .RADIAN. ) );
#39563=EDGE_LOOP ( 'NONE', ( #41439, #12070, #34721, #1974 ) ) ;
#39575=( GEOMETRIC_REPRESENTATION_CONTEXT ( 3 ) GLOBAL_UNCERTAINTY_ASSIGNED_CONTEXT ( ( #53742 ) ) GLOBAL_UNIT_ASSIGNED_CONTEXT ( ( #37382, #58787, #5294 ) ) REPRESENTATION_CONTEXT ( 'NONE', 'WORKASPACE' ) );
#39585=LINE ( 'NONE', #56060, #66066 ) ;
#39595=CARTESIAN_POINT ( 'NONE',  ( 8.000000000000000000, 5.000000000000000000, 72.00402776293825013 ) ) ;
#39608=( GEOMETRIC_REPRESENTATION_CONTEXT ( 3 ) GLOBAL_UNCERTAINTY_ASSIGNED_CONTEXT ( ( #67259 ) ) GLOBAL_UNIT_ASSIGNED_CONTEXT ( ( #62298, #3502, #34185 ) ) REPRESENTATION_CONTEXT ( 'NONE', 'WORKASPACE' ) );
#39613=MECHANICAL_DESIGN_GEOMETRIC_PRESENTATION_REPRESENTATION('',(#17118),#20501);
#39617=FILL_AREA_STYLE_COLOUR ( '', #39761 ) ;
#39628=MECHANICAL_DESIGN_GEOMETRIC_PRESENTATION_REPRESENTATION('',(#51963),#23881);
#39651=EDGE_CURVE ( 'NONE', #69192, #56560, #51250, .T. ) ;
#39663=STYLED_ITEM ( 'NONE', ( #4203 ), #47383 ) ;
#39666=ORIENTED_EDGE ( 'NONE', *, *, #67923, .F. ) ;
#39668=AXIS2_PLACEMENT_3D ( 'NONE', #64944, #34253, #48475 ) ;
#39673=AXIS2_PLACEMENT_3D ( 'NONE', #1117, #54977, #16710 ) ;
#39679=CIRCLE ( 'NONE', #32933, 16.00000000000000711 ) ;
#39684=FILL_AREA_STYLE ('',( #60741 ) ) ;
#39687=CARTESIAN_POINT ( 'NONE',  ( 57.00000000000000000, 14.00000000000000000, 80.00402776293826435 ) ) ;
#39688=AXIS2_PLACEMENT_3D ( 'NONE', #66270, #18096, #60634 ) ;
#39695=VECTOR ( 'NONE', #27057, 1000.000000000000000 ) ;
#39702=DIRECTION ( 'NONE',  ( -0.000000000000000000, -1.000000000000000000, -0.000000000000000000 ) ) ;
#39706=CARTESIAN_POINT ( 'NONE',  ( 10.00000000000001954, 42.00000000000000000, -28.38386403503541899 ) ) ;
#39712=( LENGTH_UNIT ( ) NAMED_UNIT ( * ) SI_UNIT ( .MILLI., .METRE. ) );
#39717=CARTESIAN_POINT ( 'NONE',  ( 24.70577775730027881, 26.00000000000004619, -27.50000000000000711 ) ) ;
#39721=DIRECTION ( 'NONE',  ( -1.000000000000000000, 0.000000000000000000, 0.000000000000000000 ) ) ;
#39723=CARTESIAN_POINT ( 'NONE',  ( 2.000000000000015543, 26.00000000000000355, 23.99999999999999645 ) ) ;
#39727=EDGE_CURVE ( 'NONE', #65467, #48456, #16867, .T. ) ;
#39729=VERTEX_POINT ( 'NONE', #60423 ) ;
#39731=SURFACE_STYLE_USAGE ( .BOTH. , #8396 ) ;
#39735=AXIS2_PLACEMENT_3D ( 'NONE', #14010, #2341, #56563 ) ;
#39737=LINE ( 'NONE', #7003, #30511 ) ;
#39758=ORIENTED_EDGE ( 'NONE', *, *, #24101, .F. ) ;
#39761=COLOUR_RGB ( '', 0.40784314, 0.44705882, 0.49803922) ;
#39774=SURFACE_STYLE_USAGE ( .BOTH. , #23899 ) ;
#39776=MECHANICAL_DESIGN_GEOMETRIC_PRESENTATION_REPRESENTATION('',(#13875),#59969);
#39777=CARTESIAN_POINT ( 'NONE',  ( 57.00000000000000000, 0.000000000000000000, 65.00402776293825013 ) ) ;
#39780=CARTESIAN_POINT ( 'NONE',  ( 1.000000000000000000, 43.00000000000000000, -79.00402776293826435 ) ) ;
#39781=ORIENTED_EDGE ( 'NONE', *, *, #3307, .F. ) ;
#39785=SURFACE_STYLE_USAGE ( .BOTH. , #1359 ) ;
#39789=ORIENTED_EDGE ( 'NONE', *, *, #27475, .T. ) ;
#39798=AXIS2_PLACEMENT_3D ( 'NONE', #59756, #11221, #32669 ) ;
#39799=ORIENTED_EDGE ( 'NONE', *, *, #49935, .T. ) ;
#39807=SURFACE_SIDE_STYLE ('',( #50333 ) ) ;
#39821=LINE ( 'NONE', #23597, #31035 ) ;
#39834=ORIENTED_EDGE ( 'NONE', *, *, #16406, .F. ) ;
#39835=UNCERTAINTY_MEASURE_WITH_UNIT (LENGTH_MEASURE( 1.000000000000000082E-05 ), #69086, 'distance_accuracy_value', 'NONE');
#39851=EDGE_CURVE ( 'NONE', #39384, #35304, #25380, .T. ) ;
#39866=AXIS2_PLACEMENT_3D ( 'NONE', #36669, #20073, #41235 ) ;
#39880=( NAMED_UNIT ( * ) SI_UNIT ( $, .STERADIAN. ) SOLID_ANGLE_UNIT ( ) );
#39881=EDGE_CURVE ( 'NONE', #61983, #30684, #50582, .T. ) ;
#39887=ORIENTED_EDGE ( 'NONE', *, *, #6279, .F. ) ;
#39894=CARTESIAN_POINT ( 'NONE',  ( 3.000000000000030198, 43.00000000000000000, 90.00000000000000000 ) ) ;
#39897=VECTOR ( 'NONE', #46721, 1000.000000000000000 ) ;
#39913=COLOUR_RGB ( '', 0.40784314, 0.44705882, 0.49803922) ;
#39916=ORIENTED_EDGE ( 'NONE', *, *, #7388, .F. ) ;
#39925=CARTESIAN_POINT ( 'NONE',  ( 31.00000000000002132, 42.47058823529412308, 74.11764705882352189 ) ) ;
#39935=CARTESIAN_POINT ( 'NONE',  ( 10.00000000000002309, 43.00000000000000000, 74.38749456993816978 ) ) ;
#39946=STYLED_ITEM ( 'NONE', ( #8880 ), #56478 ) ;
#39950=( GEOMETRIC_REPRESENTATION_CONTEXT ( 3 ) GLOBAL_UNCERTAINTY_ASSIGNED_CONTEXT ( ( #63732 ) ) GLOBAL_UNIT_ASSIGNED_CONTEXT ( ( #15304, #42048, #2921 ) ) REPRESENTATION_CONTEXT ( 'NONE', 'WORKASPACE' ) );
#39958=CYLINDRICAL_SURFACE ( 'NONE', #59287, 0.9999999999999974465 ) ;
#39968=SURFACE_STYLE_USAGE ( .BOTH. , #33949 ) ;
#39971=VERTEX_POINT ( 'NONE', #2688 ) ;
#39976=EDGE_CURVE ( 'NONE', #69112, #31733, #55762, .T. ) ;
#39986=DIRECTION ( 'NONE',  ( 0.000000000000000000, 0.000000000000000000, 1.000000000000000000 ) ) ;
#39987=CARTESIAN_POINT ( 'NONE',  ( 6.516641522221524596, 43.00000000000000711, 28.13388297856903719 ) ) ;
#39992=CARTESIAN_POINT ( 'NONE',  ( 22.00000000000002132, 50.00000000000000000, 65.00000000000000000 ) ) ;
#40004=EDGE_CURVE ( 'NONE', #34188, #18052, #52378, .T. ) ;
#40014=EDGE_CURVE ( 'NONE', #65503, #17013, #60235, .T. ) ;
#40015=CARTESIAN_POINT ( 'NONE',  ( 57.00000000000000000, 14.00000000000000000, -80.00402776293826435 ) ) ;
#40020=SURFACE_STYLE_USAGE ( .BOTH. , #18533 ) ;
#40021=VERTEX_POINT ( 'NONE', #14327 ) ;
#40023=DIRECTION ( 'NONE',  ( 0.000000000000000000, 0.000000000000000000, 1.000000000000000000 ) ) ;
#40041=DIRECTION ( 'NONE',  ( 0.000000000000000000, -0.000000000000000000, -1.000000000000000000 ) ) ;
#40046=CARTESIAN_POINT ( 'NONE',  ( 27.00000000000001776, 43.00000000000000000, -34.49999999999999289 ) ) ;
#40047=FACE_OUTER_BOUND ( 'NONE', #43149, .T. ) ;
#40051=CIRCLE ( 'NONE', #9721, 1.000000000000000888 ) ;
#40075=CARTESIAN_POINT ( 'NONE',  ( 24.70577775730027881, 26.17803040854050778, -27.50000000000000711 ) ) ;
#40098=ORIENTED_EDGE ( 'NONE', *, *, #31448, .F. ) ;
#40101=EDGE_CURVE ( 'NONE', #28347, #2934, #47075, .T. ) ;
#40113=FILL_AREA_STYLE_COLOUR ( '', #4453 ) ;
#40119=CARTESIAN_POINT ( 'NONE',  ( 31.00000000000000711, -60.04052944165106709, -36.50000000000000000 ) ) ;
#40127=FILL_AREA_STYLE ('',( #7727 ) ) ;
#40133=ORIENTED_EDGE ( 'NONE', *, *, #49380, .F. ) ;
#40138=DIRECTION ( 'NONE',  ( 0.000000000000000000, 0.000000000000000000, -1.000000000000000000 ) ) ;
#40160=EDGE_CURVE ( 'NONE', #34731, #24720, #56911, .T. ) ;
#40178=VERTEX_POINT ( 'NONE', #43544 ) ;
#40185=SURFACE_STYLE_USAGE ( .BOTH. , #13778 ) ;
#40189=PLANE ( 'NONE',  #41583 ) ;
#40190=LINE ( 'NONE', #56336, #62662 ) ;
#40199=FACE_OUTER_BOUND ( 'NONE', #53436, .T. ) ;
#40206=DIRECTION ( 'NONE',  ( 0.000000000000000000, -1.000000000000000000, 0.000000000000000000 ) ) ;
#40212=ORIENTED_EDGE ( 'NONE', *, *, #68979, .F. ) ;
#40215=ORIENTED_EDGE ( 'NONE', *, *, #1693, .F. ) ;
#40220=SURFACE_STYLE_FILL_AREA ( #13450 ) ;
#40221=EDGE_CURVE ( 'NONE', #9855, #16376, #17137, .T. ) ;
#40231=( NAMED_UNIT ( * ) PLANE_ANGLE_UNIT ( ) SI_UNIT ( $, .RADIAN. ) );
#40232=PRESENTATION_STYLE_ASSIGNMENT (( #29293 ) ) ;
#40246=FILL_AREA_STYLE ('',( #8578 ) ) ;
#40258=LINE ( 'NONE', #33912, #22358 ) ;
#40262=CARTESIAN_POINT ( 'NONE',  ( 24.68205682311551641, 25.64738524273002440, -27.48638708064855507 ) ) ;
#40269=( LENGTH_UNIT ( ) NAMED_UNIT ( * ) SI_UNIT ( .MILLI., .METRE. ) );
#40271=COLOUR_RGB ( '', 0.72549020, 0.75294118, 0.79215686) ;
#40275=ADVANCED_FACE ( 'NONE', ( #6521 ), #5475, .F. ) ;
#40277=EDGE_CURVE ( 'NONE', #22405, #46237, #50851, .T. ) ;
#40285=FACE_OUTER_BOUND ( 'NONE', #4968, .T. ) ;
#40293=EDGE_CURVE ( 'NONE', #11591, #57943, #62523, .T. ) ;
#40299=STYLED_ITEM ( 'NONE', ( #8723 ), #959 ) ;
#40301=EDGE_CURVE ( 'NONE', #12604, #35982, #11973, .T. ) ;
#40305=ORIENTED_EDGE ( 'NONE', *, *, #26825, .F. ) ;
#40313=FACE_OUTER_BOUND ( 'NONE', #32314, .T. ) ;
#40314=CARTESIAN_POINT ( 'NONE',  ( 27.99999999999999645, 0.000000000000000000, 24.00402776293821816 ) ) ;
#40322=ORIENTED_EDGE ( 'NONE', *, *, #65978, .T. ) ;
#40329=( NAMED_UNIT ( * ) PLANE_ANGLE_UNIT ( ) SI_UNIT ( $, .RADIAN. ) );
#40334=CARTESIAN_POINT ( 'NONE',  ( 3.000000000000030198, 42.00000000000000000, 80.00402776293826435 ) ) ;
#40339=CARTESIAN_POINT ( 'NONE',  ( 6.330869393641157750, 43.00000000000000000, -28.38386403503541899 ) ) ;
#40347=VERTEX_POINT ( 'NONE', #55777 ) ;
#40364=STYLED_ITEM ( 'NONE', ( #55992 ), #44200 ) ;
#40367=CIRCLE ( 'NONE', #10041, 1.000000000000000888 ) ;
#40368=DIRECTION ( 'NONE',  ( -0.000000000000000000, -1.000000000000000000, 0.000000000000000000 ) ) ;
#40370=EDGE_CURVE ( 'NONE', #16530, #45721, #8620, .T. ) ;
#40371=SURFACE_SIDE_STYLE ('',( #22803 ) ) ;
#40381=( GEOMETRIC_REPRESENTATION_CONTEXT ( 3 ) GLOBAL_UNCERTAINTY_ASSIGNED_CONTEXT ( ( #4601 ) ) GLOBAL_UNIT_ASSIGNED_CONTEXT ( ( #7400, #11972, #6681 ) ) REPRESENTATION_CONTEXT ( 'NONE', 'WORKASPACE' ) );
#40390=MECHANICAL_DESIGN_GEOMETRIC_PRESENTATION_REPRESENTATION('',(#4396),#43785);
#40392=PLANE ( 'NONE',  #36221 ) ;
#40405=DIRECTION ( 'NONE',  ( 1.000000000000000000, 0.000000000000000000, -1.300977106640434891E-16 ) ) ;
#40409=DIRECTION ( 'NONE',  ( -1.000000000000000000, 0.000000000000000000, 0.000000000000000000 ) ) ;
#40410=CARTESIAN_POINT ( 'NONE',  ( 2.000000000000022649, 50.00000000000000000, 60.00000000000000711 ) ) ;
#40414=AXIS2_PLACEMENT_3D ( 'NONE', #6533, #61055, #12871 ) ;
#40438=EDGE_CURVE ( 'NONE', #37912, #23750, #36776, .T. ) ;
#40445=DIRECTION ( 'NONE',  ( 1.000000000000000000, -0.000000000000000000, -1.300977106640434891E-16 ) ) ;
#40451=COLOUR_RGB ( '', 0.08235294, 0.09019608, 0.10196078) ;
#40452=SURFACE_SIDE_STYLE ('',( #30544 ) ) ;
#40456=CARTESIAN_POINT ( 'NONE',  ( 28.00000000000000000, 43.00000000000000000, -79.00402776293826435 ) ) ;
#40457=ORIENTED_EDGE ( 'NONE', *, *, #9253, .F. ) ;
#40469=AXIS2_PLACEMENT_3D ( 'NONE', #49240, #22498, #43995 ) ;
#40470=DIRECTION ( 'NONE',  ( -3.469446951953611033E-15, 0.000000000000000000, -1.000000000000000000 ) ) ;
#40472=MECHANICAL_DESIGN_GEOMETRIC_PRESENTATION_REPRESENTATION('',(#16925),#45007);
#40482=EDGE_CURVE ( 'NONE', #28531, #56560, #34518, .T. ) ;
#40483=EDGE_LOOP ( 'NONE', ( #67826, #48632, #14074 ) ) ;
#40488=MECHANICAL_DESIGN_GEOMETRIC_PRESENTATION_REPRESENTATION('',(#47238),#32607);
#40491=MECHANICAL_DESIGN_GEOMETRIC_PRESENTATION_REPRESENTATION('',(#5595),#58392);
#40493=SURFACE_STYLE_USAGE ( .BOTH. , #18983 ) ;
#40507=LINE ( 'NONE', #24988, #47607 ) ;
#40508=EDGE_LOOP ( 'NONE', ( #4936, #12889, #41986, #48457 ) ) ;
#40515=STYLED_ITEM ( 'NONE', ( #28023 ), #16655 ) ;
#40520=ORIENTED_EDGE ( 'NONE', *, *, #29440, .F. ) ;
#40521=ORIENTED_EDGE ( 'NONE', *, *, #9307, .F. ) ;
#40533=EDGE_CURVE ( 'NONE', #56835, #22411, #6394, .T. ) ;
#40541=SURFACE_SIDE_STYLE ('',( #45819 ) ) ;
#40543=COLOUR_RGB ( '', 0.40784314, 0.44705882, 0.49803922) ;
#40547=LINE ( 'NONE', #2838, #7789 ) ;
#40552=AXIS2_PLACEMENT_3D ( 'NONE', #290, #21461, #26391 ) ;
#40567=CARTESIAN_POINT ( 'NONE',  ( 1.709458476932651091E-14, 14.00000000000000533, 35.50000000000000000 ) ) ;
#40568=ORIENTED_EDGE ( 'NONE', *, *, #12746, .F. ) ;
#40569=TOROIDAL_SURFACE ( 'NONE', #24806, 4.000000000000000000, 1.000000000000000000 ) ;
#40573=COLOUR_RGB ( '', 0.31764706, 0.68627451, 0.89019608) ;
#40581=UNCERTAINTY_MEASURE_WITH_UNIT (LENGTH_MEASURE( 1.000000000000000082E-05 ), #20096, 'distance_accuracy_value', 'NONE');
#40591=EDGE_LOOP ( 'NONE', ( #8293, #20767, #48568, #38542 ) ) ;
#40595=SURFACE_STYLE_USAGE ( .BOTH. , #3953 ) ;
#40610=SPHERICAL_SURFACE ( 'NONE', #13426, 1.000000000000000000 ) ;
#40630=CARTESIAN_POINT ( 'NONE',  ( 30.99999999999998579, 5.000000000000000000, 72.00402776293822171 ) ) ;
#40637=VECTOR ( 'NONE', #20562, 1000.000000000000000 ) ;
#40641=AXIS2_PLACEMENT_3D ( 'NONE', #22364, #49456, #63115 ) ;
#40644=( LENGTH_UNIT ( ) NAMED_UNIT ( * ) SI_UNIT ( .MILLI., .METRE. ) );
#40645=PRESENTATION_STYLE_ASSIGNMENT (( #4000 ) ) ;
#40663=CARTESIAN_POINT ( 'NONE',  ( 23.50000000000001776, 15.00000000000000000, 27.18999999999999417 ) ) ;
#40664=CARTESIAN_POINT ( 'NONE',  ( 179.4361977533490347, 0.000000000000000000, -103.7004518695263044 ) ) ;
#40670=SHAPE_REPRESENTATION ( '1. Base', ( #42840 ), #53979 ) ;
#40671=MECHANICAL_DESIGN_GEOMETRIC_PRESENTATION_REPRESENTATION('',(#64190),#37283);
#40690=EDGE_CURVE ( 'NONE', #15308, #53146, #44654, .T. ) ;
#40696=DIRECTION ( 'NONE',  ( 0.000000000000000000, 0.000000000000000000, 1.000000000000000000 ) ) ;
#40701=DIRECTION ( 'NONE',  ( 1.000000000000000000, -0.000000000000000000, 0.000000000000000000 ) ) ;
#40709=ORIENTED_EDGE ( 'NONE', *, *, #2059, .T. ) ;
#40710=LINE ( 'NONE', #56150, #2113 ) ;
#40712=FACE_OUTER_BOUND ( 'NONE', #29804, .T. ) ;
#40716=( NAMED_UNIT ( * ) SI_UNIT ( $, .STERADIAN. ) SOLID_ANGLE_UNIT ( ) );
#40739=ORIENTED_EDGE ( 'NONE', *, *, #20580, .F. ) ;
#40740=VERTEX_POINT ( 'NONE', #17659 ) ;
#40743=ORIENTED_EDGE ( 'NONE', *, *, #36855, .F. ) ;
#40762=SURFACE_SIDE_STYLE ('',( #24528 ) ) ;
#40763=EDGE_CURVE ( 'NONE', #20328, #330, #14285, .T. ) ;
#40767=FACE_OUTER_BOUND ( 'NONE', #13405, .T. ) ;
#40780=ORIENTED_EDGE ( 'NONE', *, *, #51249, .F. ) ;
#40788=STYLED_ITEM ( 'NONE', ( #13728 ), #22800 ) ;
#40802=SURFACE_SIDE_STYLE ('',( #63269 ) ) ;
#40803=VECTOR ( 'NONE', #63897, 1000.000000000000000 ) ;
#40804=VECTOR ( 'NONE', #34777, 1000.000000000000000 ) ;
#40809=CARTESIAN_POINT ( 'NONE',  ( 31.00000000000000000, 15.00000000000000000, -79.00402776293826435 ) ) ;
#40811=PLANE ( 'NONE',  #46220 ) ;
#40817=FACE_OUTER_BOUND ( 'NONE', #24634, .T. ) ;
#40825=DIRECTION ( 'NONE',  ( -1.000000000000000000, 0.000000000000000000, 1.300977106640434891E-16 ) ) ;
#40830=CARTESIAN_POINT ( 'NONE',  ( 92.41620014002536720, 0.000000000000000000, -29.00402776293825724 ) ) ;
#40839=COLOUR_RGB ( '', 0.72549020, 0.75294118, 0.79215686) ;
#40857=LINE ( 'NONE', #3123, #67667 ) ;
#40860=VERTEX_POINT ( 'NONE', #56656 ) ;
#40862=ORIENTED_EDGE ( 'NONE', *, *, #8766, .T. ) ;
#40871=EDGE_CURVE ( 'NONE', #1278, #62287, #63735, .T. ) ;
#40884=AXIS2_PLACEMENT_3D ( 'NONE', #35870, #57316, #4530 ) ;
#40886=CARTESIAN_POINT ( 'NONE',  ( 57.00000000000000000, 16.00000000000000000, -47.50402776293824303 ) ) ;
#40890=MECHANICAL_DESIGN_GEOMETRIC_PRESENTATION_REPRESENTATION('',(#24028),#45423);
#40894=CIRCLE ( 'NONE', #10540, 1.000000000000000888 ) ;
#40895=LINE ( 'NONE', #57744, #48328 ) ;
#40915=DIRECTION ( 'NONE',  ( 0.000000000000000000, 0.000000000000000000, -1.000000000000000000 ) ) ;
#40920=( GEOMETRIC_REPRESENTATION_CONTEXT ( 3 ) GLOBAL_UNCERTAINTY_ASSIGNED_CONTEXT ( ( #62909 ) ) GLOBAL_UNIT_ASSIGNED_CONTEXT ( ( #53041, #63242, #36560 ) ) REPRESENTATION_CONTEXT ( 'NONE', 'WORKASPACE' ) );
#40925=AXIS2_PLACEMENT_3D ( 'NONE', #50839, #7237, #3283 ) ;
#40941=CARTESIAN_POINT ( 'NONE',  ( 4.000000000000002665, 43.00000000000000000, -79.00402776293826435 ) ) ;
#40948=CARTESIAN_POINT ( 'NONE',  ( 31.28473954617955854, 42.96841842781390142, 45.59272046071828299 ) ) ;
#40954=FILL_AREA_STYLE ('',( #51139 ) ) ;
#40966=CIRCLE ( 'NONE', #49932, 4.999999999999997335 ) ;
#40967=FACE_OUTER_BOUND ( 'NONE', #30066, .T. ) ;
#40970=AXIS2_PLACEMENT_3D ( 'NONE', #55383, #43832, #18455 ) ;
#40982=AXIS2_PLACEMENT_3D ( 'NONE', #64521, #37839, #433 ) ;
#40987=( LENGTH_UNIT ( ) NAMED_UNIT ( * ) SI_UNIT ( .MILLI., .METRE. ) );
#40991=VECTOR ( 'NONE', #3094, 1000.000000000000000 ) ;
#41002=ORIENTED_EDGE ( 'NONE', *, *, #62254, .T. ) ;
#41012=VERTEX_POINT ( 'NONE', #54127 ) ;
#41013=DIRECTION ( 'NONE',  ( -0.000000000000000000, 1.000000000000000000, -0.000000000000000000 ) ) ;
#41015=DIRECTION ( 'NONE',  ( -0.000000000000000000, -0.000000000000000000, -1.000000000000000000 ) ) ;
#41018=EDGE_CURVE ( 'NONE', #9552, #417, #31641, .T. ) ;
#41019=CARTESIAN_POINT ( 'NONE',  ( 16.00000000000001776, 42.00000000000000000, 29.68999999999999417 ) ) ;
#41022=AXIS2_PLACEMENT_3D ( 'NONE', #54643, #60274, #23002 ) ;
#41029=EDGE_CURVE ( 'NONE', #49208, #57733, #58055, .T. ) ;
#41030=( NAMED_UNIT ( * ) SI_UNIT ( $, .STERADIAN. ) SOLID_ANGLE_UNIT ( ) );
#41031=UNCERTAINTY_MEASURE_WITH_UNIT (LENGTH_MEASURE( 1.000000000000000082E-05 ), #4126, 'distance_accuracy_value', 'NONE');
#41032=ORIENTED_EDGE ( 'NONE', *, *, #45624, .T. ) ;
#41043=CARTESIAN_POINT ( 'NONE',  ( 31.00000000000002132, 43.00000000000000000, 74.38749456993815556 ) ) ;
#41045=CIRCLE ( 'NONE', #47804, 5.000000000000004441 ) ;
#41051=LINE ( 'NONE', #24141, #69410 ) ;
#41062=UNCERTAINTY_MEASURE_WITH_UNIT (LENGTH_MEASURE( 1.000000000000000082E-05 ), #47561, 'distance_accuracy_value', 'NONE');
#41084=UNCERTAINTY_MEASURE_WITH_UNIT (LENGTH_MEASURE( 1.000000000000000082E-05 ), #786, 'distance_accuracy_value', 'NONE');
#41086=FACE_OUTER_BOUND ( 'NONE', #946, .T. ) ;
#41090=CARTESIAN_POINT ( 'NONE',  ( 31.00000000000000711, 15.00000000000000711, -36.50000000000000000 ) ) ;
#41094=ORIENTED_EDGE ( 'NONE', *, *, #26170, .F. ) ;
#41099=EDGE_LOOP ( 'NONE', ( #36428, #43943, #17793, #69436 ) ) ;
#41100=DIRECTION ( 'NONE',  ( 0.000000000000000000, 0.000000000000000000, -1.000000000000000000 ) ) ;
#41101=DIRECTION ( 'NONE',  ( -0.000000000000000000, 3.469446951953611428E-15, 1.000000000000000000 ) ) ;
#41103=EDGE_CURVE ( 'NONE', #34116, #42614, #10972, .T. ) ;
#41105=DIRECTION ( 'NONE',  ( 0.000000000000000000, 1.000000000000000000, 0.000000000000000000 ) ) ;
#41107=ORIENTED_EDGE ( 'NONE', *, *, #243, .F. ) ;
#41108=FILL_AREA_STYLE_COLOUR ( '', #37826 ) ;
#41110=EDGE_CURVE ( 'NONE', #17255, #65035, #68278, .T. ) ;
#41124=CARTESIAN_POINT ( 'NONE',  ( 6.000000000000017764, 43.00000000000000000, -35.50000000000000000 ) ) ;
#41135=SURFACE_STYLE_FILL_AREA ( #15436 ) ;
#41141=FACE_OUTER_BOUND ( 'NONE', #13923, .T. ) ;
#41155=DIRECTION ( 'NONE',  ( 1.000000000000000000, 0.000000000000000000, 0.000000000000000000 ) ) ;
#41159=DIRECTION ( 'NONE',  ( 1.000000000000000000, 0.000000000000000000, 0.000000000000000000 ) ) ;
#41179=UNCERTAINTY_MEASURE_WITH_UNIT (LENGTH_MEASURE( 1.000000000000000082E-05 ), #12292, 'distance_accuracy_value', 'NONE');
#41223=ORIENTED_EDGE ( 'NONE', *, *, #52466, .F. ) ;
#41224=ORIENTED_EDGE ( 'NONE', *, *, #15041, .F. ) ;
#41225=VECTOR ( 'NONE', #49496, 1000.000000000000000 ) ;
#41228=CARTESIAN_POINT ( 'NONE',  ( 22.00000000000002132, 50.00000000000000000, 55.00000000000000711 ) ) ;
#41235=DIRECTION ( 'NONE',  ( 0.000000000000000000, 0.000000000000000000, -1.000000000000000000 ) ) ;
#41244=UNCERTAINTY_MEASURE_WITH_UNIT (LENGTH_MEASURE( 1.000000000000000082E-05 ), #12569, 'distance_accuracy_value', 'NONE');
#41246=AXIS2_PLACEMENT_3D ( 'NONE', #22734, #11818, #54717 ) ;
#41258=ORIENTED_EDGE ( 'NONE', *, *, #2974, .T. ) ;
#41277=DIRECTION ( 'NONE',  ( 0.000000000000000000, 0.000000000000000000, -1.000000000000000000 ) ) ;
#41284=UNCERTAINTY_MEASURE_WITH_UNIT (LENGTH_MEASURE( 1.000000000000000082E-05 ), #22159, 'distance_accuracy_value', 'NONE');
#41296=FACE_OUTER_BOUND ( 'NONE', #67719, .T. ) ;
#41304=CARTESIAN_POINT ( 'NONE',  ( 3.000000000000002665, 0.000000000000000000, 3.772833609257260986E-15 ) ) ;
#41313=LINE ( 'NONE', #31755, #59436 ) ;
#41314=AXIS2_PLACEMENT_3D ( 'NONE', #27050, #9891, #48587 ) ;
#41328=CARTESIAN_POINT ( 'NONE',  ( 6.000000000000017764, 26.00000000000000355, 27.49999999999999645 ) ) ;
#41336=DIRECTION ( 'NONE',  ( -0.000000000000000000, -1.000000000000000000, -0.000000000000000000 ) ) ;
#41344=ADVANCED_FACE ( 'NONE', ( #39261 ), #39958, .T. ) ;
#41370=PRESENTATION_STYLE_ASSIGNMENT (( #3665 ) ) ;
#41372=ORIENTED_EDGE ( 'NONE', *, *, #3127, .T. ) ;
#41374=DIRECTION ( 'NONE',  ( 0.000000000000000000, 0.000000000000000000, 1.000000000000000000 ) ) ;
#41380=VERTEX_POINT ( 'NONE', #52619 ) ;
#41381=( NAMED_UNIT ( * ) SI_UNIT ( $, .STERADIAN. ) SOLID_ANGLE_UNIT ( ) );
#41394=CARTESIAN_POINT ( 'NONE',  ( 0.000000000000000000, 14.00000000000000000, -79.00402776293826435 ) ) ;
#41396=DIRECTION ( 'NONE',  ( 0.000000000000000000, 0.000000000000000000, 1.000000000000000000 ) ) ;
#41401=STYLED_ITEM ( 'NONE', ( #49638 ), #9839 ) ;
#41404=ORIENTED_EDGE ( 'NONE', *, *, #59648, .F. ) ;
#41410=CARTESIAN_POINT ( 'NONE',  ( 29.00000000000002842, 42.58578643762690774, 89.58578643762690774 ) ) ;
#41417=DIRECTION ( 'NONE',  ( 0.000000000000000000, 0.9984713486292863260, 0.05527174654752588234 ) ) ;
#41424=DIRECTION ( 'NONE',  ( -0.000000000000000000, -1.000000000000000000, -0.000000000000000000 ) ) ;
#41430=CYLINDRICAL_SURFACE ( 'NONE', #55260, 16.00000000000000000 ) ;
#41439=ORIENTED_EDGE ( 'NONE', *, *, #2402, .T. ) ;
#41441=COLOUR_RGB ( '', 0.72549020, 0.75294118, 0.79215686) ;
#41445=CARTESIAN_POINT ( 'NONE',  ( 0.000000000000000000, 14.00000000000000000, 79.00402776293826435 ) ) ;
#41450=FACE_OUTER_BOUND ( 'NONE', #68572, .T. ) ;
#41456=DIRECTION ( 'NONE',  ( 0.000000000000000000, 1.000000000000000000, 0.000000000000000000 ) ) ;
#41483=DIRECTION ( 'NONE',  ( 1.000000000000000000, -0.000000000000000000, -1.300977106640434891E-16 ) ) ;
#41490=EDGE_CURVE ( 'NONE', #26732, #9552, #43486, .T. ) ;
#41496=( NAMED_UNIT ( * ) PLANE_ANGLE_UNIT ( ) SI_UNIT ( $, .RADIAN. ) );
#41507=CYLINDRICAL_SURFACE ( 'NONE', #62907, 4.999999999999990230 ) ;
#41508=( LENGTH_UNIT ( ) NAMED_UNIT ( * ) SI_UNIT ( .MILLI., .METRE. ) );
#41514=AXIS2_PLACEMENT_3D ( 'NONE', #5703, #21557, #48684 ) ;
#41515=FACE_OUTER_BOUND ( 'NONE', #42536, .T. ) ;
#41519=VERTEX_POINT ( 'NONE', #11056 ) ;
#41522=CARTESIAN_POINT ( 'NONE',  ( 2.000000000000008882, 26.00000000000000355, -24.00000000000000355 ) ) ;
#41524=VERTEX_POINT ( 'NONE', #37514 ) ;
#41526=MECHANICAL_DESIGN_GEOMETRIC_PRESENTATION_REPRESENTATION('',(#63982),#48266);
#41527=CARTESIAN_POINT ( 'NONE',  ( 22.00000000000000000, 43.00000000000000000, -90.00000000000000000 ) ) ;
#41529=VERTEX_POINT ( 'NONE', #48061 ) ;
#41532=( GEOMETRIC_REPRESENTATION_CONTEXT ( 3 ) GLOBAL_UNCERTAINTY_ASSIGNED_CONTEXT ( ( #16419 ) ) GLOBAL_UNIT_ASSIGNED_CONTEXT ( ( #7799, #7470, #1431 ) ) REPRESENTATION_CONTEXT ( 'NONE', 'WORKASPACE' ) );
#41542=EDGE_LOOP ( 'NONE', ( #18206, #48638 ) ) ;
#41569=AXIS2_PLACEMENT_3D ( 'NONE', #16331, #66918, #44798 ) ;
#41570=ORIENTED_EDGE ( 'NONE', *, *, #6662, .F. ) ;
#41573=SURFACE_STYLE_USAGE ( .BOTH. , #35936 ) ;
#41579=( NAMED_UNIT ( * ) SI_UNIT ( $, .STERADIAN. ) SOLID_ANGLE_UNIT ( ) );
#41582=DIRECTION ( 'NONE',  ( 1.000000000000000000, 0.000000000000000000, 0.000000000000000000 ) ) ;
#41583=AXIS2_PLACEMENT_3D ( 'NONE', #1786, #44463, #33498 ) ;
#41585=EDGE_CURVE ( 'NONE', #8511, #68594, #21984, .T. ) ;
#41587=DIRECTION ( 'NONE',  ( -1.000000000000000000, -0.000000000000000000, -0.000000000000000000 ) ) ;
#41589=FILL_AREA_STYLE ('',( #68656 ) ) ;
#41591=MECHANICAL_DESIGN_GEOMETRIC_PRESENTATION_REPRESENTATION('',(#10088),#46068);
#41596=FILL_AREA_STYLE ('',( #5547 ) ) ;
#41607=ORIENTED_EDGE ( 'NONE', *, *, #41680, .F. ) ;
#41612=CARTESIAN_POINT ( 'NONE',  ( 35.99999999999999289, 5.000000000000000000, 24.00402776293825369 ) ) ;
#41613=CARTESIAN_POINT ( 'NONE',  ( 108.3664351561509562, 0.000000000000000000, -18.43563588791579733 ) ) ;
#41615=AXIS2_PLACEMENT_3D ( 'NONE', #38047, #11271, #20806 ) ;
#41616=EDGE_CURVE ( 'NONE', #417, #60539, #22314, .T. ) ;
#41644=LINE ( 'NONE', #58835, #60841 ) ;
#41648=ORIENTED_EDGE ( 'NONE', *, *, #59648, .T. ) ;
#41651=COLOUR_RGB ( '', 0.40784314, 0.44705882, 0.49803922) ;
#41660=STYLED_ITEM ( 'NONE', ( #58961 ), #33429 ) ;
#41662=ORIENTED_EDGE ( 'NONE', *, *, #49659, .T. ) ;
#41663=CARTESIAN_POINT ( 'NONE',  ( 57.00000000000000000, 16.00000000000000000, -60.00402776293825724 ) ) ;
#41678=ORIENTED_EDGE ( 'NONE', *, *, #55579, .T. ) ;
#41680=EDGE_CURVE ( 'NONE', #56481, #39384, #8944, .T. ) ;
#41687=ORIENTED_EDGE ( 'NONE', *, *, #27603, .F. ) ;
#41692=FILL_AREA_STYLE ('',( #46646 ) ) ;
#41697=CIRCLE ( 'NONE', #9084, 1.000000000000001110 ) ;
#41707=FACE_OUTER_BOUND ( 'NONE', #10569, .T. ) ;
#41711=SURFACE_SIDE_STYLE ('',( #4728 ) ) ;
#41726=CARTESIAN_POINT ( 'NONE',  ( 22.00000000000000355, 60.69879356856722552, -69.02971849933236115 ) ) ;
#41731=ADVANCED_FACE ( 'NONE', ( #35654 ), #45876, .T. ) ;
#41738=VECTOR ( 'NONE', #26416, 1000.000000000000000 ) ;
#41752=LINE ( 'NONE', #41394, #3997 ) ;
#41761=CYLINDRICAL_SURFACE ( 'NONE', #21257, 5.000000000000004441 ) ;
#41762=CARTESIAN_POINT ( 'NONE',  ( 10.00000000000002132, 50.00000000000000000, 60.00000000000000000 ) ) ;
#41763=UNCERTAINTY_MEASURE_WITH_UNIT (LENGTH_MEASURE( 1.000000000000000082E-05 ), #18974, 'distance_accuracy_value', 'NONE');
#41771=CARTESIAN_POINT ( 'NONE',  ( 8.000000000000030198, 5.000000000000000000, -32.00402776293825013 ) ) ;
#41773=UNCERTAINTY_MEASURE_WITH_UNIT (LENGTH_MEASURE( 1.000000000000000082E-05 ), #63525, 'distance_accuracy_value', 'NONE');
#41776=CARTESIAN_POINT ( 'NONE',  ( 16.00000000000001776, 42.00000000000000000, -29.68999999999999417 ) ) ;
#41778=VECTOR ( 'NONE', #60891, 1000.000000000000000 ) ;
#41784=ORIENTED_EDGE ( 'NONE', *, *, #39178, .T. ) ;
#41787=SPHERICAL_SURFACE ( 'NONE', #59636, 1.000000000000000000 ) ;
#41789=STYLED_ITEM ( 'NONE', ( #16418 ), #12899 ) ;
#41792=SURFACE_STYLE_FILL_AREA ( #25222 ) ;
#41804=CARTESIAN_POINT ( 'NONE',  ( 179.4361977533490347, 0.000000000000000000, -103.7004518695263044 ) ) ;
#41808=SURFACE_SIDE_STYLE ('',( #14698 ) ) ;
#41814=DIRECTION ( 'NONE',  ( -1.000000000000000000, 0.000000000000000000, 0.000000000000000000 ) ) ;
#41825=( BOUNDED_CURVE ( )  B_SPLINE_CURVE ( 3, ( #32366, #30723, #32723, #21481 ),
 .UNSPECIFIED., .F., .F. ) 
 B_SPLINE_CURVE_WITH_KNOTS ( ( 4, 4 ),
 ( 8.673617379884026597E-16, 1.570796326794896558 ),
 .UNSPECIFIED. ) 
 CURVE ( )  GEOMETRIC_REPRESENTATION_ITEM ( )  RATIONAL_B_SPLINE_CURVE ( ( 1.000000000000000000, 0.8047378541243652705, 0.8047378541243652705, 1.000000000000000000 ) ) 
 REPRESENTATION_ITEM ( '' )  );
#41830=CARTESIAN_POINT ( 'NONE',  ( 2.999999999999998668, 5.000000000000000000, 72.00402776293822171 ) ) ;
#41833=ORIENTED_EDGE ( 'NONE', *, *, #34159, .T. ) ;
#41841=PRESENTATION_STYLE_ASSIGNMENT (( #30178 ) ) ;
#41850=COLOUR_RGB ( '', 0.72549020, 0.75294118, 0.79215686) ;
#41859=UNCERTAINTY_MEASURE_WITH_UNIT (LENGTH_MEASURE( 1.000000000000000082E-05 ), #13610, 'distance_accuracy_value', 'NONE');
#41868=DIRECTION ( 'NONE',  ( -0.000000000000000000, 1.000000000000000000, -0.000000000000000000 ) ) ;
#41870=ORIENTED_EDGE ( 'NONE', *, *, #65995, .T. ) ;
#41871=EDGE_LOOP ( 'NONE', ( #62329, #48855, #36254, #53562 ) ) ;
#41875=SURFACE_STYLE_USAGE ( .BOTH. , #47875 ) ;
#41877=( GEOMETRIC_REPRESENTATION_CONTEXT ( 3 ) GLOBAL_UNCERTAINTY_ASSIGNED_CONTEXT ( ( #21599 ) ) GLOBAL_UNIT_ASSIGNED_CONTEXT ( ( #8570, #49743, #2154 ) ) REPRESENTATION_CONTEXT ( 'NONE', 'WORKASPACE' ) );
#41887=ADVANCED_FACE ( 'NONE', ( #15956 ), #56008, .T. ) ;
#41893=AXIS2_PLACEMENT_3D ( 'NONE', #39723, #35106, #39379 ) ;
#41896=LINE ( 'NONE', #14793, #3512 ) ;
#41902=CARTESIAN_POINT ( 'NONE',  ( 23.50000000000001776, 42.00000000000000000, -28.18999999999999773 ) ) ;
#41903=STYLED_ITEM ( 'NONE', ( #49077 ), #23760 ) ;
#41905=DIRECTION ( 'NONE',  ( -1.000000000000000000, 0.000000000000000000, 0.000000000000000000 ) ) ;
#41910=ORIENTED_EDGE ( 'NONE', *, *, #60560, .F. ) ;
#41918=UNCERTAINTY_MEASURE_WITH_UNIT (LENGTH_MEASURE( 1.000000000000000082E-05 ), #63468, 'distance_accuracy_value', 'NONE');
#41950=( NAMED_UNIT ( * ) PLANE_ANGLE_UNIT ( ) SI_UNIT ( $, .RADIAN. ) );
#41954=ORIENTED_EDGE ( 'NONE', *, *, #43948, .T. ) ;
#41959=VECTOR ( 'NONE', #33372, 1000.000000000000000 ) ;
#41967=( GEOMETRIC_REPRESENTATION_CONTEXT ( 3 ) GLOBAL_UNCERTAINTY_ASSIGNED_CONTEXT ( ( #40581 ) ) GLOBAL_UNIT_ASSIGNED_CONTEXT ( ( #20096, #64060, #26424 ) ) REPRESENTATION_CONTEXT ( 'NONE', 'WORKASPACE' ) );
#41976=LINE ( 'NONE', #36704, #38043 ) ;
#41981=LINE ( 'NONE', #19779, #54452 ) ;
#41986=ORIENTED_EDGE ( 'NONE', *, *, #48672, .F. ) ;
#41994=UNCERTAINTY_MEASURE_WITH_UNIT (LENGTH_MEASURE( 1.000000000000000082E-05 ), #51106, 'distance_accuracy_value', 'NONE');
#41997=EDGE_CURVE ( 'NONE', #2313, #36334, #45906, .T. ) ;
#42004=SURFACE_STYLE_FILL_AREA ( #53550 ) ;
#42019=( GEOMETRIC_REPRESENTATION_CONTEXT ( 3 ) GLOBAL_UNCERTAINTY_ASSIGNED_CONTEXT ( ( #13046 ) ) GLOBAL_UNIT_ASSIGNED_CONTEXT ( ( #60929, #11719, #39880 ) ) REPRESENTATION_CONTEXT ( 'NONE', 'WORKASPACE' ) );
#42020=ORIENTED_EDGE ( 'NONE', *, *, #14930, .T. ) ;
#42024=FACE_OUTER_BOUND ( 'NONE', #38182, .T. ) ;
#42035=VECTOR ( 'NONE', #66036, 1000.000000000000000 ) ;
#42039=( GEOMETRIC_REPRESENTATION_CONTEXT ( 3 ) GLOBAL_UNCERTAINTY_ASSIGNED_CONTEXT ( ( #53884 ) ) GLOBAL_UNIT_ASSIGNED_CONTEXT ( ( #50006, #34492, #61546 ) ) REPRESENTATION_CONTEXT ( 'NONE', 'WORKASPACE' ) );
#42040=EDGE_CURVE ( 'NONE', #42614, #54767, #45954, .T. ) ;
#42044=ORIENTED_EDGE ( 'NONE', *, *, #36629, .F. ) ;
#42048=( NAMED_UNIT ( * ) PLANE_ANGLE_UNIT ( ) SI_UNIT ( $, .RADIAN. ) );
#42061=( NAMED_UNIT ( * ) PLANE_ANGLE_UNIT ( ) SI_UNIT ( $, .RADIAN. ) );
#42064=EDGE_CURVE ( 'NONE', #42205, #67224, #2456, .T. ) ;
#42071=VECTOR ( 'NONE', #4748, 1000.000000000000000 ) ;
#42080=UNCERTAINTY_MEASURE_WITH_UNIT (LENGTH_MEASURE( 1.000000000000000082E-05 ), #15470, 'distance_accuracy_value', 'NONE');
#42088=EDGE_CURVE ( 'NONE', #23178, #14824, #63845, .T. ) ;
#42101=CARTESIAN_POINT ( 'NONE',  ( 8.000000000000030198, 0.000000000000000000, 29.00402776293826079 ) ) ;
#42139=MECHANICAL_DESIGN_GEOMETRIC_PRESENTATION_REPRESENTATION('',(#20753),#15158);
#42140=( NAMED_UNIT ( * ) SI_UNIT ( $, .STERADIAN. ) SOLID_ANGLE_UNIT ( ) );
#42151=AXIS2_PLACEMENT_3D ( 'NONE', #6444, #32150, #48722 ) ;
#42154=DIRECTION ( 'NONE',  ( 0.000000000000000000, 1.000000000000000000, 0.000000000000000000 ) ) ;
#42159=CARTESIAN_POINT ( 'NONE',  ( 23.32272074508237480, 24.55989583710051960, -27.18999999999994088 ) ) ;
#42163=VERTEX_POINT ( 'NONE', #15094 ) ;
#42173=EDGE_CURVE ( 'NONE', #17554, #52516, #26772, .T. ) ;
#42176=DIRECTION ( 'NONE',  ( 0.000000000000000000, -0.000000000000000000, 1.000000000000000000 ) ) ;
#42177=SURFACE_STYLE_FILL_AREA ( #19612 ) ;
#42180=EDGE_CURVE ( 'NONE', #30684, #31434, #13329, .T. ) ;
#42185=CARTESIAN_POINT ( 'NONE',  ( 27.99999999999999645, 5.000000000000000000, -72.00402776293822171 ) ) ;
#42190=DIRECTION ( 'NONE',  ( 0.9418169057949938860, 0.000000000000000000, 0.3361263392814427542 ) ) ;
#42192=CARTESIAN_POINT ( 'NONE',  ( 22.99999999999996092, 0.000000000000000000, -77.00402776293825013 ) ) ;
#42205=VERTEX_POINT ( 'NONE', #52703 ) ;
#42211=VECTOR ( 'NONE', #39702, 1000.000000000000000 ) ;
#42215=( NAMED_UNIT ( * ) SI_UNIT ( $, .STERADIAN. ) SOLID_ANGLE_UNIT ( ) );
#42226=CIRCLE ( 'NONE', #12981, 4.999999999999997335 ) ;
#42228=CARTESIAN_POINT ( 'NONE',  ( 2.999999999999993339, 0.000000000000000000, 24.00402776293822882 ) ) ;
#42238=PRESENTATION_STYLE_ASSIGNMENT (( #20003 ) ) ;
#42247=FACE_OUTER_BOUND ( 'NONE', #34720, .T. ) ;
#42248=DIRECTION ( 'NONE',  ( -0.000000000000000000, -1.000000000000000000, -0.000000000000000000 ) ) ;
#42249=FILL_AREA_STYLE_COLOUR ( '', #68927 ) ;
#42253=ORIENTED_EDGE ( 'NONE', *, *, #36855, .T. ) ;
#42255=DIRECTION ( 'NONE',  ( 0.000000000000000000, 0.000000000000000000, -1.000000000000000000 ) ) ;
#42257=ORIENTED_EDGE ( 'NONE', *, *, #43948, .F. ) ;
#42262=FILL_AREA_STYLE_COLOUR ( '', #14975 ) ;
#42268=ORIENTED_EDGE ( 'NONE', *, *, #2571, .F. ) ;
#42282=DIRECTION ( 'NONE',  ( 2.168404344971007882E-16, 0.000000000000000000, 1.000000000000000000 ) ) ;
#42290=ORIENTED_EDGE ( 'NONE', *, *, #34024, .T. ) ;
#42292=CARTESIAN_POINT ( 'NONE',  ( 22.31832753082305132, 26.35367636051609708, 27.48619697041611687 ) ) ;
#42293=( LENGTH_UNIT ( ) NAMED_UNIT ( * ) SI_UNIT ( .MILLI., .METRE. ) );
#42297=( NAMED_UNIT ( * ) SI_UNIT ( $, .STERADIAN. ) SOLID_ANGLE_UNIT ( ) );
#42298=FILL_AREA_STYLE ('',( #20792 ) ) ;
#42300=ORIENTED_EDGE ( 'NONE', *, *, #42088, .T. ) ;
#42311=MECHANICAL_DESIGN_GEOMETRIC_PRESENTATION_REPRESENTATION('',(#6281),#45653);
#42314=CARTESIAN_POINT ( 'NONE',  ( 179.4361977533518484, 0.000000000000000000, 103.7004518695275550 ) ) ;
#42329=LINE ( 'NONE', #15562, #67373 ) ;
#42339=CARTESIAN_POINT ( 'NONE',  ( 32.00000000000000000, 42.00000000000000000, -79.00402776293826435 ) ) ;
#42344=DIRECTION ( 'NONE',  ( 0.000000000000000000, -0.9396926207859082059, 0.3420201433256693790 ) ) ;
#42355=CARTESIAN_POINT ( 'NONE',  ( 27.00000000000001776, 15.00000000000000000, -29.68999999999999417 ) ) ;
#42359=ORIENTED_EDGE ( 'NONE', *, *, #15232, .F. ) ;
#42364=ORIENTED_EDGE ( 'NONE', *, *, #61667, .T. ) ;
#42371=PRESENTATION_STYLE_ASSIGNMENT (( #69398 ) ) ;
#42378=( LENGTH_UNIT ( ) NAMED_UNIT ( * ) SI_UNIT ( .MILLI., .METRE. ) );
#42380=( NAMED_UNIT ( * ) PLANE_ANGLE_UNIT ( ) SI_UNIT ( $, .RADIAN. ) );
#42387=EDGE_CURVE ( 'NONE', #49909, #56560, #45291, .T. ) ;
#42389=EDGE_CURVE ( 'NONE', #23750, #60430, #29022, .T. ) ;
#42395=DIRECTION ( 'NONE',  ( -1.000000000000000000, -9.122956858292678705E-34, 1.300977106640434891E-16 ) ) ;
#42396=EDGE_CURVE ( 'NONE', #16364, #45002, #52595, .T. ) ;
#42405=PRESENTATION_STYLE_ASSIGNMENT (( #69097 ) ) ;
#42407=DIRECTION ( 'NONE',  ( 0.000000000000000000, -1.000000000000000000, 0.000000000000000000 ) ) ;
#42413=( NAMED_UNIT ( * ) PLANE_ANGLE_UNIT ( ) SI_UNIT ( $, .RADIAN. ) );
#42431=( NAMED_UNIT ( * ) SI_UNIT ( $, .STERADIAN. ) SOLID_ANGLE_UNIT ( ) );
#42435=SURFACE_SIDE_STYLE ('',( #48060 ) ) ;
#42440=ORIENTED_EDGE ( 'NONE', *, *, #64224, .F. ) ;
#42461=CARTESIAN_POINT ( 'NONE',  ( 36.00000000000002842, 0.000000000000000000, 29.00402776293825724 ) ) ;
#42474=CARTESIAN_POINT ( 'NONE',  ( 4.000000000000002665, 37.76051491742381216, -89.34202014332566932 ) ) ;
#42483=VECTOR ( 'NONE', #61771, 1000.000000000000000 ) ;
#42509=FACE_OUTER_BOUND ( 'NONE', #40508, .T. ) ;
#42534=CIRCLE ( 'NONE', #22297, 18.99999999999998934 ) ;
#42536=EDGE_LOOP ( 'NONE', ( #49903, #23851, #22620, #32468 ) ) ;
#42537=FACE_OUTER_BOUND ( 'NONE', #18397, .T. ) ;
#42538=EDGE_CURVE ( 'NONE', #54457, #65703, #40367, .T. ) ;
#42539=CARTESIAN_POINT ( 'NONE',  ( 6.000000000000017764, 43.00000000000000000, 35.50000000000000000 ) ) ;
#42547=DIRECTION ( 'NONE',  ( 0.000000000000000000, 0.000000000000000000, 1.000000000000000000 ) ) ;
#42548=EDGE_CURVE ( 'NONE', #13184, #65559, #68444, .T. ) ;
#42552=( NAMED_UNIT ( * ) PLANE_ANGLE_UNIT ( ) SI_UNIT ( $, .RADIAN. ) );
#42553=ORIENTED_EDGE ( 'NONE', *, *, #12851, .F. ) ;
#42568=SURFACE_SIDE_STYLE ('',( #31617 ) ) ;
#42574=ORIENTED_EDGE ( 'NONE', *, *, #68808, .T. ) ;
#42577=ORIENTED_EDGE ( 'NONE', *, *, #40277, .F. ) ;
#42586=CARTESIAN_POINT ( 'NONE',  ( 0.000000000000000000, 42.00000000000000000, 79.00402776293826435 ) ) ;
#42605=FACE_OUTER_BOUND ( 'NONE', #21716, .T. ) ;
#42611=FILL_AREA_STYLE_COLOUR ( '', #6419 ) ;
#42614=VERTEX_POINT ( 'NONE', #30427 ) ;
#42616=SURFACE_STYLE_FILL_AREA ( #21116 ) ;
#42618=CARTESIAN_POINT ( 'NONE',  ( 57.00000000000000000, 14.00000000000000000, -60.00402776293827145 ) ) ;
#42628=DIRECTION ( 'NONE',  ( 0.000000000000000000, 1.000000000000000000, 0.000000000000000000 ) ) ;
#42642=CARTESIAN_POINT ( 'NONE',  ( 1.000000000000000000, 14.00000000000000533, 35.50000000000000000 ) ) ;
#42644=ADVANCED_FACE ( 'NONE', ( #33236 ), #6475, .F. ) ;
#42650=DIRECTION ( 'NONE',  ( -0.000000000000000000, -1.000000000000000000, -0.000000000000000000 ) ) ;
#42654=FACE_OUTER_BOUND ( 'NONE', #21777, .T. ) ;
#42656=AXIS2_PLACEMENT_3D ( 'NONE', #13071, #7111, #17354 ) ;
#42660=CARTESIAN_POINT ( 'NONE',  ( 29.00000000000000000, 42.00000000000000000, -89.00000000000000000 ) ) ;
#42664=SURFACE_SIDE_STYLE ('',( #14496 ) ) ;
#42670=VECTOR ( 'NONE', #59945, 1000.000000000000000 ) ;
#42679=VERTEX_POINT ( 'NONE', #42804 ) ;
#42701=LINE ( 'NONE', #3584, #36690 ) ;
#42704=CARTESIAN_POINT ( 'NONE',  ( 10.00000000000000533, 50.00000000000000000, -46.00000000000000000 ) ) ;
#42705=EDGE_CURVE ( 'NONE', #69112, #38068, #27961, .T. ) ;
#42707=ORIENTED_EDGE ( 'NONE', *, *, #31448, .T. ) ;
#42708=CARTESIAN_POINT ( 'NONE',  ( 35.99999999999999289, 5.000000000000000000, -72.00402776293825013 ) ) ;
#42715=VECTOR ( 'NONE', #14466, 1000.000000000000000 ) ;
#42722=EDGE_CURVE ( 'NONE', #24855, #61901, #46001, .T. ) ;
#42746=SURFACE_SIDE_STYLE ('',( #47692 ) ) ;
#42752=DIRECTION ( 'NONE',  ( 0.000000000000000000, 0.000000000000000000, -1.000000000000000000 ) ) ;
#42756=VECTOR ( 'NONE', #62620, 1000.000000000000000 ) ;
#42770=FACE_OUTER_BOUND ( 'NONE', #24179, .T. ) ;
#42780=SURFACE_SIDE_STYLE ('',( #5087 ) ) ;
#42785=AXIS2_PLACEMENT_3D ( 'NONE', #19847, #30375, #46644 ) ;
#42794=CARTESIAN_POINT ( 'NONE',  ( 35.99999999999999289, 5.000000000000000000, 24.00402776293825369 ) ) ;
#42795=CARTESIAN_POINT ( 'NONE',  ( 27.00000000000001776, -60.04052944165106709, 35.50000000000000000 ) ) ;
#42803=EDGE_CURVE ( 'NONE', #54767, #34141, #53802, .T. ) ;
#42804=CARTESIAN_POINT ( 'NONE',  ( 7.000000000000017764, 42.74314482547740113, 27.71473342867655987 ) ) ;
#42806=AXIS2_PLACEMENT_3D ( 'NONE', #9388, #31152, #35059 ) ;
#42811=PRESENTATION_STYLE_ASSIGNMENT (( #32199 ) ) ;
#42825=DIRECTION ( 'NONE',  ( 0.000000000000000000, 0.6691306063588591257, -0.7431448254773933559 ) ) ;
#42830=VECTOR ( 'NONE', #6778, 1000.000000000000000 ) ;
#42831=DIRECTION ( 'NONE',  ( 1.000000000000000000, 0.000000000000000000, -1.300977106640434891E-16 ) ) ;
#42833=LINE ( 'NONE', #63875, #50841 ) ;
#42834=ORIENTED_EDGE ( 'NONE', *, *, #12392, .F. ) ;
#42837=EDGE_LOOP ( 'NONE', ( #24510, #23692, #8495, #4477, #62919, #43562, #53961, #5460, #5149, #63027, #28607, #50123, #26661 ) ) ;
#42839=( LENGTH_UNIT ( ) NAMED_UNIT ( * ) SI_UNIT ( .MILLI., .METRE. ) );
#42840=AXIS2_PLACEMENT_3D ( 'NONE', #59977, #7217, #49786 ) ;
#42846=SURFACE_STYLE_USAGE ( .BOTH. , #47796 ) ;
#42847=VERTEX_POINT ( 'NONE', #18093 ) ;
#42853=CYLINDRICAL_SURFACE ( 'NONE', #21572, 5.000000000000004441 ) ;
#42866=FILL_AREA_STYLE_COLOUR ( '', #773 ) ;
#42876=AXIS2_PLACEMENT_3D ( 'NONE', #11099, #15390, #5818 ) ;
#42885=CARTESIAN_POINT ( 'NONE',  ( 93.00000000000000000, 14.00000000000000000, 0.000000000000000000 ) ) ;
#42897=FACE_OUTER_BOUND ( 'NONE', #60444, .T. ) ;
#42898=DIRECTION ( 'NONE',  ( 0.000000000000000000, 0.000000000000000000, 1.000000000000000000 ) ) ;
#42906=FILL_AREA_STYLE_COLOUR ( '', #34236 ) ;
#42908=( GEOMETRIC_REPRESENTATION_CONTEXT ( 3 ) GLOBAL_UNCERTAINTY_ASSIGNED_CONTEXT ( ( #10849 ) ) GLOBAL_UNIT_ASSIGNED_CONTEXT ( ( #35251, #13431, #39513 ) ) REPRESENTATION_CONTEXT ( 'NONE', 'WORKASPACE' ) );
#42914=SURFACE_STYLE_USAGE ( .BOTH. , #25718 ) ;
#42915=FILL_AREA_STYLE_COLOUR ( '', #41651 ) ;
#42919=ORIENTED_EDGE ( 'NONE', *, *, #66827, .F. ) ;
#42921=CIRCLE ( 'NONE', #24873, 5.000000000000004441 ) ;
#42936=DIRECTION ( 'NONE',  ( -1.239088197126290817E-16, 0.000000000000000000, -1.000000000000000000 ) ) ;
#42943=FILL_AREA_STYLE_COLOUR ( '', #47437 ) ;
#42944=DIRECTION ( 'NONE',  ( 1.000000000000000000, -0.000000000000000000, -1.300977106640434891E-16 ) ) ;
#42953=ADVANCED_FACE ( 'NONE', ( #68365 ), #40610, .T. ) ;
#42954=EDGE_LOOP ( 'NONE', ( #60801, #17270, #28129, #53312 ) ) ;
#42955=CYLINDRICAL_SURFACE ( 'NONE', #62957, 1.000000000000000888 ) ;
#42967=VERTEX_POINT ( 'NONE', #24730 ) ;
#42968=CIRCLE ( 'NONE', #20422, 111.0000000000000142 ) ;
#42970=CARTESIAN_POINT ( 'NONE',  ( 23.50000000000001776, 24.55989583710066171, 27.18999999999999062 ) ) ;
#42975=SURFACE_STYLE_USAGE ( .BOTH. , #59096 ) ;
#42985=FILL_AREA_STYLE_COLOUR ( '', #40451 ) ;
#43000=COLOUR_RGB ( '', 0.40784314, 0.44705882, 0.49803922) ;
#43004=AXIS2_PLACEMENT_3D ( 'NONE', #59356, #11195, #48530 ) ;
#43007=CIRCLE ( 'NONE', #65452, 3.499999999999999556 ) ;
#43012=FACE_OUTER_BOUND ( 'NONE', #40483, .T. ) ;
#43013=( GEOMETRIC_REPRESENTATION_CONTEXT ( 3 ) GLOBAL_UNCERTAINTY_ASSIGNED_CONTEXT ( ( #28591 ) ) GLOBAL_UNIT_ASSIGNED_CONTEXT ( ( #22298, #38174, #49391 ) ) REPRESENTATION_CONTEXT ( 'NONE', 'WORKASPACE' ) );
#43018=EDGE_CURVE ( 'NONE', #44052, #41519, #32805, .T. ) ;
#43020=ORIENTED_EDGE ( 'NONE', *, *, #50669, .T. ) ;
#43023=AXIS2_PLACEMENT_3D ( 'NONE', #46122, #29909, #62943 ) ;
#43038=FACE_OUTER_BOUND ( 'NONE', #6275, .T. ) ;
#43039=EDGE_CURVE ( 'NONE', #21950, #51841, #21914, .T. ) ;
#43045=LINE ( 'NONE', #65835, #60309 ) ;
#43056=FILL_AREA_STYLE ('',( #4288 ) ) ;
#43057=SURFACE_SIDE_STYLE ('',( #58153 ) ) ;
#43060=CARTESIAN_POINT ( 'NONE',  ( 22.99999999999995026, 0.000000000000000000, -32.00402776293824303 ) ) ;
#43068=AXIS2_PLACEMENT_3D ( 'NONE', #47450, #10124, #57967 ) ;
#43078=CIRCLE ( 'NONE', #18326, 1.000000000000000888 ) ;
#43087=CARTESIAN_POINT ( 'NONE',  ( 10.00000000000002132, 50.00000000000000000, 65.00000000000000000 ) ) ;
#43103=DIRECTION ( 'NONE',  ( 0.000000000000000000, 0.000000000000000000, 1.000000000000000000 ) ) ;
#43108=AXIS2_PLACEMENT_3D ( 'NONE', #31736, #4659, #31044 ) ;
#43118=FILL_AREA_STYLE ('',( #5749 ) ) ;
#43119=ORIENTED_EDGE ( 'NONE', *, *, #28062, .F. ) ;
#43124=AXIS2_PLACEMENT_3D ( 'NONE', #66424, #1307, #60782 ) ;
#43126=CARTESIAN_POINT ( 'NONE',  ( 3.000000000000002665, 38.00000000000000711, -90.00000000000000000 ) ) ;
#43131=CIRCLE ( 'NONE', #47611, 0.9999999999999995559 ) ;
#43133=DIRECTION ( 'NONE',  ( 1.300977106640434891E-16, 0.000000000000000000, 1.000000000000000000 ) ) ;
#43143=EDGE_CURVE ( 'NONE', #38534, #22897, #33616, .T. ) ;
#43149=EDGE_LOOP ( 'NONE', ( #67635, #21535, #58299, #4756 ) ) ;
#43151=DIRECTION ( 'NONE',  ( 1.300977106640434891E-16, 0.000000000000000000, 1.000000000000000000 ) ) ;
#43166=CIRCLE ( 'NONE', #47645, 1.499999999999997780 ) ;
#43182=CARTESIAN_POINT ( 'NONE',  ( 27.00000000000001776, 15.00000000000000000, -29.68999999999999417 ) ) ;
#43186=ADVANCED_FACE ( 'NONE', ( #12033 ), #28542, .F. ) ;
#43197=CARTESIAN_POINT ( 'NONE',  ( 4.000000000000030198, 38.70020753820971748, 89.00000000000000000 ) ) ;
#43199=ORIENTED_EDGE ( 'NONE', *, *, #1587, .T. ) ;
#43215=SURFACE_STYLE_USAGE ( .BOTH. , #26937 ) ;
#43220=ORIENTED_EDGE ( 'NONE', *, *, #16406, .T. ) ;
#43221=CARTESIAN_POINT ( 'NONE',  ( 28.00000000000002842, 43.00000000000000000, 79.00402776293826435 ) ) ;
#43226=DIRECTION ( 'NONE',  ( -0.000000000000000000, -1.000000000000000000, -0.000000000000000000 ) ) ;
#43246=( NAMED_UNIT ( * ) SI_UNIT ( $, .STERADIAN. ) SOLID_ANGLE_UNIT ( ) );
#43249=CARTESIAN_POINT ( 'NONE',  ( 1.000000000000000000, 43.00000000000000000, -35.50000000000000000 ) ) ;
#43263=ADVANCED_FACE ( 'NONE', ( #34875 ), #19387, .F. ) ;
#43271=CARTESIAN_POINT ( 'NONE',  ( 36.00000000000002842, 0.000000000000000000, -32.00402776293825724 ) ) ;
#43274=EDGE_LOOP ( 'NONE', ( #17632, #22132, #60856, #7009, #2440 ) ) ;
#43283=DIRECTION ( 'NONE',  ( -1.000000000000000000, 0.000000000000000000, 0.000000000000000000 ) ) ;
#43285=SURFACE_STYLE_USAGE ( .BOTH. , #38681 ) ;
#43288=ORIENTED_EDGE ( 'NONE', *, *, #40370, .F. ) ;
#43309=B_SPLINE_CURVE_WITH_KNOTS ( 'NONE', 3,
 ( #19216, #3717, #29796, #50907, #30459, #13961, #14665, #35433 ),
 .UNSPECIFIED., .F., .F.,
 ( 4, 2, 2, 4 ),
 ( -6.733023926838822157E-06, 0.0008427316310560363033, 0.001267463958547469620, 0.001692196286038903045 ),
 .UNSPECIFIED. ) ;
#43315=ORIENTED_EDGE ( 'NONE', *, *, #40690, .F. ) ;
#43333=FILL_AREA_STYLE_COLOUR ( '', #38309 ) ;
#43341=MECHANICAL_DESIGN_GEOMETRIC_PRESENTATION_REPRESENTATION('',(#3936),#39950);
#43351=CARTESIAN_POINT ( 'NONE',  ( 25.00000000000001421, 42.00000000000000000, 34.49999999999999289 ) ) ;
#43379=ORIENTED_EDGE ( 'NONE', *, *, #19129, .F. ) ;
#43385=CARTESIAN_POINT ( 'NONE',  ( 0.000000000000000000, 42.00000000000000000, -75.00000000000001421 ) ) ;
#43387=( BOUNDED_CURVE ( )  B_SPLINE_CURVE ( 3, ( #18547, #28013, #66366, #24152 ),
 .UNSPECIFIED., .F., .F. ) 
 B_SPLINE_CURVE_WITH_KNOTS ( ( 4, 4 ),
 ( 0.000000000000000000, 1.570796326794896558 ),
 .UNSPECIFIED. ) 
 CURVE ( )  GEOMETRIC_REPRESENTATION_ITEM ( )  RATIONAL_B_SPLINE_CURVE ( ( 1.000000000000000000, 0.8047378541243649375, 0.8047378541243649375, 1.000000000000000000 ) ) 
 REPRESENTATION_ITEM ( '' )  );
#43397=UNCERTAINTY_MEASURE_WITH_UNIT (LENGTH_MEASURE( 1.000000000000000082E-05 ), #7052, 'distance_accuracy_value', 'NONE');
#43404=EDGE_LOOP ( 'NONE', ( #58868, #21721, #22720, #40568 ) ) ;
#43406=UNCERTAINTY_MEASURE_WITH_UNIT (LENGTH_MEASURE( 1.000000000000000082E-05 ), #55608, 'distance_accuracy_value', 'NONE');
#43427=SPHERICAL_SURFACE ( 'NONE', #31319, 1.000000000000000000 ) ;
#43438=CYLINDRICAL_SURFACE ( 'NONE', #32529, 1.000000000000000000 ) ;
#43442=EDGE_CURVE ( 'NONE', #25944, #53365, #68378, .T. ) ;
#43450=DIRECTION ( 'NONE',  ( 0.000000000000000000, 1.000000000000000000, -0.000000000000000000 ) ) ;
#43468=UNCERTAINTY_MEASURE_WITH_UNIT (LENGTH_MEASURE( 1.000000000000000082E-05 ), #10217, 'distance_accuracy_value', 'NONE');
#43476=CARTESIAN_POINT ( 'NONE',  ( 24.08647788275853685, 27.27834388199489268, -27.25847631938719218 ) ) ;
#43482=DIRECTION ( 'NONE',  ( -0.000000000000000000, -1.000000000000000000, -0.000000000000000000 ) ) ;
#43484=ORIENTED_EDGE ( 'NONE', *, *, #7684, .T. ) ;
#43486=LINE ( 'NONE', #59588, #31176 ) ;
#43489=( NAMED_UNIT ( * ) SI_UNIT ( $, .STERADIAN. ) SOLID_ANGLE_UNIT ( ) );
#43504=ADVANCED_FACE ( 'NONE', ( #49257 ), #59798, .T. ) ;
#43506=CARTESIAN_POINT ( 'NONE',  ( 3.414213562373098032, 34.36176364315826248, -80.00402776293826435 ) ) ;
#43513=CARTESIAN_POINT ( 'NONE',  ( 2.999999999999994671, 5.000000000000000000, -24.00402776293822527 ) ) ;
#43527=SURFACE_STYLE_FILL_AREA ( #49455 ) ;
#43532=ORIENTED_EDGE ( 'NONE', *, *, #5187, .T. ) ;
#43533=( NAMED_UNIT ( * ) SI_UNIT ( $, .STERADIAN. ) SOLID_ANGLE_UNIT ( ) );
#43544=CARTESIAN_POINT ( 'NONE',  ( 27.00000000000001776, 14.00000000000000000, -29.68999999999999417 ) ) ;
#43557=VECTOR ( 'NONE', #31280, 1000.000000000000000 ) ;
#43558=CARTESIAN_POINT ( 'NONE',  ( 36.00000000000002842, 5.000000000000000000, -32.00402776293825724 ) ) ;
#43559=ORIENTED_EDGE ( 'NONE', *, *, #19549, .T. ) ;
#43562=ORIENTED_EDGE ( 'NONE', *, *, #63159, .T. ) ;
#43567=DIRECTION ( 'NONE',  ( -0.000000000000000000, 1.000000000000000000, -0.000000000000000000 ) ) ;
#43586=CARTESIAN_POINT ( 'NONE',  ( 24.70573118280081815, 26.17819722711635677, 27.49997435685320113 ) ) ;
#43589=( GEOMETRIC_REPRESENTATION_CONTEXT ( 3 ) GLOBAL_UNCERTAINTY_ASSIGNED_CONTEXT ( ( #22791 ) ) GLOBAL_UNIT_ASSIGNED_CONTEXT ( ( #6639, #39064, #43653 ) ) REPRESENTATION_CONTEXT ( 'NONE', 'WORKASPACE' ) );
#43593=COLOUR_RGB ( '', 0.09019608, 0.27058824, 0.51372549) ;
#43600=STYLED_ITEM ( 'NONE', ( #2915 ), #67510 ) ;
#43603=( NAMED_UNIT ( * ) SI_UNIT ( $, .STERADIAN. ) SOLID_ANGLE_UNIT ( ) );
#43608=( NAMED_UNIT ( * ) PLANE_ANGLE_UNIT ( ) SI_UNIT ( $, .RADIAN. ) );
#43620=( LENGTH_UNIT ( ) NAMED_UNIT ( * ) SI_UNIT ( .MILLI., .METRE. ) );
#43623=CARTESIAN_POINT ( 'NONE',  ( 30.99999999999999289, 0.000000000000000000, -37.00402776293829277 ) ) ;
#43625=CARTESIAN_POINT ( 'NONE',  ( 57.00000000000000000, 14.00000000000000000, -60.00402776293825724 ) ) ;
#43639=FACE_OUTER_BOUND ( 'NONE', #7011, .T. ) ;
#43644=( NAMED_UNIT ( * ) SI_UNIT ( $, .STERADIAN. ) SOLID_ANGLE_UNIT ( ) );
#43647=ORIENTED_EDGE ( 'NONE', *, *, #3368, .F. ) ;
#43650=ORIENTED_EDGE ( 'NONE', *, *, #58093, .F. ) ;
#43653=( NAMED_UNIT ( * ) SI_UNIT ( $, .STERADIAN. ) SOLID_ANGLE_UNIT ( ) );
#43656=DIRECTION ( 'NONE',  ( -0.000000000000000000, -1.000000000000000000, -0.000000000000000000 ) ) ;
#43658=( NAMED_UNIT ( * ) PLANE_ANGLE_UNIT ( ) SI_UNIT ( $, .RADIAN. ) );
#43659=CARTESIAN_POINT ( 'NONE',  ( 27.99999999999998934, 5.000000000000000000, 37.00402776293829277 ) ) ;
#43661=ADVANCED_FACE ( 'NONE', ( #42897, #63937 ), #15449, .T. ) ;
#43673=LINE ( 'NONE', #32721, #5009 ) ;
#43702=SPHERICAL_SURFACE ( 'NONE', #34626, 1.000000000000000000 ) ;
#43704=VERTEX_POINT ( 'NONE', #42539 ) ;
#43707=FACE_OUTER_BOUND ( 'NONE', #65716, .T. ) ;
#43709=SURFACE_STYLE_USAGE ( .BOTH. , #33124 ) ;
#43717=VECTOR ( 'NONE', #2637, 1000.000000000000000 ) ;
#43722=EDGE_LOOP ( 'NONE', ( #1794, #24138, #25742, #49199 ) ) ;
#43726=DIRECTION ( 'NONE',  ( 0.000000000000000000, 0.000000000000000000, -1.000000000000000000 ) ) ;
#43734=DIRECTION ( 'NONE',  ( 0.000000000000000000, 1.000000000000000000, -0.000000000000000000 ) ) ;
#43737=DIRECTION ( 'NONE',  ( -0.000000000000000000, -1.000000000000000000, -0.000000000000000000 ) ) ;
#43766=FILL_AREA_STYLE_COLOUR ( '', #27138 ) ;
#43773=DIRECTION ( 'NONE',  ( 0.000000000000000000, 0.000000000000000000, 1.000000000000000000 ) ) ;
#43774=DIRECTION ( 'NONE',  ( -1.000000000000000000, -0.000000000000000000, 1.300977106640434891E-16 ) ) ;
#43784=CARTESIAN_POINT ( 'NONE',  ( 16.00000000000001776, 15.00000000000000000, -33.68999999999999773 ) ) ;
#43785=( GEOMETRIC_REPRESENTATION_CONTEXT ( 3 ) GLOBAL_UNCERTAINTY_ASSIGNED_CONTEXT ( ( #10902 ) ) GLOBAL_UNIT_ASSIGNED_CONTEXT ( ( #66272, #49428, #3246 ) ) REPRESENTATION_CONTEXT ( 'NONE', 'WORKASPACE' ) );
#43796=TOROIDAL_SURFACE ( 'NONE', #57259, 4.000000000000000000, 1.000000000000000000 ) ;
#43804=( NAMED_UNIT ( * ) SI_UNIT ( $, .STERADIAN. ) SOLID_ANGLE_UNIT ( ) );
#43805=FACE_OUTER_BOUND ( 'NONE', #16646, .T. ) ;
#43806=ORIENTED_EDGE ( 'NONE', *, *, #4335, .T. ) ;
#43818=STYLED_ITEM ( 'NONE', ( #23015 ), #10844 ) ;
#43832=DIRECTION ( 'NONE',  ( -1.000000000000000000, -0.000000000000000000, 1.300977106640434891E-16 ) ) ;
#43833=( NAMED_UNIT ( * ) SI_UNIT ( $, .STERADIAN. ) SOLID_ANGLE_UNIT ( ) );
#43841=UNCERTAINTY_MEASURE_WITH_UNIT (LENGTH_MEASURE( 1.000000000000000082E-05 ), #32162, 'distance_accuracy_value', 'NONE');
#43849=( GEOMETRIC_REPRESENTATION_CONTEXT ( 3 ) GLOBAL_UNCERTAINTY_ASSIGNED_CONTEXT ( ( #6049 ) ) GLOBAL_UNIT_ASSIGNED_CONTEXT ( ( #38544, #59586, #771 ) ) REPRESENTATION_CONTEXT ( 'NONE', 'WORKASPACE' ) );
#43861=DIRECTION ( 'NONE',  ( -0.000000000000000000, 0.6691306063588591257, -0.7431448254773933559 ) ) ;
#43863=MECHANICAL_DESIGN_GEOMETRIC_PRESENTATION_REPRESENTATION('',(#34826),#12373);
#43866=AXIS2_PLACEMENT_3D ( 'NONE', #68234, #3456, #36250 ) ;
#43871=CIRCLE ( 'NONE', #21318, 1.000000000000000888 ) ;
#43873=AXIS2_PLACEMENT_3D ( 'NONE', #3355, #8691, #14667 ) ;
#43877=EDGE_CURVE ( 'NONE', #37203, #42205, #59406, .T. ) ;
#43878=FILL_AREA_STYLE_COLOUR ( '', #65296 ) ;
#43887=STYLED_ITEM ( 'NONE', ( #571 ), #16682 ) ;
#43893=DIRECTION ( 'NONE',  ( -0.000000000000000000, -1.000000000000000000, 0.000000000000000000 ) ) ;
#43898=SURFACE_STYLE_FILL_AREA ( #17495 ) ;
#43921=EDGE_LOOP ( 'NONE', ( #16250, #48665, #2769, #42359 ) ) ;
#43926=CARTESIAN_POINT ( 'NONE',  ( 24.50471495965034308, 26.85083734004840750, 27.39802421297251200 ) ) ;
#43927=AXIS2_PLACEMENT_3D ( 'NONE', #69433, #42407, #36774 ) ;
#43931=STYLED_ITEM ( 'NONE', ( #15870 ), #17692 ) ;
#43943=ORIENTED_EDGE ( 'NONE', *, *, #32023, .F. ) ;
#43944=ORIENTED_EDGE ( 'NONE', *, *, #16019, .F. ) ;
#43946=FILL_AREA_STYLE_COLOUR ( '', #61123 ) ;
#43947=AXIS2_PLACEMENT_3D ( 'NONE', #41612, #10281, #63029 ) ;
#43948=EDGE_CURVE ( 'NONE', #1567, #39120, #18988, .T. ) ;
#43949=( GEOMETRIC_REPRESENTATION_CONTEXT ( 3 ) GLOBAL_UNCERTAINTY_ASSIGNED_CONTEXT ( ( #45471 ) ) GLOBAL_UNIT_ASSIGNED_CONTEXT ( ( #34102, #32710, #54166 ) ) REPRESENTATION_CONTEXT ( 'NONE', 'WORKASPACE' ) );
#43955=AXIS2_PLACEMENT_3D ( 'NONE', #67506, #57655, #30906 ) ;
#43961=( LENGTH_UNIT ( ) NAMED_UNIT ( * ) SI_UNIT ( .MILLI., .METRE. ) );
#43976=DIRECTION ( 'NONE',  ( -0.000000000000000000, -0.000000000000000000, 1.000000000000000000 ) ) ;
#43991=ORIENTED_EDGE ( 'NONE', *, *, #19312, .T. ) ;
#43994=CARTESIAN_POINT ( 'NONE',  ( 10.00000000000001776, 17.78868675966041835, -5.824939844684579265E-16 ) ) ;
#43995=DIRECTION ( 'NONE',  ( 0.000000000000000000, 0.000000000000000000, 1.000000000000000000 ) ) ;
#43996=B_SPLINE_CURVE_WITH_KNOTS ( 'NONE', 3,
 ( #52189, #58144, #40948, #19448, #15591, #68014, #57444, #14900 ),
 .UNSPECIFIED., .F., .F.,
 ( 4, 2, 2, 4 ),
 ( 0.000000000000000000, 0.0004249208466734696334, 0.0008498416933469392668, 0.001699683386693891327 ),
 .UNSPECIFIED. ) ;
#44006=DIRECTION ( 'NONE',  ( -1.000000000000000000, 0.000000000000000000, -0.000000000000000000 ) ) ;
#44016=LINE ( 'NONE', #65427, #27004 ) ;
#44029=UNCERTAINTY_MEASURE_WITH_UNIT (LENGTH_MEASURE( 1.000000000000000082E-05 ), #14697, 'distance_accuracy_value', 'NONE');
#44036=EDGE_CURVE ( 'NONE', #15405, #52477, #62723, .T. ) ;
#44042=STYLED_ITEM ( 'NONE', ( #57978 ), #25220 ) ;
#44044=FILL_AREA_STYLE_COLOUR ( '', #37101 ) ;
#44045=CIRCLE ( 'NONE', #137, 0.9999999999999986677 ) ;
#44048=ORIENTED_EDGE ( 'NONE', *, *, #30154, .F. ) ;
#44052=VERTEX_POINT ( 'NONE', #58172 ) ;
#44054=DIRECTION ( 'NONE',  ( 0.000000000000000000, 0.000000000000000000, 1.000000000000000000 ) ) ;
#44057=CARTESIAN_POINT ( 'NONE',  ( 57.00000000000000000, 14.00000000000000000, -72.50402776293826435 ) ) ;
#44060=CYLINDRICAL_SURFACE ( 'NONE', #43023, 4.999999999999997335 ) ;
#44068=VERTEX_POINT ( 'NONE', #65156 ) ;
#44072=FILL_AREA_STYLE ('',( #54892 ) ) ;
#44077=MECHANICAL_DESIGN_GEOMETRIC_PRESENTATION_REPRESENTATION('',(#19303),#48592);
#44097=SURFACE_STYLE_FILL_AREA ( #65140 ) ;
#44104=SURFACE_STYLE_USAGE ( .BOTH. , #22600 ) ;
#44105=ORIENTED_EDGE ( 'NONE', *, *, #60971, .T. ) ;
#44108=SURFACE_STYLE_FILL_AREA ( #55986 ) ;
#44113=FILL_AREA_STYLE_COLOUR ( '', #15716 ) ;
#44118=DIRECTION ( 'NONE',  ( 1.000000000000000000, -0.000000000000000000, -1.300977106640434891E-16 ) ) ;
#44126=PRESENTATION_STYLE_ASSIGNMENT (( #1446 ) ) ;
#44128=STYLED_ITEM ( 'NONE', ( #21968 ), #54665 ) ;
#44130=CARTESIAN_POINT ( 'NONE',  ( 86.21825843581743243, 5.000000000000000000, -39.83014742847162637 ) ) ;
#44131=SURFACE_STYLE_USAGE ( .BOTH. , #22628 ) ;
#44135=ORIENTED_EDGE ( 'NONE', *, *, #55760, .F. ) ;
#44142=DIRECTION ( 'NONE',  ( -0.000000000000000000, -1.000000000000000000, 0.000000000000000000 ) ) ;
#44143=EDGE_CURVE ( 'NONE', #35442, #29587, #53907, .T. ) ;
#44148=FACE_OUTER_BOUND ( 'NONE', #65286, .T. ) ;
#44151=UNCERTAINTY_MEASURE_WITH_UNIT (LENGTH_MEASURE( 1.000000000000000082E-05 ), #5018, 'distance_accuracy_value', 'NONE');
#44157=FACE_OUTER_BOUND ( 'NONE', #44652, .T. ) ;
#44162=ORIENTED_EDGE ( 'NONE', *, *, #40004, .F. ) ;
#44186=CARTESIAN_POINT ( 'NONE',  ( 22.00000000000002132, 42.00000000000000000, 75.00000000000000000 ) ) ;
#44191=SURFACE_SIDE_STYLE ('',( #1153 ) ) ;
#44198=( NAMED_UNIT ( * ) SI_UNIT ( $, .STERADIAN. ) SOLID_ANGLE_UNIT ( ) );
#44200=ADVANCED_FACE ( 'NONE', ( #50381 ), #40189, .T. ) ;
#44202=AXIS2_PLACEMENT_3D ( 'NONE', #35359, #9324, #45928 ) ;
#44212=DIRECTION ( 'NONE',  ( 0.000000000000000000, 0.000000000000000000, 1.000000000000000000 ) ) ;
#44216=CARTESIAN_POINT ( 'NONE',  ( 82.09357085539566867, 5.000000000000000000, -37.00402776293823592 ) ) ;
#44232=DIRECTION ( 'NONE',  ( -0.000000000000000000, 0.3420201433256629953, 0.9396926207859104263 ) ) ;
#44238=ORIENTED_EDGE ( 'NONE', *, *, #66932, .T. ) ;
#44243=FILL_AREA_STYLE_COLOUR ( '', #35147 ) ;
#44249=EDGE_LOOP ( 'NONE', ( #60003, #60210, #62883, #49140 ) ) ;
#44250=FILL_AREA_STYLE_COLOUR ( '', #21488 ) ;
#44256=CARTESIAN_POINT ( 'NONE',  ( 11.00000000000001776, 16.44305403005404287, 6.465863758942333782E-16 ) ) ;
#44259=AXIS2_PLACEMENT_3D ( 'NONE', #67279, #29282, #66228 ) ;
#44262=B_SPLINE_CURVE_WITH_KNOTS ( 'NONE', 3,
 ( #43385, #64431, #53198, #68678, #32759, #16281, #20478, #54210 ),
 .UNSPECIFIED., .F., .F.,
 ( 4, 2, 2, 4 ),
 ( -6.733023926831683363E-06, 0.0008427316310560315328, 0.001267463958547471355, 0.001692196286038911502 ),
 .UNSPECIFIED. ) ;
#44263=ORIENTED_EDGE ( 'NONE', *, *, #18817, .F. ) ;
#44266=( LENGTH_UNIT ( ) NAMED_UNIT ( * ) SI_UNIT ( .MILLI., .METRE. ) );
#44275=VERTEX_POINT ( 'NONE', #54930 ) ;
#44282=DIRECTION ( 'NONE',  ( -0.000000000000000000, -1.000000000000000000, -0.000000000000000000 ) ) ;
#44290=MECHANICAL_DESIGN_GEOMETRIC_PRESENTATION_REPRESENTATION('',(#55481),#42039);
#44302=ADVANCED_FACE ( 'NONE', ( #8167 ), #7850, .T. ) ;
#44303=( NAMED_UNIT ( * ) PLANE_ANGLE_UNIT ( ) SI_UNIT ( $, .RADIAN. ) );
#44315=CARTESIAN_POINT ( 'NONE',  ( 3.000000000000002665, 0.000000000000000000, -89.00000000000000000 ) ) ;
#44324=DIRECTION ( 'NONE',  ( -0.000000000000000000, -1.000000000000000000, 0.000000000000000000 ) ) ;
#44329=LINE ( 'NONE', #39037, #11639 ) ;
#44331=ORIENTED_EDGE ( 'NONE', *, *, #14538, .F. ) ;
#44335=CARTESIAN_POINT ( 'NONE',  ( 57.00000000000000000, 5.000000000000000000, 60.00402776293825724 ) ) ;
#44338=SURFACE_SIDE_STYLE ('',( #48918 ) ) ;
#44345=CARTESIAN_POINT ( 'NONE',  ( 10.00000000000001776, 43.00000000000000000, 29.68999999999999417 ) ) ;
#44360=AXIS2_PLACEMENT_3D ( 'NONE', #52930, #25477, #25139 ) ;
#44364=EDGE_CURVE ( 'NONE', #17013, #39245, #37087, .T. ) ;
#44365=( NAMED_UNIT ( * ) PLANE_ANGLE_UNIT ( ) SI_UNIT ( $, .RADIAN. ) );
#44366=SURFACE_SIDE_STYLE ('',( #12278 ) ) ;
#44367=( NAMED_UNIT ( * ) SI_UNIT ( $, .STERADIAN. ) SOLID_ANGLE_UNIT ( ) );
#44368=CARTESIAN_POINT ( 'NONE',  ( 57.00000000000000000, 0.000000000000000000, -79.00402776293826435 ) ) ;
#44381=DIRECTION ( 'NONE',  ( -0.000000000000000000, 1.000000000000000000, -0.000000000000000000 ) ) ;
#44382=CIRCLE ( 'NONE', #36492, 1.000000000000000888 ) ;
#44386=COLOUR_RGB ( '', 0.09019608, 0.27058824, 0.51372549) ;
#44390=EDGE_CURVE ( 'NONE', #68594, #54457, #30275, .T. ) ;
#44393=EDGE_LOOP ( 'NONE', ( #50707, #60765, #33485, #57881 ) ) ;
#44399=PRESENTATION_STYLE_ASSIGNMENT (( #18657 ) ) ;
#44400=B_SPLINE_CURVE_WITH_KNOTS ( 'NONE', 3,
 ( #66350, #44945, #55457, #34353, #29041, #7281, #55803, #24139 ),
 .UNSPECIFIED., .F., .F.,
 ( 4, 2, 2, 4 ),
 ( 4.336808689942017736E-19, 0.0004249208466734718018, 0.0008498416933469431700, 0.001699683386693885906 ),
 .UNSPECIFIED. ) ;
#44414=( NAMED_UNIT ( * ) PLANE_ANGLE_UNIT ( ) SI_UNIT ( $, .RADIAN. ) );
#44419=FILL_AREA_STYLE_COLOUR ( '', #21804 ) ;
#44426=STYLED_ITEM ( 'NONE', ( #18521 ), #2245 ) ;
#44428=FILL_AREA_STYLE_COLOUR ( '', #9229 ) ;
#44437=ORIENTED_EDGE ( 'NONE', *, *, #51736, .F. ) ;
#44443=( NAMED_UNIT ( * ) SI_UNIT ( $, .STERADIAN. ) SOLID_ANGLE_UNIT ( ) );
#44446=EDGE_CURVE ( 'NONE', #42679, #17912, #40895, .T. ) ;
#44448=LINE ( 'NONE', #27148, #31943 ) ;
#44452=PRESENTATION_STYLE_ASSIGNMENT (( #44104 ) ) ;
#44457=STYLED_ITEM ( 'NONE', ( #17441 ), #63878 ) ;
#44463=DIRECTION ( 'NONE',  ( 1.000000000000000000, -0.000000000000000000, 0.000000000000000000 ) ) ;
#44467=EDGE_CURVE ( 'NONE', #61113, #26732, #46891, .T. ) ;
#44468=MECHANICAL_DESIGN_GEOMETRIC_PRESENTATION_REPRESENTATION('',(#16336),#32065);
#44469=PRESENTATION_STYLE_ASSIGNMENT (( #38498 ) ) ;
#44478=LINE ( 'NONE', #61610, #60730 ) ;
#44485=DIRECTION ( 'NONE',  ( 0.000000000000000000, 0.000000000000000000, -1.000000000000000000 ) ) ;
#44488=SURFACE_STYLE_USAGE ( .BOTH. , #3829 ) ;
#44508=CARTESIAN_POINT ( 'NONE',  ( 0.000000000000000000, 43.00000000000000000, 0.000000000000000000 ) ) ;
#44547=DIRECTION ( 'NONE',  ( -0.000000000000000000, -1.000000000000000000, -0.000000000000000000 ) ) ;
#44559=PRESENTATION_STYLE_ASSIGNMENT (( #34632 ) ) ;
#44562=CARTESIAN_POINT ( 'NONE',  ( 57.00000000000000000, 0.000000000000000000, -77.00402776293825013 ) ) ;
#44564=AXIS2_PLACEMENT_3D ( 'NONE', #39706, #41101, #62509 ) ;
#44565=EDGE_LOOP ( 'NONE', ( #20357, #29550 ) ) ;
#44566=( NAMED_UNIT ( * ) SI_UNIT ( $, .STERADIAN. ) SOLID_ANGLE_UNIT ( ) );
#44570=FACE_BOUND ( 'NONE', #54875, .T. ) ;
#44574=SURFACE_SIDE_STYLE ('',( #22729 ) ) ;
#44590=( NAMED_UNIT ( * ) PLANE_ANGLE_UNIT ( ) SI_UNIT ( $, .RADIAN. ) );
#44592=STYLED_ITEM ( 'NONE', ( #57602 ), #3197 ) ;
#44593=CYLINDRICAL_SURFACE ( 'NONE', #46538, 0.9999999999999974465 ) ;
#44599=CARTESIAN_POINT ( 'NONE',  ( 1.000000000000000000, 42.00000000000000000, 79.00402776293826435 ) ) ;
#44600=PRESENTATION_STYLE_ASSIGNMENT (( #533 ) ) ;
#44616=FACE_OUTER_BOUND ( 'NONE', #6308, .T. ) ;
#44618=EDGE_CURVE ( 'NONE', #32368, #61460, #48252, .T. ) ;
#44632=UNCERTAINTY_MEASURE_WITH_UNIT (LENGTH_MEASURE( 1.000000000000000082E-05 ), #60415, 'distance_accuracy_value', 'NONE');
#44633=DIRECTION ( 'NONE',  ( 0.000000000000000000, 1.000000000000000000, 0.000000000000000000 ) ) ;
#44636=MECHANICAL_DESIGN_GEOMETRIC_PRESENTATION_REPRESENTATION('',(#51330),#50226);
#44637=DIRECTION ( 'NONE',  ( -0.000000000000000000, -1.000000000000000000, -0.000000000000000000 ) ) ;
#44638=( GEOMETRIC_REPRESENTATION_CONTEXT ( 3 ) GLOBAL_UNCERTAINTY_ASSIGNED_CONTEXT ( ( #8646 ) ) GLOBAL_UNIT_ASSIGNED_CONTEXT ( ( #26456, #37063, #26103 ) ) REPRESENTATION_CONTEXT ( 'NONE', 'WORKASPACE' ) );
#44641=CYLINDRICAL_SURFACE ( 'NONE', #47477, 1.000000000000000888 ) ;
#44644=CARTESIAN_POINT ( 'NONE',  ( 0.4142135623730956451, 13.99999999999999645, -35.49999999999999289 ) ) ;
#44652=EDGE_LOOP ( 'NONE', ( #11036, #1129, #1486, #15736 ) ) ;
#44654=CIRCLE ( 'NONE', #64838, 112.9999999999981526 ) ;
#44657=SURFACE_SIDE_STYLE ('',( #38689 ) ) ;
#44668=VERTEX_POINT ( 'NONE', #26058 ) ;
#44673=( NAMED_UNIT ( * ) SI_UNIT ( $, .STERADIAN. ) SOLID_ANGLE_UNIT ( ) );
#44678=FILL_AREA_STYLE_COLOUR ( '', #30 ) ;
#44694=DIRECTION ( 'NONE',  ( 0.000000000000000000, 0.000000000000000000, -1.000000000000000000 ) ) ;
#44696=VERTEX_POINT ( 'NONE', #61191 ) ;
#44705=DIRECTION ( 'NONE',  ( 0.000000000000000000, 1.000000000000000000, 0.000000000000000000 ) ) ;
#44715=CARTESIAN_POINT ( 'NONE',  ( 10.00000000000000711, 50.00000000000000000, -60.00000000000000000 ) ) ;
#44719=( NAMED_UNIT ( * ) PLANE_ANGLE_UNIT ( ) SI_UNIT ( $, .RADIAN. ) );
#44725=FACE_OUTER_BOUND ( 'NONE', #57773, .T. ) ;
#44733=( GEOMETRIC_REPRESENTATION_CONTEXT ( 3 ) GLOBAL_UNCERTAINTY_ASSIGNED_CONTEXT ( ( #57931 ) ) GLOBAL_UNIT_ASSIGNED_CONTEXT ( ( #35758, #24149, #57195 ) ) REPRESENTATION_CONTEXT ( 'NONE', 'WORKASPACE' ) );
#44737=PRESENTATION_STYLE_ASSIGNMENT (( #49991 ) ) ;
#44758=UNCERTAINTY_MEASURE_WITH_UNIT (LENGTH_MEASURE( 1.000000000000000082E-05 ), #30737, 'distance_accuracy_value', 'NONE');
#44764=ORIENTED_EDGE ( 'NONE', *, *, #56526, .T. ) ;
#44768=EDGE_LOOP ( 'NONE', ( #53002, #56661, #39463, #34919, #53361, #3105 ) ) ;
#44769=DIRECTION ( 'NONE',  ( 1.000000000000000000, 0.000000000000000000, -1.300977106640434891E-16 ) ) ;
#44784=VERTEX_POINT ( 'NONE', #56957 ) ;
#44786=COLOUR_RGB ( '', 0.66274510, 0.83137255, 0.94901961) ;
#44789=( GEOMETRIC_REPRESENTATION_CONTEXT ( 3 ) GLOBAL_UNCERTAINTY_ASSIGNED_CONTEXT ( ( #62822 ) ) GLOBAL_UNIT_ASSIGNED_CONTEXT ( ( #12110, #27914, #22683 ) ) REPRESENTATION_CONTEXT ( 'NONE', 'WORKASPACE' ) );
#44794=SURFACE_SIDE_STYLE ('',( #28185 ) ) ;
#44798=DIRECTION ( 'NONE',  ( -1.000000000000000000, 0.000000000000000000, 0.000000000000000000 ) ) ;
#44807=CYLINDRICAL_SURFACE ( 'NONE', #36539, 4.999999999999997335 ) ;
#44808=COLOUR_RGB ( '', 0.72549020, 0.75294118, 0.79215686) ;
#44811=AXIS2_PLACEMENT_3D ( 'NONE', #57983, #47827, #63246 ) ;
#44815=CARTESIAN_POINT ( 'NONE',  ( 74.89452121010485541, 14.00000000000000000, 66.39042820928573008 ) ) ;
#44818=CARTESIAN_POINT ( 'NONE',  ( 27.00000000000001776, 14.00000000000000000, 29.68999999999999417 ) ) ;
#44832=EDGE_CURVE ( 'NONE', #8511, #22643, #51704, .T. ) ;
#44835=SURFACE_SIDE_STYLE ('',( #60955 ) ) ;
#44836=ORIENTED_EDGE ( 'NONE', *, *, #22975, .F. ) ;
#44841=FACE_OUTER_BOUND ( 'NONE', #61888, .T. ) ;
#44842=DIRECTION ( 'NONE',  ( -0.000000000000000000, -0.6449798928094537809, 0.7641995406119435064 ) ) ;
#44851=ADVANCED_FACE ( 'NONE', ( #35511 ), #29872, .T. ) ;
#44864=DIRECTION ( 'NONE',  ( 0.000000000000000000, 0.000000000000000000, -1.000000000000000000 ) ) ;
#44865=SURFACE_SIDE_STYLE ('',( #1510 ) ) ;
#44871=AXIS2_PLACEMENT_3D ( 'NONE', #18977, #62256, #34823 ) ;
#44873=CARTESIAN_POINT ( 'NONE',  ( 93.00000000000000000, 13.00000000000000178, 0.000000000000000000 ) ) ;
#44874=EDGE_CURVE ( 'NONE', #60366, #8099, #58429, .T. ) ;
#44881=FILL_AREA_STYLE ('',( #33591 ) ) ;
#44884=CARTESIAN_POINT ( 'NONE',  ( 10.58578643762692195, 17.78868675966042190, -3.198396408832238080E-15 ) ) ;
#44891=STYLED_ITEM ( 'NONE', ( #16319 ), #19793 ) ;
#44893=SURFACE_STYLE_FILL_AREA ( #28658 ) ;
#44897=( LENGTH_UNIT ( ) NAMED_UNIT ( * ) SI_UNIT ( .MILLI., .METRE. ) );
#44903=CIRCLE ( 'NONE', #46051, 25.00000000000001421 ) ;
#44909=( GEOMETRIC_REPRESENTATION_CONTEXT ( 3 ) GLOBAL_UNCERTAINTY_ASSIGNED_CONTEXT ( ( #31281 ) ) GLOBAL_UNIT_ASSIGNED_CONTEXT ( ( #62710, #35665, #13853 ) ) REPRESENTATION_CONTEXT ( 'NONE', 'WORKASPACE' ) );
#44913=DIRECTION ( 'NONE',  ( -1.000000000000000000, -0.000000000000000000, 1.300977106640434644E-16 ) ) ;
#44916=AXIS2_PLACEMENT_3D ( 'NONE', #167, #6900, #23098 ) ;
#44943=DIRECTION ( 'NONE',  ( -0.000000000000000000, -1.000000000000000000, 0.000000000000000000 ) ) ;
#44945=CARTESIAN_POINT ( 'NONE',  ( 0.8561460859850872351, 43.00000000000000000, 45.61250543006184444 ) ) ;
#44949=DIRECTION ( 'NONE',  ( -1.000000000000000000, 0.000000000000000000, -0.000000000000000000 ) ) ;
#44967=( GEOMETRIC_REPRESENTATION_CONTEXT ( 3 ) GLOBAL_UNCERTAINTY_ASSIGNED_CONTEXT ( ( #43397 ) ) GLOBAL_UNIT_ASSIGNED_CONTEXT ( ( #7052, #33105, #49286 ) ) REPRESENTATION_CONTEXT ( 'NONE', 'WORKASPACE' ) );
#44972=EDGE_CURVE ( 'NONE', #330, #40347, #59034, .T. ) ;
#44974=VECTOR ( 'NONE', #34449, 1000.000000000000000 ) ;
#44976=FILL_AREA_STYLE ('',( #24856 ) ) ;
#44979=EDGE_CURVE ( 'NONE', #20918, #49856, #46105, .T. ) ;
#44987=ORIENTED_EDGE ( 'NONE', *, *, #38094, .F. ) ;
#44990=CARTESIAN_POINT ( 'NONE',  ( 28.00000000000000000, 38.70020753820971748, -89.00000000000000000 ) ) ;
#44991=PLANE ( 'NONE',  #51241 ) ;
#45002=VERTEX_POINT ( 'NONE', #13106 ) ;
#45007=( GEOMETRIC_REPRESENTATION_CONTEXT ( 3 ) GLOBAL_UNCERTAINTY_ASSIGNED_CONTEXT ( ( #6487 ) ) GLOBAL_UNIT_ASSIGNED_CONTEXT ( ( #51686, #3431, #52046 ) ) REPRESENTATION_CONTEXT ( 'NONE', 'WORKASPACE' ) );
#45016=MECHANICAL_DESIGN_GEOMETRIC_PRESENTATION_REPRESENTATION('',(#46118),#10143);
#45020=AXIS2_PLACEMENT_3D ( 'NONE', #64021, #47209, #32018 ) ;
#45031=VERTEX_POINT ( 'NONE', #50759 ) ;
#45032=ORIENTED_EDGE ( 'NONE', *, *, #20983, .F. ) ;
#45055=DIRECTION ( 'NONE',  ( 0.000000000000000000, 0.000000000000000000, -1.000000000000000000 ) ) ;
#45057=AXIS2_PLACEMENT_3D ( 'NONE', #45670, #29797, #2667 ) ;
#45062=EDGE_LOOP ( 'NONE', ( #8888, #46615, #38034, #52569, #29712, #28571, #57273, #37953 ) ) ;
#45064=MECHANICAL_DESIGN_GEOMETRIC_PRESENTATION_REPRESENTATION('',(#36048),#57379);
#45067=SURFACE_STYLE_FILL_AREA ( #7041 ) ;
#45068=EDGE_CURVE ( 'NONE', #41524, #50329, #25059, .T. ) ;
#45069=( LENGTH_UNIT ( ) NAMED_UNIT ( * ) SI_UNIT ( .MILLI., .METRE. ) );
#45075=STYLED_ITEM ( 'NONE', ( #20559 ), #34621 ) ;
#45082=COLOUR_RGB ( '', 0.40784314, 0.44705882, 0.49803922) ;
#45087=ORIENTED_EDGE ( 'NONE', *, *, #9062, .T. ) ;
#45097=ORIENTED_EDGE ( 'NONE', *, *, #46583, .F. ) ;
#45112=VECTOR ( 'NONE', #27853, 1000.000000000000000 ) ;
#45114=ORIENTED_EDGE ( 'NONE', *, *, #64178, .T. ) ;
#45130=EDGE_CURVE ( 'NONE', #50401, #60879, #20302, .T. ) ;
#45142=ADVANCED_FACE ( 'NONE', ( #24017 ), #61295, .F. ) ;
#45146=EDGE_CURVE ( 'NONE', #36170, #15405, #3, .T. ) ;
#45148=SURFACE_STYLE_USAGE ( .BOTH. , #55999 ) ;
#45151=ORIENTED_EDGE ( 'NONE', *, *, #36008, .T. ) ;
#45157=CARTESIAN_POINT ( 'NONE',  ( 0.3542424171060606919, 42.77450929379337907, 74.52798306220823576 ) ) ;
#45162=ORIENTED_EDGE ( 'NONE', *, *, #60219, .T. ) ;
#45177=( GEOMETRIC_REPRESENTATION_CONTEXT ( 3 ) GLOBAL_UNCERTAINTY_ASSIGNED_CONTEXT ( ( #63001 ) ) GLOBAL_UNIT_ASSIGNED_CONTEXT ( ( #38503, #54268, #49048 ) ) REPRESENTATION_CONTEXT ( 'NONE', 'WORKASPACE' ) );
#45178=FACE_OUTER_BOUND ( 'NONE', #30217, .T. ) ;
#45187=CARTESIAN_POINT ( 'NONE',  ( 6.000000000000020428, 43.00000000000000711, 29.06445261836602256 ) ) ;
#45188=COLOUR_RGB ( '', 0.66274510, 0.83137255, 0.94901961) ;
#45209=AXIS2_PLACEMENT_3D ( 'NONE', #54571, #6379, #27809 ) ;
#45224=ADVANCED_FACE ( 'NONE', ( #15239 ), #69025, .T. ) ;
#45229=CARTESIAN_POINT ( 'NONE',  ( 10.00000000000000533, 50.00000000000000000, -60.00000000000000000 ) ) ;
#45241=ADVANCED_FACE ( 'NONE', ( #57418 ), #30665, .T. ) ;
#45244=PLANE ( 'NONE',  #64434 ) ;
#45249=AXIS2_PLACEMENT_3D ( 'NONE', #46867, #20417, #5258 ) ;
#45250=VECTOR ( 'NONE', #8698, 1000.000000000000000 ) ;
#45264=CARTESIAN_POINT ( 'NONE',  ( 6.330869393641158638, 43.00000000000000000, 28.38386403503541899 ) ) ;
#45276=AXIS2_PLACEMENT_3D ( 'NONE', #66691, #29383, #51911 ) ;
#45281=VERTEX_POINT ( 'NONE', #44057 ) ;
#45282=SURFACE_STYLE_USAGE ( .BOTH. , #30690 ) ;
#45285=DIRECTION ( 'NONE',  ( 0.000000000000000000, 1.000000000000000000, 0.000000000000000000 ) ) ;
#45291=LINE ( 'NONE', #40015, #43717 ) ;
#45292=EDGE_LOOP ( 'NONE', ( #60762, #54536 ) ) ;
#45295=CARTESIAN_POINT ( 'NONE',  ( 8.000000000000030198, 5.000000000000000000, -32.00402776293825013 ) ) ;
#45299=DIRECTION ( 'NONE',  ( -1.982541115402069054E-16, -0.000000000000000000, 1.000000000000000000 ) ) ;
#45304=ORIENTED_EDGE ( 'NONE', *, *, #28505, .T. ) ;
#45310=CARTESIAN_POINT ( 'NONE',  ( 31.00000000000000355, 43.00000000000000000, -45.61250543006184444 ) ) ;
#45311=SURFACE_STYLE_USAGE ( .BOTH. , #29426 ) ;
#45319=UNCERTAINTY_MEASURE_WITH_UNIT (LENGTH_MEASURE( 1.000000000000000082E-05 ), #61008, 'distance_accuracy_value', 'NONE');
#45330=DIRECTION ( 'NONE',  ( 0.000000000000000000, 0.000000000000000000, -1.000000000000000000 ) ) ;
#45331=LINE ( 'NONE', #1268, #42035 ) ;
#45341=CARTESIAN_POINT ( 'NONE',  ( 75.83633811589984930, 14.00000000000000000, -66.72655454856717938 ) ) ;
#45343=ORIENTED_EDGE ( 'NONE', *, *, #30020, .F. ) ;
#45345=DIRECTION ( 'NONE',  ( -1.000000000000000000, -0.000000000000000000, 1.300977106640434891E-16 ) ) ;
#45351=ORIENTED_EDGE ( 'NONE', *, *, #40482, .F. ) ;
#45354=DIRECTION ( 'NONE',  ( -1.000000000000000000, 0.000000000000000000, 0.000000000000000000 ) ) ;
#45355=DIRECTION ( 'NONE',  ( 1.000000000000000000, 0.000000000000000000, 0.000000000000000000 ) ) ;
#45362=SURFACE_SIDE_STYLE ('',( #51291 ) ) ;
#45364=MECHANICAL_DESIGN_GEOMETRIC_PRESENTATION_REPRESENTATION('',(#18519),#42019);
#45368=SURFACE_SIDE_STYLE ('',( #18602 ) ) ;
#45394=CARTESIAN_POINT ( 'NONE',  ( 36.00000000000002132, 5.000000000000000000, -77.00402776293825013 ) ) ;
#45396=ORIENTED_EDGE ( 'NONE', *, *, #66567, .T. ) ;
#45400=AXIS2_PLACEMENT_3D ( 'NONE', #44216, #6507, #27950 ) ;
#45406=CIRCLE ( 'NONE', #31884, 3.499999999999999556 ) ;
#45412=CIRCLE ( 'NONE', #21760, 17.00000000000000711 ) ;
#45423=( GEOMETRIC_REPRESENTATION_CONTEXT ( 3 ) GLOBAL_UNCERTAINTY_ASSIGNED_CONTEXT ( ( #34158 ) ) GLOBAL_UNIT_ASSIGNED_CONTEXT ( ( #46903, #66931, #34902 ) ) REPRESENTATION_CONTEXT ( 'NONE', 'WORKASPACE' ) );
#45432=DIRECTION ( 'NONE',  ( 0.000000000000000000, 0.3420201433256694346, -0.9396926207859082059 ) ) ;
#45447=( LENGTH_UNIT ( ) NAMED_UNIT ( * ) SI_UNIT ( .MILLI., .METRE. ) );
#45470=DIRECTION ( 'NONE',  ( -2.478176394252580648E-16, 0.000000000000000000, -1.000000000000000000 ) ) ;
#45471=UNCERTAINTY_MEASURE_WITH_UNIT (LENGTH_MEASURE( 1.000000000000000082E-05 ), #34102, 'distance_accuracy_value', 'NONE');
#45476=FACE_OUTER_BOUND ( 'NONE', #52338, .T. ) ;
#45477=DIRECTION ( 'NONE',  ( -2.478176394252586564E-16, 0.000000000000000000, -1.000000000000000000 ) ) ;
#45481=EDGE_CURVE ( 'NONE', #20918, #52016, #66140, .T. ) ;
#45484=MECHANICAL_DESIGN_GEOMETRIC_PRESENTATION_REPRESENTATION('',(#3880),#49969);
#45486=( GEOMETRIC_REPRESENTATION_CONTEXT ( 3 ) GLOBAL_UNCERTAINTY_ASSIGNED_CONTEXT ( ( #67164 ) ) GLOBAL_UNIT_ASSIGNED_CONTEXT ( ( #35708, #751, #48038 ) ) REPRESENTATION_CONTEXT ( 'NONE', 'WORKASPACE' ) );
#45489=CIRCLE ( 'NONE', #9503, 1.000000000000000888 ) ;
#45490=ORIENTED_EDGE ( 'NONE', *, *, #48910, .T. ) ;
#45491=SURFACE_SIDE_STYLE ('',( #29241 ) ) ;
#45499=SURFACE_STYLE_USAGE ( .BOTH. , #44794 ) ;
#45516=DIRECTION ( 'NONE',  ( 1.000000000000000000, -0.000000000000000000, 0.000000000000000000 ) ) ;
#45524=LINE ( 'NONE', #35270, #45569 ) ;
#45538=SURFACE_STYLE_USAGE ( .BOTH. , #44835 ) ;
#45545=FACE_OUTER_BOUND ( 'NONE', #43274, .T. ) ;
#45550=( LENGTH_UNIT ( ) NAMED_UNIT ( * ) SI_UNIT ( .MILLI., .METRE. ) );
#45553=MECHANICAL_DESIGN_GEOMETRIC_PRESENTATION_REPRESENTATION('',(#17416),#69075);
#45560=AXIS2_PLACEMENT_3D ( 'NONE', #69604, #47522, #42255 ) ;
#45567=SURFACE_SIDE_STYLE ('',( #24062 ) ) ;
#45568=ADVANCED_FACE ( 'NONE', ( #20996, #31535, #10105 ), #153, .F. ) ;
#45569=VECTOR ( 'NONE', #19776, 1000.000000000000000 ) ;
#45571=CARTESIAN_POINT ( 'NONE',  ( 22.00000000000000711, 43.00000000000000000, -45.61250543006183733 ) ) ;
#45593=PLANE ( 'NONE',  #57683 ) ;
#45596=APPLICATION_CONTEXT ( 'automotive_design' ) ;
#45605=CIRCLE ( 'NONE', #61269, 4.999999999999997335 ) ;
#45606=ORIENTED_EDGE ( 'NONE', *, *, #16849, .T. ) ;
#45617=CIRCLE ( 'NONE', #56831, 110.0000000000000142 ) ;
#45624=EDGE_CURVE ( 'NONE', #35471, #55787, #54374, .T. ) ;
#45645=EDGE_LOOP ( 'NONE', ( #700, #23828, #60501, #45707, #24606, #54027, #63414, #38624 ) ) ;
#45653=( GEOMETRIC_REPRESENTATION_CONTEXT ( 3 ) GLOBAL_UNCERTAINTY_ASSIGNED_CONTEXT ( ( #33299 ) ) GLOBAL_UNIT_ASSIGNED_CONTEXT ( ( #65731, #18238, #11570 ) ) REPRESENTATION_CONTEXT ( 'NONE', 'WORKASPACE' ) );
#45657=CARTESIAN_POINT ( 'NONE',  ( 96.10348817448824832, 0.000000000000000000, -27.38099488609876531 ) ) ;
#45663=ADVANCED_FACE ( 'NONE', ( #49139 ), #18144, .T. ) ;
#45665=COLOUR_RGB ( '', 0.66274510, 0.83137255, 0.94901961) ;
#45670=CARTESIAN_POINT ( 'NONE',  ( 92.41620014002536720, 0.000000000000000000, 24.00402776293825369 ) ) ;
#45671=CARTESIAN_POINT ( 'NONE',  ( 33.00000000000000711, 14.00000000000000000, -35.50000000000000000 ) ) ;
#45676=ORIENTED_EDGE ( 'NONE', *, *, #28891, .F. ) ;
#45686=DIRECTION ( 'NONE',  ( 0.000000000000000000, 1.000000000000000000, 0.000000000000000000 ) ) ;
#45692=SURFACE_STYLE_USAGE ( .BOTH. , #8714 ) ;
#45700=EDGE_LOOP ( 'NONE', ( #13004, #50335, #10285, #10605 ) ) ;
#45704=COLOUR_RGB ( '', 0.09019608, 0.27058824, 0.51372549) ;
#45707=ORIENTED_EDGE ( 'NONE', *, *, #1626, .T. ) ;
#45711=( NAMED_UNIT ( * ) SI_UNIT ( $, .STERADIAN. ) SOLID_ANGLE_UNIT ( ) );
#45721=VERTEX_POINT ( 'NONE', #51535 ) ;
#45725=CARTESIAN_POINT ( 'NONE',  ( 4.000000000000029310, 43.00000000000000000, 90.00000000000000000 ) ) ;
#45726=CARTESIAN_POINT ( 'NONE',  ( 12.00000000000001776, 15.00000000000000000, -29.68999999999999417 ) ) ;
#45731=( LENGTH_UNIT ( ) NAMED_UNIT ( * ) SI_UNIT ( .MILLI., .METRE. ) );
#45735=( LENGTH_UNIT ( ) NAMED_UNIT ( * ) SI_UNIT ( .MILLI., .METRE. ) );
#45740=( NAMED_UNIT ( * ) SI_UNIT ( $, .STERADIAN. ) SOLID_ANGLE_UNIT ( ) );
#45746=CARTESIAN_POINT ( 'NONE',  ( 35.99999999999999289, 5.000000000000000000, 72.00402776293825013 ) ) ;
#45747=FACE_OUTER_BOUND ( 'NONE', #41099, .T. ) ;
#45756=FACE_OUTER_BOUND ( 'NONE', #8106, .T. ) ;
#45760=LINE ( 'NONE', #24261, #1574 ) ;
#45775=SURFACE_STYLE_FILL_AREA ( #24278 ) ;
#45777=FILL_AREA_STYLE_COLOUR ( '', #57760 ) ;
#45784=STYLED_ITEM ( 'NONE', ( #58079 ), #65509 ) ;
#45785=EDGE_CURVE ( 'NONE', #29677, #44784, #1261, .T. ) ;
#45788=ORIENTED_EDGE ( 'NONE', *, *, #6820, .T. ) ;
#45792=( LENGTH_UNIT ( ) NAMED_UNIT ( * ) SI_UNIT ( .MILLI., .METRE. ) );
#45798=ADVANCED_FACE ( 'NONE', ( #58205 ), #53287, .F. ) ;
#45802=ORIENTED_EDGE ( 'NONE', *, *, #20150, .T. ) ;
#45803=FILL_AREA_STYLE ('',( #24309 ) ) ;
#45819=SURFACE_STYLE_FILL_AREA ( #19030 ) ;
#45833=CARTESIAN_POINT ( 'NONE',  ( 4.000000000000002665, 43.00000000000000000, -89.00000000000000000 ) ) ;
#45856=EDGE_CURVE ( 'NONE', #4579, #49504, #13680, .T. ) ;
#45865=PLANE ( 'NONE',  #12598 ) ;
#45869=( LENGTH_UNIT ( ) NAMED_UNIT ( * ) SI_UNIT ( .MILLI., .METRE. ) );
#45870=ORIENTED_EDGE ( 'NONE', *, *, #59099, .T. ) ;
#45876=CYLINDRICAL_SURFACE ( 'NONE', #24672, 0.9999999999999995559 ) ;
#45878=VERTEX_POINT ( 'NONE', #26178 ) ;
#45879=LINE ( 'NONE', #62018, #10053 ) ;
#45880=AXIS2_PLACEMENT_3D ( 'NONE', #9308, #30731, #25463 ) ;
#45888=CARTESIAN_POINT ( 'NONE',  ( 57.00000000000000000, 5.000000000000000000, 60.00402776293827145 ) ) ;
#45899=EDGE_CURVE ( 'NONE', #39384, #34141, #66453, .T. ) ;
#45901=SPHERICAL_SURFACE ( 'NONE', #33468, 1.000000000000000000 ) ;
#45906=CIRCLE ( 'NONE', #58274, 1.000000000000000888 ) ;
#45907=SURFACE_STYLE_FILL_AREA ( #68385 ) ;
#45908=VECTOR ( 'NONE', #65810, 1000.000000000000114 ) ;
#45914=PRODUCT_CONTEXT ( 'NONE', #62165, 'mechanical' ) ;
#45923=LINE ( 'NONE', #35700, #49617 ) ;
#45928=DIRECTION ( 'NONE',  ( 1.000000000000000000, 0.000000000000000000, 0.000000000000000000 ) ) ;
#45938=( LENGTH_UNIT ( ) NAMED_UNIT ( * ) SI_UNIT ( .MILLI., .METRE. ) );
#45940=DIRECTION ( 'NONE',  ( 1.000000000000000000, -0.000000000000000000, -1.300977106640434891E-16 ) ) ;
#45947=PRESENTATION_STYLE_ASSIGNMENT (( #7940 ) ) ;
#45948=( NAMED_UNIT ( * ) PLANE_ANGLE_UNIT ( ) SI_UNIT ( $, .RADIAN. ) );
#45954=CIRCLE ( 'NONE', #24505, 19.99999999999998934 ) ;
#45967=DIRECTION ( 'NONE',  ( 0.000000000000000000, 0.000000000000000000, -1.000000000000000000 ) ) ;
#45970=COLOUR_RGB ( '', 0.72549020, 0.75294118, 0.79215686) ;
#45982=ADVANCED_FACE ( 'NONE', ( #6449 ), #35287, .T. ) ;
#45992=DIRECTION ( 'NONE',  ( 0.000000000000000000, -0.000000000000000000, 1.000000000000000000 ) ) ;
#45999=DIRECTION ( 'NONE',  ( 0.000000000000000000, 1.000000000000000000, 0.000000000000000000 ) ) ;
#46001=CIRCLE ( 'NONE', #33575, 4.999999999999997335 ) ;
#46005=AXIS2_PLACEMENT_3D ( 'NONE', #49781, #2565, #66997 ) ;
#46016=EDGE_CURVE ( 'NONE', #55848, #408, #21527, .T. ) ;
#46022=ORIENTED_EDGE ( 'NONE', *, *, #40438, .F. ) ;
#46025=( LENGTH_UNIT ( ) NAMED_UNIT ( * ) SI_UNIT ( .MILLI., .METRE. ) );
#46026=VERTEX_POINT ( 'NONE', #20119 ) ;
#46045=DIRECTION ( 'NONE',  ( 0.000000000000000000, -1.000000000000000000, 0.000000000000000000 ) ) ;
#46047=( LENGTH_UNIT ( ) NAMED_UNIT ( * ) SI_UNIT ( .MILLI., .METRE. ) );
#46051=AXIS2_PLACEMENT_3D ( 'NONE', #26193, #20224, #68791 ) ;
#46054=ORIENTED_EDGE ( 'NONE', *, *, #55351, .F. ) ;
#46068=( GEOMETRIC_REPRESENTATION_CONTEXT ( 3 ) GLOBAL_UNCERTAINTY_ASSIGNED_CONTEXT ( ( #65899 ) ) GLOBAL_UNIT_ASSIGNED_CONTEXT ( ( #45792, #34169, #66884 ) ) REPRESENTATION_CONTEXT ( 'NONE', 'WORKASPACE' ) );
#46070=COLOUR_RGB ( '', 0.09019608, 0.27058824, 0.51372549) ;
#46075=SURFACE_STYLE_USAGE ( .BOTH. , #34786 ) ;
#46084=FACE_OUTER_BOUND ( 'NONE', #43921, .T. ) ;
#46091=EDGE_CURVE ( 'NONE', #1198, #35184, #50800, .T. ) ;
#46095=AXIS2_PLACEMENT_3D ( 'NONE', #18943, #40445, #13687 ) ;
#46102=ORIENTED_EDGE ( 'NONE', *, *, #66552, .F. ) ;
#46104=DIRECTION ( 'NONE',  ( -0.000000000000000000, 1.000000000000000000, -0.000000000000000000 ) ) ;
#46105=CIRCLE ( 'NONE', #32593, 113.0000000000030127 ) ;
#46115=ORIENTED_EDGE ( 'NONE', *, *, #18505, .F. ) ;
#46118=STYLED_ITEM ( 'NONE', ( #26657 ), #21041 ) ;
#46122=CARTESIAN_POINT ( 'NONE',  ( 7.999999999999992895, 5.000000000000000000, -24.00402776293826079 ) ) ;
#46153=DIRECTION ( 'NONE',  ( -1.000000000000000000, 0.000000000000000000, 0.000000000000000000 ) ) ;
#46155=CYLINDRICAL_SURFACE ( 'NONE', #38477, 1.000000000000000888 ) ;
#46160=SURFACE_SIDE_STYLE ('',( #14451 ) ) ;
#46163=( GEOMETRIC_REPRESENTATION_CONTEXT ( 3 ) GLOBAL_UNCERTAINTY_ASSIGNED_CONTEXT ( ( #2448 ) ) GLOBAL_UNIT_ASSIGNED_CONTEXT ( ( #57735, #35233, #66908 ) ) REPRESENTATION_CONTEXT ( 'NONE', 'WORKASPACE' ) );
#46165=DIRECTION ( 'NONE',  ( -0.000000000000000000, -0.000000000000000000, 1.000000000000000000 ) ) ;
#46166=ORIENTED_EDGE ( 'NONE', *, *, #63915, .T. ) ;
#46167=CARTESIAN_POINT ( 'NONE',  ( 22.49457430327976581, 26.84935569382991716, -27.39837423296133778 ) ) ;
#46172=AXIS2_PLACEMENT_3D ( 'NONE', #67982, #40206, #61611 ) ;
#46173=CARTESIAN_POINT ( 'NONE',  ( 57.00000000000000000, 0.9999999999999991118, 60.00402776293827145 ) ) ;
#46175=UNCERTAINTY_MEASURE_WITH_UNIT (LENGTH_MEASURE( 1.000000000000000082E-05 ), #23556, 'distance_accuracy_value', 'NONE');
#46181=LINE ( 'NONE', #12471, #65792 ) ;
#46187=FILL_AREA_STYLE ('',( #8179 ) ) ;
#46192=COLOUR_RGB ( '', 0.66274510, 0.83137255, 0.94901961) ;
#46197=DIRECTION ( 'NONE',  ( 2.478176394252580648E-16, 0.000000000000000000, 1.000000000000000000 ) ) ;
#46199=DIRECTION ( 'NONE',  ( -1.000000000000000000, 0.000000000000000000, 0.000000000000000000 ) ) ;
#46200=ADVANCED_FACE ( 'NONE', ( #50015 ), #5673, .F. ) ;
#46213=MECHANICAL_DESIGN_GEOMETRIC_PRESENTATION_REPRESENTATION('',(#14701),#43949);
#46215=ORIENTED_EDGE ( 'NONE', *, *, #53670, .T. ) ;
#46220=AXIS2_PLACEMENT_3D ( 'NONE', #51339, #62226, #56249 ) ;
#46228=MECHANICAL_DESIGN_GEOMETRIC_PRESENTATION_REPRESENTATION('',(#5740),#50716);
#46229=ORIENTED_EDGE ( 'NONE', *, *, #6581, .F. ) ;
#46237=VERTEX_POINT ( 'NONE', #1025 ) ;
#46261=EDGE_CURVE ( 'NONE', #45002, #65761, #40857, .T. ) ;
#46263=FACE_OUTER_BOUND ( 'NONE', #11229, .T. ) ;
#46270=EDGE_CURVE ( 'NONE', #60715, #11384, #24288, .T. ) ;
#46275=ADVANCED_FACE ( 'NONE', ( #24985, #51377 ), #56999, .F. ) ;
#46279=EDGE_CURVE ( 'NONE', #56560, #60715, #52782, .T. ) ;
#46289=CARTESIAN_POINT ( 'NONE',  ( 92.41620014002536720, 5.000000000000000000, -29.00402776293825724 ) ) ;
#46290=DIRECTION ( 'NONE',  ( -1.000000000000000000, -0.000000000000000000, -4.516179008354028246E-16 ) ) ;
#46291=ORIENTED_EDGE ( 'NONE', *, *, #7085, .F. ) ;
#46293=SURFACE_STYLE_USAGE ( .BOTH. , #68074 ) ;
#46299=( NAMED_UNIT ( * ) PLANE_ANGLE_UNIT ( ) SI_UNIT ( $, .RADIAN. ) );
#46300=ORIENTED_EDGE ( 'NONE', *, *, #63113, .F. ) ;
#46304=MECHANICAL_DESIGN_GEOMETRIC_PRESENTATION_REPRESENTATION('',(#61970),#39575);
#46312=VERTEX_POINT ( 'NONE', #15845 ) ;
#46336=VECTOR ( 'NONE', #36564, 1000.000000000000114 ) ;
#46340=( LENGTH_UNIT ( ) NAMED_UNIT ( * ) SI_UNIT ( .MILLI., .METRE. ) );
#46346=EDGE_CURVE ( 'NONE', #5288, #11604, #43007, .T. ) ;
#46358=CARTESIAN_POINT ( 'NONE',  ( 57.00000000000000000, 16.00000000000000000, -60.00402776293825724 ) ) ;
#46361=VECTOR ( 'NONE', #2435, 1000.000000000000000 ) ;
#46365=SURFACE_STYLE_FILL_AREA ( #51598 ) ;
#46366=DIRECTION ( 'NONE',  ( 0.000000000000000000, 0.000000000000000000, 1.000000000000000000 ) ) ;
#46371=COLOUR_RGB ( '', 0.72549020, 0.75294118, 0.79215686) ;
#46375=( NAMED_UNIT ( * ) PLANE_ANGLE_UNIT ( ) SI_UNIT ( $, .RADIAN. ) );
#46378=ORIENTED_EDGE ( 'NONE', *, *, #45130, .T. ) ;
#46380=( NAMED_UNIT ( * ) PLANE_ANGLE_UNIT ( ) SI_UNIT ( $, .RADIAN. ) );
#46389=MECHANICAL_DESIGN_GEOMETRIC_PRESENTATION_REPRESENTATION('',(#36310),#17161);
#46401=VERTEX_POINT ( 'NONE', #929 ) ;
#46403=LINE ( 'NONE', #67827, #7986 ) ;
#46436=SURFACE_SIDE_STYLE ('',( #56944 ) ) ;
#46438=PRESENTATION_STYLE_ASSIGNMENT (( #62899 ) ) ;
#46448=FILL_AREA_STYLE ('',( #61509 ) ) ;
#46454=EDGE_CURVE ( 'NONE', #4175, #4230, #9282, .T. ) ;
#46457=DIRECTION ( 'NONE',  ( 0.000000000000000000, 0.000000000000000000, 1.000000000000000000 ) ) ;
#46458=PRESENTATION_STYLE_ASSIGNMENT (( #20007 ) ) ;
#46459=EDGE_LOOP ( 'NONE', ( #45802, #26532, #3834, #25656 ) ) ;
#46460=CIRCLE ( 'NONE', #1421, 1.000000000000000888 ) ;
#46463=CARTESIAN_POINT ( 'NONE',  ( 22.00000000000001776, 43.00000000000000000, 45.61250543006183022 ) ) ;
#46470=ORIENTED_EDGE ( 'NONE', *, *, #9661, .T. ) ;
#46493=( GEOMETRIC_REPRESENTATION_CONTEXT ( 3 ) GLOBAL_UNCERTAINTY_ASSIGNED_CONTEXT ( ( #60949 ) ) GLOBAL_UNIT_ASSIGNED_CONTEXT ( ( #6648, #67146, #28803 ) ) REPRESENTATION_CONTEXT ( 'NONE', 'WORKASPACE' ) );
#46494=FILL_AREA_STYLE_COLOUR ( '', #19402 ) ;
#46500=CARTESIAN_POINT ( 'NONE',  ( 36.00000000000002842, 5.000000000000000000, 77.00402776293825013 ) ) ;
#46501=CARTESIAN_POINT ( 'NONE',  ( 107.0858988931383777, 0.000000000000000000, -16.89933289725613363 ) ) ;
#46503=ORIENTED_EDGE ( 'NONE', *, *, #46911, .T. ) ;
#46507=ADVANCED_FACE ( 'NONE', ( #55160 ), #59762, .F. ) ;
#46515=DIRECTION ( 'NONE',  ( 0.000000000000000000, 0.000000000000000000, -1.000000000000000000 ) ) ;
#46516=ADVANCED_FACE ( 'NONE', ( #56555 ), #18596, .F. ) ;
#46517=AXIS2_PLACEMENT_3D ( 'NONE', #18749, #25071, #62359 ) ;
#46519=EDGE_LOOP ( 'NONE', ( #68607, #55437, #59766, #48186 ) ) ;
#46526=COLOUR_RGB ( '', 0.40784314, 0.44705882, 0.49803922) ;
#46538=AXIS2_PLACEMENT_3D ( 'NONE', #28334, #28693, #11837 ) ;
#46551=ORIENTED_EDGE ( 'NONE', *, *, #8191, .T. ) ;
#46552=DIRECTION ( 'NONE',  ( 0.000000000000000000, 0.000000000000000000, -1.000000000000000000 ) ) ;
#46558=COLOUR_RGB ( '', 0.40784314, 0.44705882, 0.49803922) ;
#46583=EDGE_CURVE ( 'NONE', #20391, #31566, #4836, .T. ) ;
#46585=ORIENTED_EDGE ( 'NONE', *, *, #25336, .T. ) ;
#46590=ORIENTED_EDGE ( 'NONE', *, *, #30020, .T. ) ;
#46597=SURFACE_STYLE_FILL_AREA ( #24375 ) ;
#46602=FACE_OUTER_BOUND ( 'NONE', #61557, .T. ) ;
#46608=PRESENTATION_STYLE_ASSIGNMENT (( #57095 ) ) ;
#46615=ORIENTED_EDGE ( 'NONE', *, *, #60975, .T. ) ;
#46629=SURFACE_SIDE_STYLE ('',( #66649 ) ) ;
#46632=CYLINDRICAL_SURFACE ( 'NONE', #64589, 1.000000000000000888 ) ;
#46644=DIRECTION ( 'NONE',  ( -1.000000000000000000, 0.000000000000000000, 6.938893903907222067E-15 ) ) ;
#46646=FILL_AREA_STYLE_COLOUR ( '', #29252 ) ;
#46650=DIRECTION ( 'NONE',  ( 0.000000000000000000, 0.000000000000000000, -1.000000000000000000 ) ) ;
#46659=DIRECTION ( 'NONE',  ( 1.000000000000000000, 0.000000000000000000, -0.000000000000000000 ) ) ;
#46674=FILL_AREA_STYLE_COLOUR ( '', #36765 ) ;
#46679=DIRECTION ( 'NONE',  ( 0.000000000000000000, 0.000000000000000000, -1.000000000000000000 ) ) ;
#46688=FACE_OUTER_BOUND ( 'NONE', #21250, .T. ) ;
#46698=ORIENTED_EDGE ( 'NONE', *, *, #21912, .F. ) ;
#46699=DIRECTION ( 'NONE',  ( 0.000000000000000000, 0.000000000000000000, -1.000000000000000000 ) ) ;
#46717=DIRECTION ( 'NONE',  ( -1.000000000000000000, 0.000000000000000000, 0.000000000000000000 ) ) ;
#46718=( GEOMETRIC_REPRESENTATION_CONTEXT ( 3 ) GLOBAL_UNCERTAINTY_ASSIGNED_CONTEXT ( ( #32628 ) ) GLOBAL_UNIT_ASSIGNED_CONTEXT ( ( #1515, #12814, #43833 ) ) REPRESENTATION_CONTEXT ( 'NONE', 'WORKASPACE' ) );
#46721=DIRECTION ( 'NONE',  ( -0.000000000000000000, -0.3420201433256629953, 0.9396926207859104263 ) ) ;
#46722=VECTOR ( 'NONE', #31921, 1000.000000000000000 ) ;
#46723=DIRECTION ( 'NONE',  ( 0.000000000000000000, 1.000000000000000000, 0.000000000000000000 ) ) ;
#46724=UNCERTAINTY_MEASURE_WITH_UNIT (LENGTH_MEASURE( 1.000000000000000082E-05 ), #25445, 'distance_accuracy_value', 'NONE');
#46727=FILL_AREA_STYLE_COLOUR ( '', #48347 ) ;
#46728=( NAMED_UNIT ( * ) SI_UNIT ( $, .STERADIAN. ) SOLID_ANGLE_UNIT ( ) );
#46735=EDGE_LOOP ( 'NONE', ( #12449, #57081, #19929, #52194 ) ) ;
#46736=DIRECTION ( 'NONE',  ( 0.000000000000000000, 0.000000000000000000, 1.000000000000000000 ) ) ;
#46743=ORIENTED_EDGE ( 'NONE', *, *, #33304, .F. ) ;
#46748=DIRECTION ( 'NONE',  ( 1.084202172485504434E-16, 0.000000000000000000, 1.000000000000000000 ) ) ;
#46749=PRESENTATION_STYLE_ASSIGNMENT (( #68160 ) ) ;
#46751=FILL_AREA_STYLE ('',( #8381 ) ) ;
#46755=LINE ( 'NONE', #41445, #68119 ) ;
#46756=( LENGTH_UNIT ( ) NAMED_UNIT ( * ) SI_UNIT ( .MILLI., .METRE. ) );
#46760=CARTESIAN_POINT ( 'NONE',  ( 10.00000000000001776, 42.00000000000000000, 28.38386403503541899 ) ) ;
#46762=CYLINDRICAL_SURFACE ( 'NONE', #16602, 14.00000000000000533 ) ;
#46763=ORIENTED_EDGE ( 'NONE', *, *, #60947, .T. ) ;
#46766=CARTESIAN_POINT ( 'NONE',  ( 29.00000000000002842, 42.58578643762690774, 80.00402776293826435 ) ) ;
#46767=VECTOR ( 'NONE', #15332, 1000.000000000000000 ) ;
#46775=( BOUNDED_CURVE ( )  B_SPLINE_CURVE ( 3, ( #22260, #41410, #54259, #48342 ),
 .UNSPECIFIED., .F., .F. ) 
 B_SPLINE_CURVE_WITH_KNOTS ( ( 4, 4 ),
 ( 4.712388980384689674, 6.283185307179586232 ),
 .UNSPECIFIED. ) 
 CURVE ( )  GEOMETRIC_REPRESENTATION_ITEM ( )  RATIONAL_B_SPLINE_CURVE ( ( 1.000000000000000000, 0.8047378541243649375, 0.8047378541243649375, 1.000000000000000000 ) ) 
 REPRESENTATION_ITEM ( '' )  );
#46776=CARTESIAN_POINT ( 'NONE',  ( 10.00000000000001954, 42.00000000000000000, 28.38386403503541899 ) ) ;
#46779=EDGE_CURVE ( 'NONE', #1044, #49461, #9328, .T. ) ;
#46780=DIRECTION ( 'NONE',  ( 0.000000000000000000, -1.000000000000000000, 0.000000000000000000 ) ) ;
#46784=DIRECTION ( 'NONE',  ( -0.000000000000000000, -1.000000000000000000, -0.000000000000000000 ) ) ;
#46792=FILL_AREA_STYLE_COLOUR ( '', #67251 ) ;
#46799=DIRECTION ( 'NONE',  ( 0.000000000000000000, 0.000000000000000000, -1.000000000000000000 ) ) ;
#46809=CARTESIAN_POINT ( 'NONE',  ( 31.00000000000000000, 14.00000000000000000, -79.00402776293826435 ) ) ;
#46821=AXIS2_PLACEMENT_3D ( 'NONE', #62516, #8717, #42176 ) ;
#46829=( NAMED_UNIT ( * ) SI_UNIT ( $, .STERADIAN. ) SOLID_ANGLE_UNIT ( ) );
#46835=AXIS2_PLACEMENT_3D ( 'NONE', #62155, #45686, #67105 ) ;
#46843=FILL_AREA_STYLE ('',( #67194 ) ) ;
#46845=DIRECTION ( 'NONE',  ( 0.000000000000000000, -1.000000000000000000, 0.000000000000000000 ) ) ;
#46848=CARTESIAN_POINT ( 'NONE',  ( 26.00000000000001776, 15.00000000000000000, 34.49999999999999289 ) ) ;
#46854=DIRECTION ( 'NONE',  ( 0.000000000000000000, -1.000000000000000000, 0.000000000000000000 ) ) ;
#46857=CARTESIAN_POINT ( 'NONE',  ( 29.00000000000002842, 35.42594141563417054, 80.00402776293826435 ) ) ;
#46864=ORIENTED_EDGE ( 'NONE', *, *, #39346, .F. ) ;
#46866=UNCERTAINTY_MEASURE_WITH_UNIT (LENGTH_MEASURE( 1.000000000000000082E-05 ), #43961, 'distance_accuracy_value', 'NONE');
#46867=CARTESIAN_POINT ( 'NONE',  ( 22.00000000000002132, 50.00000000000000000, 60.00000000000000711 ) ) ;
#46872=VERTEX_POINT ( 'NONE', #8909 ) ;
#46873=ORIENTED_EDGE ( 'NONE', *, *, #11292, .T. ) ;
#46874=CARTESIAN_POINT ( 'NONE',  ( 22.49933229817787605, 26.84000769619876436, 27.39862673134610205 ) ) ;
#46878=SURFACE_SIDE_STYLE ('',( #4215 ) ) ;
#46883=ORIENTED_EDGE ( 'NONE', *, *, #38499, .F. ) ;
#46886=PRESENTATION_STYLE_ASSIGNMENT (( #41573 ) ) ;
#46888=MECHANICAL_DESIGN_GEOMETRIC_PRESENTATION_REPRESENTATION('',(#24324),#2932);
#46891=LINE ( 'NONE', #68294, #17958 ) ;
#46894=DIRECTION ( 'NONE',  ( 0.000000000000000000, 0.000000000000000000, -1.000000000000000000 ) ) ;
#46901=FACE_OUTER_BOUND ( 'NONE', #16382, .T. ) ;
#46903=( LENGTH_UNIT ( ) NAMED_UNIT ( * ) SI_UNIT ( .MILLI., .METRE. ) );
#46911=EDGE_CURVE ( 'NONE', #62752, #28347, #38632, .T. ) ;
#46912=ADVANCED_FACE ( 'NONE', ( #41296 ), #35301, .T. ) ;
#46916=( NAMED_UNIT ( * ) PLANE_ANGLE_UNIT ( ) SI_UNIT ( $, .RADIAN. ) );
#46920=CARTESIAN_POINT ( 'NONE',  ( 8.000000000000030198, 0.000000000000000000, 29.00402776293826079 ) ) ;
#46922=ADVANCED_FACE ( 'NONE', ( #2883 ), #34944, .F. ) ;
#46931=DIRECTION ( 'NONE',  ( -0.000000000000000000, -0.6449798928094537809, 0.7641995406119435064 ) ) ;
#46933=ORIENTED_EDGE ( 'NONE', *, *, #66055, .F. ) ;
#46941=CARTESIAN_POINT ( 'NONE',  ( 22.99999999999998934, 5.000000000000000000, 37.00402776293825724 ) ) ;
#46944=LINE ( 'NONE', #68351, #34376 ) ;
#46959=SURFACE_SIDE_STYLE ('',( #30706 ) ) ;
#46972=SURFACE_STYLE_USAGE ( .BOTH. , #52572 ) ;
#46975=CARTESIAN_POINT ( 'NONE',  ( 57.00000000000000000, 13.00000000000000178, -60.00402776293827145 ) ) ;
#46988=DIRECTION ( 'NONE',  ( 1.000000000000000000, 0.000000000000000000, -1.300977106640435137E-16 ) ) ;
#46991=VERTEX_POINT ( 'NONE', #58484 ) ;
#46995=CIRCLE ( 'NONE', #36844, 16.00000000000000711 ) ;
#46998=UNCERTAINTY_MEASURE_WITH_UNIT (LENGTH_MEASURE( 1.000000000000000082E-05 ), #45069, 'distance_accuracy_value', 'NONE');
#47011=CARTESIAN_POINT ( 'NONE',  ( 6.000000000000015099, 17.23130743308432855, -3.144186300207962859E-15 ) ) ;
#47012=DIRECTION ( 'NONE',  ( 1.000000000000000000, -0.000000000000000000, -1.300977106640434891E-16 ) ) ;
#47021=SURFACE_STYLE_FILL_AREA ( #8656 ) ;
#47029=DIRECTION ( 'NONE',  ( 1.000000000000000000, 0.000000000000000000, 0.000000000000000000 ) ) ;
#47041=AXIS2_PLACEMENT_3D ( 'NONE', #18910, #40409, #61819 ) ;
#47050=EDGE_CURVE ( 'NONE', #35442, #5819, #13883, .T. ) ;
#47063=EDGE_CURVE ( 'NONE', #37678, #41012, #22233, .T. ) ;
#47064=CARTESIAN_POINT ( 'NONE',  ( 31.00000000000000711, 42.00000000000000000, -36.50000000000000000 ) ) ;
#47065=EDGE_CURVE ( 'NONE', #60615, #43704, #22586, .T. ) ;
#47073=ORIENTED_EDGE ( 'NONE', *, *, #7388, .T. ) ;
#47075=LINE ( 'NONE', #36536, #9696 ) ;
#47087=( GEOMETRIC_REPRESENTATION_CONTEXT ( 3 ) GLOBAL_UNCERTAINTY_ASSIGNED_CONTEXT ( ( #67778 ) ) GLOBAL_UNIT_ASSIGNED_CONTEXT ( ( #21918, #27836, #38486 ) ) REPRESENTATION_CONTEXT ( 'NONE', 'WORKASPACE' ) );
#47116=( NAMED_UNIT ( * ) SI_UNIT ( $, .STERADIAN. ) SOLID_ANGLE_UNIT ( ) );
#47123=( NAMED_UNIT ( * ) SI_UNIT ( $, .STERADIAN. ) SOLID_ANGLE_UNIT ( ) );
#47147=FILL_AREA_STYLE ('',( #9493 ) ) ;
#47161=FACE_OUTER_BOUND ( 'NONE', #30805, .T. ) ;
#47162=ORIENTED_EDGE ( 'NONE', *, *, #19838, .T. ) ;
#47165=SURFACE_STYLE_USAGE ( .BOTH. , #63642 ) ;
#47172=DIRECTION ( 'NONE',  ( 0.000000000000000000, 0.000000000000000000, -1.000000000000000000 ) ) ;
#47177=CARTESIAN_POINT ( 'NONE',  ( 31.00000000000000000, 43.00000000000000000, -75.00000000000001421 ) ) ;
#47178=AXIS2_PLACEMENT_3D ( 'NONE', #44873, #30714, #57113 ) ;
#47193=CARTESIAN_POINT ( 'NONE',  ( 8.000000000000030198, 5.000000000000000000, -29.00402776293826079 ) ) ;
#47202=ORIENTED_EDGE ( 'NONE', *, *, #32971, .F. ) ;
#47204=ORIENTED_EDGE ( 'NONE', *, *, #44364, .T. ) ;
#47209=DIRECTION ( 'NONE',  ( 0.000000000000000000, 1.000000000000000000, 0.000000000000000000 ) ) ;
#47216=LINE ( 'NONE', #64032, #18055 ) ;
#47224=DIRECTION ( 'NONE',  ( 0.000000000000000000, 0.000000000000000000, -1.000000000000000000 ) ) ;
#47229=EDGE_LOOP ( 'NONE', ( #1850, #13477, #60429, #1412 ) ) ;
#47237=CARTESIAN_POINT ( 'NONE',  ( 179.4361977533490347, 13.00000000000000178, -103.7004518695263044 ) ) ;
#47238=STYLED_ITEM ( 'NONE', ( #15526 ), #11186 ) ;
#47240=PRESENTATION_STYLE_ASSIGNMENT (( #42914 ) ) ;
#47250=ORIENTED_EDGE ( 'NONE', *, *, #40763, .T. ) ;
#47258=DIRECTION ( 'NONE',  ( -0.000000000000000000, -1.000000000000000000, -0.000000000000000000 ) ) ;
#47287=FACE_OUTER_BOUND ( 'NONE', #7512, .T. ) ;
#47291=CARTESIAN_POINT ( 'NONE',  ( 7.999999999999989342, 5.000000000000000000, 37.00402776293825724 ) ) ;
#47297=ORIENTED_EDGE ( 'NONE', *, *, #4270, .F. ) ;
#47304=EDGE_CURVE ( 'NONE', #42967, #12357, #31298, .T. ) ;
#47305=( LENGTH_UNIT ( ) NAMED_UNIT ( * ) SI_UNIT ( .MILLI., .METRE. ) );
#47314=ORIENTED_EDGE ( 'NONE', *, *, #8626, .F. ) ;
#47316=CARTESIAN_POINT ( 'NONE',  ( 33.00000000000000000, 15.00000000000000000, -80.00402776293826435 ) ) ;
#47319=EDGE_CURVE ( 'NONE', #26109, #50403, #5879, .T. ) ;
#47328=CYLINDRICAL_SURFACE ( 'NONE', #8938, 110.0000000000000142 ) ;
#47329=TOROIDAL_SURFACE ( 'NONE', #19191, 4.000000000000000000, 1.000000000000000000 ) ;
#47331=ORIENTED_EDGE ( 'NONE', *, *, #2402, .F. ) ;
#47341=CARTESIAN_POINT ( 'NONE',  ( 82.09357085539578236, 5.000000000000000000, 32.00402776293825724 ) ) ;
#47344=PRESENTATION_STYLE_ASSIGNMENT (( #25831 ) ) ;
#47348=STYLED_ITEM ( 'NONE', ( #34748 ), #17817 ) ;
#47352=ORIENTED_EDGE ( 'NONE', *, *, #12836, .T. ) ;
#47361=FILL_AREA_STYLE_COLOUR ( '', #12303 ) ;
#47376=ORIENTED_EDGE ( 'NONE', *, *, #42705, .F. ) ;
#47383=ADVANCED_FACE ( 'NONE', ( #42605 ), #36294, .F. ) ;
#47387=MECHANICAL_DESIGN_GEOMETRIC_PRESENTATION_REPRESENTATION('',(#24872),#15940);
#47391=ORIENTED_EDGE ( 'NONE', *, *, #19114, .T. ) ;
#47395=UNCERTAINTY_MEASURE_WITH_UNIT (LENGTH_MEASURE( 1.000000000000000082E-05 ), #51445, 'distance_accuracy_value', 'NONE');
#47402=COLOUR_RGB ( '', 0.08235294, 0.09019608, 0.10196078) ;
#47405=UNCERTAINTY_MEASURE_WITH_UNIT (LENGTH_MEASURE( 1.000000000000000082E-05 ), #61763, 'distance_accuracy_value', 'NONE');
#47407=SURFACE_SIDE_STYLE ('',( #25887 ) ) ;
#47417=ORIENTED_EDGE ( 'NONE', *, *, #29359, .F. ) ;
#47418=VERTEX_POINT ( 'NONE', #7006 ) ;
#47429=ORIENTED_EDGE ( 'NONE', *, *, #18682, .F. ) ;
#47431=CARTESIAN_POINT ( 'NONE',  ( 57.00000000000000000, 14.00000000000000000, -60.00402776293827145 ) ) ;
#47437=COLOUR_RGB ( '', 0.09019608, 0.27058824, 0.51372549) ;
#47438=FACE_OUTER_BOUND ( 'NONE', #25756, .T. ) ;
#47442=PLANE ( 'NONE',  #46821 ) ;
#47450=CARTESIAN_POINT ( 'NONE',  ( 31.00000000000000711, 14.00000000000000000, -36.50000000000000000 ) ) ;
#47451=VECTOR ( 'NONE', #46780, 1000.000000000000000 ) ;
#47469=LINE ( 'NONE', #52018, #11537 ) ;
#47477=AXIS2_PLACEMENT_3D ( 'NONE', #28031, #23469, #66037 ) ;
#47484=CARTESIAN_POINT ( 'NONE',  ( 16.00000000000001776, 14.00000000000000000, 29.68999999999999417 ) ) ;
#47498=UNCERTAINTY_MEASURE_WITH_UNIT (LENGTH_MEASURE( 1.000000000000000082E-05 ), #59921, 'distance_accuracy_value', 'NONE');
#47503=SURFACE_SIDE_STYLE ('',( #25297 ) ) ;
#47514=DIRECTION ( 'NONE',  ( 1.000000000000000000, -0.000000000000000000, -1.300977106640434891E-16 ) ) ;
#47516=STYLED_ITEM ( 'NONE', ( #35297 ), #24383 ) ;
#47518=SURFACE_STYLE_FILL_AREA ( #52070 ) ;
#47519=ORIENTED_EDGE ( 'NONE', *, *, #51801, .T. ) ;
#47522=DIRECTION ( 'NONE',  ( 0.000000000000000000, -1.000000000000000000, 0.000000000000000000 ) ) ;
#47524=EDGE_LOOP ( 'NONE', ( #46300, #13611, #64384, #59910 ) ) ;
#47525=SURFACE_SIDE_STYLE ('',( #63304 ) ) ;
#47540=UNCERTAINTY_MEASURE_WITH_UNIT (LENGTH_MEASURE( 1.000000000000000082E-05 ), #52883, 'distance_accuracy_value', 'NONE');
#47557=UNCERTAINTY_MEASURE_WITH_UNIT (LENGTH_MEASURE( 1.000000000000000082E-05 ), #60289, 'distance_accuracy_value', 'NONE');
#47560=EDGE_CURVE ( 'NONE', #36332, #53365, #53164, .T. ) ;
#47561=( LENGTH_UNIT ( ) NAMED_UNIT ( * ) SI_UNIT ( .MILLI., .METRE. ) );
#47568=CARTESIAN_POINT ( 'NONE',  ( 22.31821212674813637, 25.64654866474386807, 27.48625202223684383 ) ) ;
#47600=DIRECTION ( 'NONE',  ( 1.000000000000000000, 0.000000000000000000, -1.300977106640434891E-16 ) ) ;
#47601=COLOUR_RGB ( '', 0.09019608, 0.27058824, 0.51372549) ;
#47605=EDGE_LOOP ( 'NONE', ( #64769, #68934, #30648, #56577 ) ) ;
#47607=VECTOR ( 'NONE', #14801, 1000.000000000000000 ) ;
#47611=AXIS2_PLACEMENT_3D ( 'NONE', #68334, #15248, #42344 ) ;
#47623=VERTEX_POINT ( 'NONE', #55882 ) ;
#47636=VERTEX_POINT ( 'NONE', #29120 ) ;
#47645=AXIS2_PLACEMENT_3D ( 'NONE', #7835, #67632, #19069 ) ;
#47648=DIRECTION ( 'NONE',  ( 0.000000000000000000, 0.000000000000000000, -1.000000000000000000 ) ) ;
#47651=SURFACE_STYLE_USAGE ( .BOTH. , #63423 ) ;
#47655=FACE_BOUND ( 'NONE', #66439, .T. ) ;
#47659=CIRCLE ( 'NONE', #39735, 1.000000000000000888 ) ;
#47660=( LENGTH_UNIT ( ) NAMED_UNIT ( * ) SI_UNIT ( .MILLI., .METRE. ) );
#47688=ORIENTED_EDGE ( 'NONE', *, *, #56549, .T. ) ;
#47692=SURFACE_STYLE_FILL_AREA ( #52915 ) ;
#47696=SURFACE_STYLE_FILL_AREA ( #41692 ) ;
#47700=FILL_AREA_STYLE ('',( #26162 ) ) ;
#47714=ORIENTED_EDGE ( 'NONE', *, *, #63261, .T. ) ;
#47734=DIRECTION ( 'NONE',  ( 0.000000000000000000, 0.000000000000000000, -1.000000000000000000 ) ) ;
#47738=DIRECTION ( 'NONE',  ( -1.000000000000000000, -0.000000000000000000, 1.300977106640435137E-16 ) ) ;
#47739=ORIENTED_EDGE ( 'NONE', *, *, #25110, .F. ) ;
#47762=ORIENTED_EDGE ( 'NONE', *, *, #31656, .F. ) ;
#47782=SURFACE_STYLE_FILL_AREA ( #10092 ) ;
#47785=EDGE_CURVE ( 'NONE', #48506, #15864, #33648, .T. ) ;
#47787=CARTESIAN_POINT ( 'NONE',  ( 22.29422224269976027, 25.82156383787605236, -27.50000000000000711 ) ) ;
#47792=CARTESIAN_POINT ( 'NONE',  ( 29.00000000000000000, 42.58578643762690774, -89.58578643762690774 ) ) ;
#47796=SURFACE_SIDE_STYLE ('',( #26261 ) ) ;
#47801=CARTESIAN_POINT ( 'NONE',  ( 98.00000000000000000, 0.000000000000000000, 0.000000000000000000 ) ) ;
#47804=AXIS2_PLACEMENT_3D ( 'NONE', #50760, #34563, #56364 ) ;
#47807=EDGE_CURVE ( 'NONE', #67697, #43704, #16124, .T. ) ;
#47811=( NAMED_UNIT ( * ) SI_UNIT ( $, .STERADIAN. ) SOLID_ANGLE_UNIT ( ) );
#47820=SURFACE_STYLE_USAGE ( .BOTH. , #27304 ) ;
#47822=CIRCLE ( 'NONE', #56757, 5.000000000000004441 ) ;
#47823=CIRCLE ( 'NONE', #14070, 1.000000000000000888 ) ;
#47825=LINE ( 'NONE', #28252, #38473 ) ;
#47827=DIRECTION ( 'NONE',  ( 0.000000000000000000, 1.000000000000000000, -0.000000000000000000 ) ) ;
#47829=ORIENTED_EDGE ( 'NONE', *, *, #48423, .T. ) ;
#47846=ORIENTED_EDGE ( 'NONE', *, *, #41997, .F. ) ;
#47847=DIRECTION ( 'NONE',  ( 0.000000000000000000, -1.000000000000000000, 0.000000000000000000 ) ) ;
#47850=DIRECTION ( 'NONE',  ( 0.000000000000000000, 1.000000000000000000, 0.000000000000000000 ) ) ;
#47859=CARTESIAN_POINT ( 'NONE',  ( 16.00000000000001776, 15.00000000000000000, -29.68999999999999417 ) ) ;
#47866=DIRECTION ( 'NONE',  ( -1.000000000000000000, -0.000000000000000000, -4.516179008354028246E-16 ) ) ;
#47873=( GEOMETRIC_REPRESENTATION_CONTEXT ( 3 ) GLOBAL_UNCERTAINTY_ASSIGNED_CONTEXT ( ( #8141 ) ) GLOBAL_UNIT_ASSIGNED_CONTEXT ( ( #54065, #48847, #6552 ) ) REPRESENTATION_CONTEXT ( 'NONE', 'WORKASPACE' ) );
#47875=SURFACE_SIDE_STYLE ('',( #64321 ) ) ;
#47876=DIRECTION ( 'NONE',  ( -0.000000000000000000, -1.000000000000000000, 0.000000000000000000 ) ) ;
#47889=CARTESIAN_POINT ( 'NONE',  ( 22.99999999999999645, 5.000000000000000000, 24.00402776293825013 ) ) ;
#47890=ORIENTED_EDGE ( 'NONE', *, *, #18006, .F. ) ;
#47895=ORIENTED_EDGE ( 'NONE', *, *, #20983, .T. ) ;
#47899=( LENGTH_UNIT ( ) NAMED_UNIT ( * ) SI_UNIT ( .MILLI., .METRE. ) );
#47900=CIRCLE ( 'NONE', #15286, 5.999999999999998224 ) ;
#47905=ORIENTED_EDGE ( 'NONE', *, *, #52517, .F. ) ;
#47912=DIRECTION ( 'NONE',  ( 0.000000000000000000, -0.6691306063588591257, 0.7431448254773933559 ) ) ;
#47913=CYLINDRICAL_SURFACE ( 'NONE', #24706, 16.00000000000000711 ) ;
#47916=ORIENTED_EDGE ( 'NONE', *, *, #1203, .T. ) ;
#47923=SURFACE_STYLE_USAGE ( .BOTH. , #16572 ) ;
#47938=MECHANICAL_DESIGN_GEOMETRIC_PRESENTATION_REPRESENTATION('',(#29892),#65856);
#47952=STYLED_ITEM ( 'NONE', ( #40232 ), #57571 ) ;
#47957=ORIENTED_EDGE ( 'NONE', *, *, #31696, .F. ) ;
#47959=EDGE_CURVE ( 'NONE', #7763, #37266, #46460, .T. ) ;
#47964=ORIENTED_EDGE ( 'NONE', *, *, #7469, .F. ) ;
#47965=( LENGTH_UNIT ( ) NAMED_UNIT ( * ) SI_UNIT ( .MILLI., .METRE. ) );
#47967=LINE ( 'NONE', #65097, #63460 ) ;
#47969=DIRECTION ( 'NONE',  ( 0.000000000000000000, 0.000000000000000000, 1.000000000000000000 ) ) ;
#47976=LINE ( 'NONE', #64783, #58796 ) ;
#47979=CARTESIAN_POINT ( 'NONE',  ( 35.99999999999999289, 0.000000000000000000, 32.00402776293825724 ) ) ;
#47984=ORIENTED_EDGE ( 'NONE', *, *, #27021, .T. ) ;
#47988=CARTESIAN_POINT ( 'NONE',  ( 21.00000000000001776, -3.148064030671221758, 29.68999999999999417 ) ) ;
#47992=( BOUNDED_CURVE ( )  B_SPLINE_CURVE ( 3, ( #17258, #28075, #61160, #2350 ),
 .UNSPECIFIED., .F., .F. ) 
 B_SPLINE_CURVE_WITH_KNOTS ( ( 4, 4 ),
 ( 1.570796326794891451, 3.141592653589793116 ),
 .UNSPECIFIED. ) 
 CURVE ( )  GEOMETRIC_REPRESENTATION_ITEM ( )  RATIONAL_B_SPLINE_CURVE ( ( 1.000000000000000000, 0.8047378541243637162, 0.8047378541243637162, 1.000000000000000000 ) ) 
 REPRESENTATION_ITEM ( '' )  );
#47998=ORIENTED_EDGE ( 'NONE', *, *, #50645, .T. ) ;
#47999=SURFACE_SIDE_STYLE ('',( #52201 ) ) ;
#48004=ORIENTED_EDGE ( 'NONE', *, *, #19634, .T. ) ;
#48007=AXIS2_PLACEMENT_3D ( 'NONE', #59924, #16369, #54973 ) ;
#48013=CARTESIAN_POINT ( 'NONE',  ( 10.00000000000000178, 60.69879356856722552, -69.02971849933236115 ) ) ;
#48033=FACE_OUTER_BOUND ( 'NONE', #1378, .T. ) ;
#48038=( NAMED_UNIT ( * ) SI_UNIT ( $, .STERADIAN. ) SOLID_ANGLE_UNIT ( ) );
#48047=CARTESIAN_POINT ( 'NONE',  ( 23.50000000000001776, 15.00000000000000000, 26.18999999999999417 ) ) ;
#48049=CARTESIAN_POINT ( 'NONE',  ( 27.00000000000001776, -3.148064030671221758, -34.49999999999999289 ) ) ;
#48050=VERTEX_POINT ( 'NONE', #27002 ) ;
#48058=VECTOR ( 'NONE', #1219, 1000.000000000000000 ) ;
#48060=SURFACE_STYLE_FILL_AREA ( #11055 ) ;
#48061=CARTESIAN_POINT ( 'NONE',  ( 10.00000000000001954, 43.00000000000000000, 45.61250543006183733 ) ) ;
#48064=ORIENTED_EDGE ( 'NONE', *, *, #52479, .T. ) ;
#48075=SURFACE_STYLE_FILL_AREA ( #54332 ) ;
#48105=ORIENTED_EDGE ( 'NONE', *, *, #58608, .T. ) ;
#48113=ORIENTED_EDGE ( 'NONE', *, *, #38412, .F. ) ;
#48116=MECHANICAL_DESIGN_GEOMETRIC_PRESENTATION_REPRESENTATION('',(#3076),#51439);
#48122=DIRECTION ( 'NONE',  ( -0.000000000000000000, 1.000000000000000000, -0.000000000000000000 ) ) ;
#48138=PRESENTATION_STYLE_ASSIGNMENT (( #47820 ) ) ;
#48139=DIRECTION ( 'NONE',  ( -0.000000000000000000, -1.000000000000000000, 0.000000000000000000 ) ) ;
#48145=( GEOMETRIC_REPRESENTATION_CONTEXT ( 3 ) GLOBAL_UNCERTAINTY_ASSIGNED_CONTEXT ( ( #28278 ) ) GLOBAL_UNIT_ASSIGNED_CONTEXT ( ( #61316, #39560, #2881 ) ) REPRESENTATION_CONTEXT ( 'NONE', 'WORKASPACE' ) );
#48159=CYLINDRICAL_SURFACE ( 'NONE', #16743, 1.000000000000000888 ) ;
#48165=CARTESIAN_POINT ( 'NONE',  ( 23.85059380760285563, 27.39840537729088510, 27.20962804606061880 ) ) ;
#48167=EDGE_CURVE ( 'NONE', #48050, #8636, #66965, .T. ) ;
#48171=SURFACE_SIDE_STYLE ('',( #32996 ) ) ;
#48182=CARTESIAN_POINT ( 'NONE',  ( 22.00000000000000711, 50.00000000000000000, -60.00000000000000711 ) ) ;
#48183=DIRECTION ( 'NONE',  ( 0.000000000000000000, 1.000000000000000000, 0.000000000000000000 ) ) ;
#48186=ORIENTED_EDGE ( 'NONE', *, *, #6342, .T. ) ;
#48208=DIRECTION ( 'NONE',  ( 0.000000000000000000, -1.000000000000000000, 0.000000000000000000 ) ) ;
#48210=ORIENTED_EDGE ( 'NONE', *, *, #60971, .F. ) ;
#48218=DIRECTION ( 'NONE',  ( 1.000000000000000000, 0.000000000000000000, 0.000000000000000000 ) ) ;
#48220=( NAMED_UNIT ( * ) SI_UNIT ( $, .STERADIAN. ) SOLID_ANGLE_UNIT ( ) );
#48224=UNCERTAINTY_MEASURE_WITH_UNIT (LENGTH_MEASURE( 1.000000000000000082E-05 ), #19992, 'distance_accuracy_value', 'NONE');
#48235=CARTESIAN_POINT ( 'NONE',  ( 31.00000000000002132, 43.00000000000000000, 75.00000000000000000 ) ) ;
#48236=DIRECTION ( 'NONE',  ( 0.000000000000000000, -1.000000000000000000, 0.000000000000000000 ) ) ;
#48237=MECHANICAL_DESIGN_GEOMETRIC_PRESENTATION_REPRESENTATION('',(#32412),#9995);
#48246=EDGE_CURVE ( 'NONE', #8864, #51444, #45412, .T. ) ;
#48251=CIRCLE ( 'NONE', #5494, 5.000000000000004441 ) ;
#48252=LINE ( 'NONE', #10251, #58375 ) ;
#48254=UNCERTAINTY_MEASURE_WITH_UNIT (LENGTH_MEASURE( 1.000000000000000082E-05 ), #27628, 'distance_accuracy_value', 'NONE');
#48255=AXIS2_PLACEMENT_3D ( 'NONE', #45888, #3244, #35322 ) ;
#48266=( GEOMETRIC_REPRESENTATION_CONTEXT ( 3 ) GLOBAL_UNCERTAINTY_ASSIGNED_CONTEXT ( ( #13696 ) ) GLOBAL_UNIT_ASSIGNED_CONTEXT ( ( #38964, #44590, #60365 ) ) REPRESENTATION_CONTEXT ( 'NONE', 'WORKASPACE' ) );
#48271=STYLED_ITEM ( 'NONE', ( #44452 ), #43186 ) ;
#48283=COLOUR_RGB ( '', 0.09019608, 0.27058824, 0.51372549) ;
#48288=AXIS2_PLACEMENT_3D ( 'NONE', #2935, #51885, #46650 ) ;
#48295=ORIENTED_EDGE ( 'NONE', *, *, #4758, .T. ) ;
#48298=UNCERTAINTY_MEASURE_WITH_UNIT (LENGTH_MEASURE( 1.000000000000000082E-05 ), #9974, 'distance_accuracy_value', 'NONE');
#48304=MECHANICAL_DESIGN_GEOMETRIC_PRESENTATION_REPRESENTATION('',(#2096),#2131);
#48317=PLANE ( 'NONE',  #2396 ) ;
#48321=ADVANCED_FACE ( 'NONE', ( #23473 ), #13261, .F. ) ;
#48324=MECHANICAL_DESIGN_GEOMETRIC_PRESENTATION_REPRESENTATION('',(#39323),#50496);
#48328=VECTOR ( 'NONE', #58098, 1000.000000000000000 ) ;
#48340=ADVANCED_FACE ( 'NONE', ( #3726 ), #20641, .F. ) ;
#48342=CARTESIAN_POINT ( 'NONE',  ( 28.00000000000002132, 43.00000000000000000, 90.00000000000000000 ) ) ;
#48347=COLOUR_RGB ( '', 0.09019608, 0.27058824, 0.51372549) ;
#48348=ADVANCED_FACE ( 'NONE', ( #53003 ), #26582, .T. ) ;
#48356=AXIS2_PLACEMENT_3D ( 'NONE', #63701, #32726, #10595 ) ;
#48365=VERTEX_POINT ( 'NONE', #827 ) ;
#48377=ORIENTED_EDGE ( 'NONE', *, *, #18285, .T. ) ;
#48379=PRESENTATION_STYLE_ASSIGNMENT (( #53946 ) ) ;
#48382=MECHANICAL_DESIGN_GEOMETRIC_PRESENTATION_REPRESENTATION('',(#14660),#36007);
#48383=CARTESIAN_POINT ( 'NONE',  ( 23.85401998315348493, 27.39726515740571244, -27.21013614952132542 ) ) ;
#48384=AXIS2_PLACEMENT_3D ( 'NONE', #23526, #56226, #29131 ) ;
#48392=COLOUR_RGB ( '', 0.31764706, 0.68627451, 0.89019608) ;
#48399=CARTESIAN_POINT ( 'NONE',  ( 31.53557507391671066, 42.85561104658233944, -45.52242297229209811 ) ) ;
#48414=PRESENTATION_STYLE_ASSIGNMENT (( #5106 ) ) ;
#48423=EDGE_CURVE ( 'NONE', #8149, #26431, #24070, .T. ) ;
#48427=EDGE_LOOP ( 'NONE', ( #6958, #1644, #11402, #41372, #45788, #23552, #59135, #47714, #30094, #39044, #3807, #57251 ) ) ;
#48429=DIRECTION ( 'NONE',  ( -0.000000000000000000, -1.000000000000000000, 0.000000000000000000 ) ) ;
#48430=( GEOMETRIC_REPRESENTATION_CONTEXT ( 3 ) GLOBAL_UNCERTAINTY_ASSIGNED_CONTEXT ( ( #803 ) ) GLOBAL_UNIT_ASSIGNED_CONTEXT ( ( #47965, #9934, #52855 ) ) REPRESENTATION_CONTEXT ( 'NONE', 'WORKASPACE' ) );
#48440=STYLED_ITEM ( 'NONE', ( #44737 ), #34703 ) ;
#48446=MECHANICAL_DESIGN_GEOMETRIC_PRESENTATION_REPRESENTATION('',(#63009),#16995);
#48449=CARTESIAN_POINT ( 'NONE',  ( 16.00000000000001776, 14.00000000000000000, -29.68999999999999417 ) ) ;
#48453=ADVANCED_FACE ( 'NONE', ( #54706, #54366, #5461, #44570 ), #54021, .F. ) ;
#48456=VERTEX_POINT ( 'NONE', #24426 ) ;
#48457=ORIENTED_EDGE ( 'NONE', *, *, #45068, .F. ) ;
#48461=ORIENTED_EDGE ( 'NONE', *, *, #13711, .T. ) ;
#48463=SURFACE_STYLE_FILL_AREA ( #60008 ) ;
#48470=CARTESIAN_POINT ( 'NONE',  ( 22.99999999999999645, 5.000000000000000000, 24.00402776293825013 ) ) ;
#48473=CARTESIAN_POINT ( 'NONE',  ( 32.00000000000000000, 43.00000000000000000, -80.00402776293826435 ) ) ;
#48474=COLOUR_RGB ( '', 0.66274510, 0.83137255, 0.94901961) ;
#48475=DIRECTION ( 'NONE',  ( 0.000000000000000000, 0.000000000000000000, -1.000000000000000000 ) ) ;
#48484=AXIS2_PLACEMENT_3D ( 'NONE', #38526, #21961, #16696 ) ;
#48497=FILL_AREA_STYLE_COLOUR ( '', #56805 ) ;
#48498=ORIENTED_EDGE ( 'NONE', *, *, #30092, .T. ) ;
#48506=VERTEX_POINT ( 'NONE', #13185 ) ;
#48517=FILL_AREA_STYLE ('',( #42906 ) ) ;
#48530=DIRECTION ( 'NONE',  ( -1.000000000000000000, 0.000000000000000000, 0.000000000000000000 ) ) ;
#48532=ORIENTED_EDGE ( 'NONE', *, *, #59955, .T. ) ;
#48549=PRESENTATION_STYLE_ASSIGNMENT (( #54793 ) ) ;
#48551=EDGE_LOOP ( 'NONE', ( #11328, #26669, #32205, #55223 ) ) ;
#48552=CIRCLE ( 'NONE', #18177, 14.00000000000000533 ) ;
#48556=COLOUR_RGB ( '', 0.72549020, 0.75294118, 0.79215686) ;
#48568=ORIENTED_EDGE ( 'NONE', *, *, #48578, .F. ) ;
#48569=DIRECTION ( 'NONE',  ( 0.000000000000000000, 0.000000000000000000, -1.000000000000000000 ) ) ;
#48578=EDGE_CURVE ( 'NONE', #28375, #15308, #20713, .T. ) ;
#48587=DIRECTION ( 'NONE',  ( 1.000000000000000000, 0.000000000000000000, 0.000000000000000000 ) ) ;
#48591=FILL_AREA_STYLE_COLOUR ( '', #31786 ) ;
#48592=( GEOMETRIC_REPRESENTATION_CONTEXT ( 3 ) GLOBAL_UNCERTAINTY_ASSIGNED_CONTEXT ( ( #4016 ) ) GLOBAL_UNIT_ASSIGNED_CONTEXT ( ( #42839, #57226, #53009 ) ) REPRESENTATION_CONTEXT ( 'NONE', 'WORKASPACE' ) );
#48593=DIRECTION ( 'NONE',  ( -0.000000000000000000, -1.000000000000000000, -0.000000000000000000 ) ) ;
#48605=CYLINDRICAL_SURFACE ( 'NONE', #37110, 2.500000000000002220 ) ;
#48624=ORIENTED_EDGE ( 'NONE', *, *, #56526, .F. ) ;
#48626=CARTESIAN_POINT ( 'NONE',  ( 6.000000000000017764, 26.00000000000000355, 23.99999999999999645 ) ) ;
#48631=( NAMED_UNIT ( * ) PLANE_ANGLE_UNIT ( ) SI_UNIT ( $, .RADIAN. ) );
#48632=ORIENTED_EDGE ( 'NONE', *, *, #66567, .F. ) ;
#48634=VERTEX_POINT ( 'NONE', #9686 ) ;
#48638=ORIENTED_EDGE ( 'NONE', *, *, #40871, .T. ) ;
#48639=PRESENTATION_STYLE_ASSIGNMENT (( #32071 ) ) ;
#48645=FILL_AREA_STYLE ('',( #60191 ) ) ;
#48656=SURFACE_STYLE_FILL_AREA ( #65830 ) ;
#48665=ORIENTED_EDGE ( 'NONE', *, *, #14976, .F. ) ;
#48666=CARTESIAN_POINT ( 'NONE',  ( 10.00000000000000355, 43.00000000000000000, -74.38749456993816978 ) ) ;
#48667=STYLED_ITEM ( 'NONE', ( #1772 ), #25963 ) ;
#48672=EDGE_CURVE ( 'NONE', #50329, #11349, #49999, .T. ) ;
#48684=DIRECTION ( 'NONE',  ( 0.000000000000000000, 0.000000000000000000, -1.000000000000000000 ) ) ;
#48692=EDGE_CURVE ( 'NONE', #62763, #69376, #23026, .T. ) ;
#48721=DIRECTION ( 'NONE',  ( 0.000000000000000000, 0.000000000000000000, -1.000000000000000000 ) ) ;
#48722=DIRECTION ( 'NONE',  ( -1.000000000000000000, 0.000000000000000000, 0.000000000000000000 ) ) ;
#48724=AXIS2_PLACEMENT_3D ( 'NONE', #68763, #59202, #43103 ) ;
#48733=( NAMED_UNIT ( * ) SI_UNIT ( $, .STERADIAN. ) SOLID_ANGLE_UNIT ( ) );
#48735=CARTESIAN_POINT ( 'NONE',  ( 22.00000000000000711, 50.00000000000000000, -54.99999999999998579 ) ) ;
#48739=PRESENTATION_STYLE_ASSIGNMENT (( #27201 ) ) ;
#48742=STYLED_ITEM ( 'NONE', ( #27984 ), #55765 ) ;
#48757=CARTESIAN_POINT ( 'NONE',  ( 8.000000000000035527, 5.000000000000000000, 77.00402776293825013 ) ) ;
#48764=DIRECTION ( 'NONE',  ( -0.000000000000000000, 1.000000000000000000, -0.000000000000000000 ) ) ;
#48765=ORIENTED_EDGE ( 'NONE', *, *, #52845, .T. ) ;
#48771=LINE ( 'NONE', #60311, #59010 ) ;
#48779=UNCERTAINTY_MEASURE_WITH_UNIT (LENGTH_MEASURE( 1.000000000000000082E-05 ), #26672, 'distance_accuracy_value', 'NONE');
#48793=B_SPLINE_CURVE_WITH_KNOTS ( 'NONE', 3,
 ( #19389, #29949, #51414, #24321, #62995, #46167, #67236, #67591, #56324, #61948 ),
 .UNSPECIFIED., .F., .F.,
 ( 4, 2, 2, 2, 4 ),
 ( 0.006344968262825391968, 0.006871805238692929065, 0.007398642214560467029, 0.007925479190428004125, 0.008452316166295541222 ),
 .UNSPECIFIED. ) ;
#48817=ADVANCED_FACE ( 'NONE', ( #24597 ), #35178, .T. ) ;
#48818=STYLED_ITEM ( 'NONE', ( #11104 ), #48453 ) ;
#48830=FACE_OUTER_BOUND ( 'NONE', #3499, .T. ) ;
#48841=LINE ( 'NONE', #11148, #58477 ) ;
#48847=( NAMED_UNIT ( * ) PLANE_ANGLE_UNIT ( ) SI_UNIT ( $, .RADIAN. ) );
#48855=ORIENTED_EDGE ( 'NONE', *, *, #41110, .T. ) ;
#48863=CYLINDRICAL_SURFACE ( 'NONE', #9049, 12.50000000000001066 ) ;
#48872=SURFACE_STYLE_USAGE ( .BOTH. , #6948 ) ;
#48879=EDGE_CURVE ( 'NONE', #29587, #27240, #49952, .T. ) ;
#48899=DIRECTION ( 'NONE',  ( -1.000000000000000000, 0.000000000000000000, 0.000000000000000000 ) ) ;
#48907=MECHANICAL_DESIGN_GEOMETRIC_PRESENTATION_REPRESENTATION('',(#8456),#62319);
#48909=DIRECTION ( 'NONE',  ( 0.000000000000000000, 0.000000000000000000, 1.000000000000000000 ) ) ;
#48910=EDGE_CURVE ( 'NONE', #60780, #38982, #21074, .T. ) ;
#48918=SURFACE_STYLE_FILL_AREA ( #50262 ) ;
#48931=ORIENTED_EDGE ( 'NONE', *, *, #16095, .F. ) ;
#48938=CARTESIAN_POINT ( 'NONE',  ( 73.01088739851488185, 5.000000000000000000, -65.71817553072278884 ) ) ;
#48939=DIRECTION ( 'NONE',  ( 1.000000000000000000, -0.000000000000000000, 1.982541115402069054E-16 ) ) ;
#48940=FILL_AREA_STYLE ('',( #48591 ) ) ;
#48946=CIRCLE ( 'NONE', #18570, 19.99999999999998934 ) ;
#48947=PRESENTATION_STYLE_ASSIGNMENT (( #16581 ) ) ;
#48958=ORIENTED_EDGE ( 'NONE', *, *, #53728, .T. ) ;
#48968=ORIENTED_EDGE ( 'NONE', *, *, #46270, .F. ) ;
#48973=ADVANCED_FACE ( 'NONE', ( #4172, #26341 ), #10534, .T. ) ;
#48975=FILL_AREA_STYLE_COLOUR ( '', #34829 ) ;
#48978=ORIENTED_EDGE ( 'NONE', *, *, #3619, .T. ) ;
#49028=ORIENTED_EDGE ( 'NONE', *, *, #19201, .F. ) ;
#49031=CARTESIAN_POINT ( 'NONE',  ( 0.000000000000000000, 42.00000000000000000, -45.61250543006183733 ) ) ;
#49038=DIRECTION ( 'NONE',  ( 0.000000000000000000, 0.000000000000000000, -1.000000000000000000 ) ) ;
#49039=EDGE_CURVE ( 'NONE', #31350, #18241, #26415, .T. ) ;
#49046=ORIENTED_EDGE ( 'NONE', *, *, #16151, .F. ) ;
#49048=( NAMED_UNIT ( * ) SI_UNIT ( $, .STERADIAN. ) SOLID_ANGLE_UNIT ( ) );
#49053=EDGE_CURVE ( 'NONE', #63380, #63408, #64596, .T. ) ;
#49055=CARTESIAN_POINT ( 'NONE',  ( 0.000000000000000000, 42.00000000000000000, 75.00000000000001421 ) ) ;
#49063=CARTESIAN_POINT ( 'NONE',  ( 4.000000000000002665, 38.70020753820971748, -90.00000000000000000 ) ) ;
#49071=UNCERTAINTY_MEASURE_WITH_UNIT (LENGTH_MEASURE( 1.000000000000000082E-05 ), #27531, 'distance_accuracy_value', 'NONE');
#49072=DIRECTION ( 'NONE',  ( 1.300977106640434891E-16, -0.000000000000000000, 1.000000000000000000 ) ) ;
#49077=PRESENTATION_STYLE_ASSIGNMENT (( #37846 ) ) ;
#49101=PRESENTATION_STYLE_ASSIGNMENT (( #49427 ) ) ;
#49102=PLANE ( 'NONE',  #917 ) ;
#49110=EDGE_CURVE ( 'NONE', #26732, #9217, #2785, .T. ) ;
#49116=EDGE_CURVE ( 'NONE', #51841, #29900, #55140, .T. ) ;
#49117=SURFACE_STYLE_FILL_AREA ( #27595 ) ;
#49120=AXIS2_PLACEMENT_3D ( 'NONE', #49310, #13045, #22568 ) ;
#49137=ORIENTED_EDGE ( 'NONE', *, *, #46270, .T. ) ;
#49139=FACE_OUTER_BOUND ( 'NONE', #50112, .T. ) ;
#49140=ORIENTED_EDGE ( 'NONE', *, *, #28157, .T. ) ;
#49144=EDGE_CURVE ( 'NONE', #1306, #33888, #10713, .T. ) ;
#49149=DIRECTION ( 'NONE',  ( 0.000000000000000000, -1.000000000000000000, 0.000000000000000000 ) ) ;
#49183=AXIS2_PLACEMENT_3D ( 'NONE', #28797, #27741, #49245 ) ;
#49197=CARTESIAN_POINT ( 'NONE',  ( 11.00000000000001776, 42.00000000000000000, 29.68999999999999417 ) ) ;
#49199=ORIENTED_EDGE ( 'NONE', *, *, #13363, .F. ) ;
#49202=CYLINDRICAL_SURFACE ( 'NONE', #2273, 1.000000000000000888 ) ;
#49208=VERTEX_POINT ( 'NONE', #16094 ) ;
#49209=DIRECTION ( 'NONE',  ( 0.000000000000000000, 1.000000000000000000, -0.000000000000000000 ) ) ;
#49211=ORIENTED_EDGE ( 'NONE', *, *, #26051, .T. ) ;
#49233=STYLED_ITEM ( 'NONE', ( #61427 ), #13966 ) ;
#49236=SURFACE_STYLE_FILL_AREA ( #65033 ) ;
#49240=CARTESIAN_POINT ( 'NONE',  ( 92.41620014002536720, 5.000000000000000000, 24.00402776293825369 ) ) ;
#49245=DIRECTION ( 'NONE',  ( 0.000000000000000000, 0.000000000000000000, -1.000000000000000000 ) ) ;
#49255=EDGE_CURVE ( 'NONE', #14021, #40860, #14138, .T. ) ;
#49256=MECHANICAL_DESIGN_GEOMETRIC_PRESENTATION_REPRESENTATION('',(#9941),#13323);
#49257=FACE_OUTER_BOUND ( 'NONE', #35821, .T. ) ;
#49258=DIRECTION ( 'NONE',  ( 1.300977106640434891E-16, 0.000000000000000000, 1.000000000000000000 ) ) ;
#49281=VECTOR ( 'NONE', #2578, 1000.000000000000000 ) ;
#49286=( NAMED_UNIT ( * ) SI_UNIT ( $, .STERADIAN. ) SOLID_ANGLE_UNIT ( ) );
#49288=DIRECTION ( 'NONE',  ( 1.000000000000000000, 0.000000000000000000, 0.000000000000000000 ) ) ;
#49293=ORIENTED_EDGE ( 'NONE', *, *, #24758, .T. ) ;
#49294=LINE ( 'NONE', #1004, #45908 ) ;
#49299=( LENGTH_UNIT ( ) NAMED_UNIT ( * ) SI_UNIT ( .MILLI., .METRE. ) );
#49302=DIRECTION ( 'NONE',  ( 0.000000000000000000, -1.000000000000000000, 0.000000000000000000 ) ) ;
#49307=DIRECTION ( 'NONE',  ( 0.000000000000000000, 0.000000000000000000, -1.000000000000000000 ) ) ;
#49310=CARTESIAN_POINT ( 'NONE',  ( 35.99999999999999289, 0.000000000000000000, 24.00402776293825369 ) ) ;
#49311=DIRECTION ( 'NONE',  ( -0.000000000000000000, -1.000000000000000000, -0.000000000000000000 ) ) ;
#49363=CIRCLE ( 'NONE', #19006, 1.000000000000001110 ) ;
#49365=FILL_AREA_STYLE ('',( #23647 ) ) ;
#49367=CARTESIAN_POINT ( 'NONE',  ( 8.000000000000035527, 0.000000000000000000, 77.00402776293825013 ) ) ;
#49368=FACE_OUTER_BOUND ( 'NONE', #21153, .T. ) ;
#49371=FACE_OUTER_BOUND ( 'NONE', #20991, .T. ) ;
#49380=EDGE_CURVE ( 'NONE', #61113, #9855, #32030, .T. ) ;
#49381=ORIENTED_EDGE ( 'NONE', *, *, #49116, .F. ) ;
#49390=DIRECTION ( 'NONE',  ( 0.000000000000000000, 0.000000000000000000, 1.000000000000000000 ) ) ;
#49391=( NAMED_UNIT ( * ) SI_UNIT ( $, .STERADIAN. ) SOLID_ANGLE_UNIT ( ) );
#49403=DIRECTION ( 'NONE',  ( 0.000000000000000000, 0.000000000000000000, -1.000000000000000000 ) ) ;
#49411=ADVANCED_FACE ( 'NONE', ( #55061 ), #59653, .T. ) ;
#49414=TOROIDAL_SURFACE ( 'NONE', #4419, 3.499999999999998668, 1.000000000000000000 ) ;
#49427=SURFACE_STYLE_USAGE ( .BOTH. , #59246 ) ;
#49428=( NAMED_UNIT ( * ) PLANE_ANGLE_UNIT ( ) SI_UNIT ( $, .RADIAN. ) );
#49430=( NAMED_UNIT ( * ) PLANE_ANGLE_UNIT ( ) SI_UNIT ( $, .RADIAN. ) );
#49437=LINE ( 'NONE', #1158, #52145 ) ;
#49442=UNCERTAINTY_MEASURE_WITH_UNIT (LENGTH_MEASURE( 1.000000000000000082E-05 ), #20447, 'distance_accuracy_value', 'NONE');
#49455=FILL_AREA_STYLE ('',( #27946 ) ) ;
#49456=DIRECTION ( 'NONE',  ( 0.000000000000000000, 1.000000000000000000, 0.000000000000000000 ) ) ;
#49459=AXIS2_PLACEMENT_3D ( 'NONE', #62916, #31607, #4877 ) ;
#49461=VERTEX_POINT ( 'NONE', #60344 ) ;
#49468=ORIENTED_EDGE ( 'NONE', *, *, #26195, .T. ) ;
#49470=( NAMED_UNIT ( * ) SI_UNIT ( $, .STERADIAN. ) SOLID_ANGLE_UNIT ( ) );
#49475=AXIS2_PLACEMENT_3D ( 'NONE', #29150, #41155, #62555 ) ;
#49478=EDGE_LOOP ( 'NONE', ( #16343, #9000, #14675, #53600 ) ) ;
#49481=EDGE_CURVE ( 'NONE', #45878, #34731, #7927, .T. ) ;
#49483=FACE_OUTER_BOUND ( 'NONE', #31982, .T. ) ;
#49484=UNCERTAINTY_MEASURE_WITH_UNIT (LENGTH_MEASURE( 1.000000000000000082E-05 ), #14337, 'distance_accuracy_value', 'NONE');
#49492=SURFACE_STYLE_USAGE ( .BOTH. , #38968 ) ;
#49494=CARTESIAN_POINT ( 'NONE',  ( 25.00000000000001421, 43.00000000000000000, 0.000000000000000000 ) ) ;
#49496=DIRECTION ( 'NONE',  ( -0.000000000000000000, -1.000000000000000000, -0.000000000000000000 ) ) ;
#49498=FACE_OUTER_BOUND ( 'NONE', #32727, .T. ) ;
#49500=MECHANICAL_DESIGN_GEOMETRIC_PRESENTATION_REPRESENTATION('',(#4586),#59617);
#49504=VERTEX_POINT ( 'NONE', #40663 ) ;
#49513=SURFACE_SIDE_STYLE ('',( #28003 ) ) ;
#49528=ADVANCED_FACE ( 'NONE', ( #35718 ), #8637, .F. ) ;
#49536=VERTEX_POINT ( 'NONE', #66318 ) ;
#49544=MECHANICAL_DESIGN_GEOMETRIC_PRESENTATION_REPRESENTATION('',(#52917),#18111);
#49546=( NAMED_UNIT ( * ) SI_UNIT ( $, .STERADIAN. ) SOLID_ANGLE_UNIT ( ) );
#49551=PRESENTATION_STYLE_ASSIGNMENT (( #33364 ) ) ;
#49561=ORIENTED_EDGE ( 'NONE', *, *, #2193, .F. ) ;
#49576=PRESENTATION_STYLE_ASSIGNMENT (( #61149 ) ) ;
#49577=EDGE_LOOP ( 'NONE', ( #5701, #3045, #4371, #24125 ) ) ;
#49578=SURFACE_SIDE_STYLE ('',( #65738 ) ) ;
#49584=UNCERTAINTY_MEASURE_WITH_UNIT (LENGTH_MEASURE( 1.000000000000000082E-05 ), #36125, 'distance_accuracy_value', 'NONE');
#49588=DIRECTION ( 'NONE',  ( -1.000000000000000000, 0.000000000000000000, 1.982541115402069054E-16 ) ) ;
#49597=ORIENTED_EDGE ( 'NONE', *, *, #50203, .F. ) ;
#49603=VECTOR ( 'NONE', #44232, 1000.000000000000000 ) ;
#49606=FILL_AREA_STYLE ('',( #54515 ) ) ;
#49614=VECTOR ( 'NONE', #41013, 1000.000000000000000 ) ;
#49616=UNCERTAINTY_MEASURE_WITH_UNIT (LENGTH_MEASURE( 1.000000000000000082E-05 ), #37311, 'distance_accuracy_value', 'NONE');
#49617=VECTOR ( 'NONE', #62748, 1000.000000000000000 ) ;
#49623=CYLINDRICAL_SURFACE ( 'NONE', #67337, 5.000000000000004441 ) ;
#49626=FACE_OUTER_BOUND ( 'NONE', #15259, .T. ) ;
#49629=CARTESIAN_POINT ( 'NONE',  ( 98.00000000000000000, 16.00000000000000000, 5.000000000000004441 ) ) ;
#49633=LINE ( 'NONE', #11983, #67951 ) ;
#49634=EDGE_LOOP ( 'NONE', ( #60461, #34745, #32784, #39781 ) ) ;
#49638=PRESENTATION_STYLE_ASSIGNMENT (( #60858 ) ) ;
#49643=CARTESIAN_POINT ( 'NONE',  ( 82.09357085539578236, 0.000000000000000000, 32.00402776293825724 ) ) ;
#49659=EDGE_CURVE ( 'NONE', #42163, #6374, #45605, .T. ) ;
#49670=DIRECTION ( 'NONE',  ( 0.000000000000000000, 0.000000000000000000, -1.000000000000000000 ) ) ;
#49677=CARTESIAN_POINT ( 'NONE',  ( 2.999999999999993339, 5.000000000000000000, 24.00402776293822882 ) ) ;
#49680=ORIENTED_EDGE ( 'NONE', *, *, #1203, .F. ) ;
#49686=FILL_AREA_STYLE_COLOUR ( '', #3632 ) ;
#49689=COLOUR_RGB ( '', 0.66274510, 0.83137255, 0.94901961) ;
#49693=MECHANICAL_DESIGN_GEOMETRIC_PRESENTATION_REPRESENTATION('',(#47516),#41877);
#49698=AXIS2_PLACEMENT_3D ( 'NONE', #53543, #58821, #25753 ) ;
#49701=STYLED_ITEM ( 'NONE', ( #48739 ), #23705 ) ;
#49709=SURFACE_STYLE_FILL_AREA ( #49365 ) ;
#49710=DIRECTION ( 'NONE',  ( 0.000000000000000000, 1.000000000000000000, 0.000000000000000000 ) ) ;
#49711=AXIS2_PLACEMENT_3D ( 'NONE', #54974, #6802, #25755 ) ;
#49712=CARTESIAN_POINT ( 'NONE',  ( 98.00000000000000000, 14.00000000000000000, -12.50000000000000178 ) ) ;
#49714=DIRECTION ( 'NONE',  ( -0.000000000000000000, -1.000000000000000000, -0.000000000000000000 ) ) ;
#49719=VECTOR ( 'NONE', #66713, 1000.000000000000000 ) ;
#49721=SPHERICAL_SURFACE ( 'NONE', #1684, 1.000000000000000000 ) ;
#49728=ORIENTED_EDGE ( 'NONE', *, *, #53917, .F. ) ;
#49731=UNCERTAINTY_MEASURE_WITH_UNIT (LENGTH_MEASURE( 1.000000000000000082E-05 ), #25437, 'distance_accuracy_value', 'NONE');
#49734=DIRECTION ( 'NONE',  ( 0.000000000000000000, 0.000000000000000000, -1.000000000000000000 ) ) ;
#49740=( LENGTH_UNIT ( ) NAMED_UNIT ( * ) SI_UNIT ( .MILLI., .METRE. ) );
#49742=ORIENTED_EDGE ( 'NONE', *, *, #54854, .F. ) ;
#49743=( NAMED_UNIT ( * ) PLANE_ANGLE_UNIT ( ) SI_UNIT ( $, .RADIAN. ) );
#49744=STYLED_ITEM ( 'NONE', ( #22480 ), #46507 ) ;
#49747=EDGE_CURVE ( 'NONE', #49208, #33374, #52938, .T. ) ;
#49761=( NAMED_UNIT ( * ) SI_UNIT ( $, .STERADIAN. ) SOLID_ANGLE_UNIT ( ) );
#49769=( NAMED_UNIT ( * ) SI_UNIT ( $, .STERADIAN. ) SOLID_ANGLE_UNIT ( ) );
#49771=PRESENTATION_STYLE_ASSIGNMENT (( #6841 ) ) ;
#49781=CARTESIAN_POINT ( 'NONE',  ( 28.00000000000002842, 38.70020753820971748, 89.00000000000000000 ) ) ;
#49783=FILL_AREA_STYLE_COLOUR ( '', #37338 ) ;
#49786=DIRECTION ( 'NONE',  ( 1.000000000000000000, 0.000000000000000000, 0.000000000000000000 ) ) ;
#49788=CARTESIAN_POINT ( 'NONE',  ( 36.00000000000002132, 0.000000000000000000, -77.00402776293825013 ) ) ;
#49789=SURFACE_STYLE_FILL_AREA ( #18118 ) ;
#49797=DIRECTION ( 'NONE',  ( 0.000000000000000000, 0.000000000000000000, -1.000000000000000000 ) ) ;
#49804=DIRECTION ( 'NONE',  ( 1.000000000000000000, 0.000000000000000000, 0.000000000000000000 ) ) ;
#49806=CARTESIAN_POINT ( 'NONE',  ( 27.99999999999999289, 43.00000000000000000, -90.00000000000000000 ) ) ;
#49808=CARTESIAN_POINT ( 'NONE',  ( 6.000000000000017764, 26.00000000000000355, 23.99999999999999645 ) ) ;
#49813=CARTESIAN_POINT ( 'NONE',  ( 23.50000000000001776, -3.148064030671221758, -27.18999999999999417 ) ) ;
#49819=DIRECTION ( 'NONE',  ( 0.000000000000000000, 0.000000000000000000, -1.000000000000000000 ) ) ;
#49823=CARTESIAN_POINT ( 'NONE',  ( 3.000000000000002665, 35.42594141563417054, -80.00402776293826435 ) ) ;
#49827=CARTESIAN_POINT ( 'NONE',  ( 32.00000000000001421, 42.00000000000000000, 35.50000000000000000 ) ) ;
#49828=CIRCLE ( 'NONE', #34100, 22.00000000000001421 ) ;
#49831=EDGE_LOOP ( 'NONE', ( #66972, #63501, #46054, #46873 ) ) ;
#49835=LINE ( 'NONE', #27646, #16189 ) ;
#49837=DIRECTION ( 'NONE',  ( 0.000000000000000000, 0.000000000000000000, -1.000000000000000000 ) ) ;
#49849=VECTOR ( 'NONE', #33868, 1000.000000000000000 ) ;
#49856=VERTEX_POINT ( 'NONE', #33875 ) ;
#49860=CARTESIAN_POINT ( 'NONE',  ( 27.99999999999998224, 0.000000000000000000, 72.00402776293822171 ) ) ;
#49870=CARTESIAN_POINT ( 'NONE',  ( 23.67886883698855272, 24.55989583710066171, 27.18999999999999062 ) ) ;
#49871=DIRECTION ( 'NONE',  ( -0.000000000000000000, -1.000000000000000000, -0.000000000000000000 ) ) ;
#49879=SURFACE_SIDE_STYLE ('',( #12913 ) ) ;
#49881=COLOUR_RGB ( '', 0.72549020, 0.75294118, 0.79215686) ;
#49888=DIRECTION ( 'NONE',  ( 0.000000000000000000, -1.000000000000000000, 0.000000000000000000 ) ) ;
#49889=ADVANCED_FACE ( 'NONE', ( #45178 ), #34929, .F. ) ;
#49903=ORIENTED_EDGE ( 'NONE', *, *, #64894, .F. ) ;
#49909=VERTEX_POINT ( 'NONE', #4269 ) ;
#49912=VERTEX_POINT ( 'NONE', #47979 ) ;
#49920=CIRCLE ( 'NONE', #22951, 4.999999999999990230 ) ;
#49928=ORIENTED_EDGE ( 'NONE', *, *, #38403, .F. ) ;
#49929=ORIENTED_EDGE ( 'NONE', *, *, #27688, .T. ) ;
#49932=AXIS2_PLACEMENT_3D ( 'NONE', #31024, #14502, #52176 ) ;
#49935=EDGE_CURVE ( 'NONE', #48634, #15615, #31725, .T. ) ;
#49937=COLOUR_RGB ( '', 0.66274510, 0.83137255, 0.94901961) ;
#49945=DIRECTION ( 'NONE',  ( -0.000000000000000000, -1.000000000000000000, -0.000000000000000000 ) ) ;
#49947=ORIENTED_EDGE ( 'NONE', *, *, #19621, .F. ) ;
#49952=CIRCLE ( 'NONE', #27459, 1.000000000000000888 ) ;
#49961=( LENGTH_UNIT ( ) NAMED_UNIT ( * ) SI_UNIT ( .MILLI., .METRE. ) );
#49968=( LENGTH_UNIT ( ) NAMED_UNIT ( * ) SI_UNIT ( .MILLI., .METRE. ) );
#49969=( GEOMETRIC_REPRESENTATION_CONTEXT ( 3 ) GLOBAL_UNCERTAINTY_ASSIGNED_CONTEXT ( ( #28511 ) ) GLOBAL_UNIT_ASSIGNED_CONTEXT ( ( #38764, #48631, #32062 ) ) REPRESENTATION_CONTEXT ( 'NONE', 'WORKASPACE' ) );
#49984=VERTEX_POINT ( 'NONE', #20849 ) ;
#49991=SURFACE_STYLE_USAGE ( .BOTH. , #67432 ) ;
#49999=CIRCLE ( 'NONE', #42151, 1.000000000000000000 ) ;
#50006=( LENGTH_UNIT ( ) NAMED_UNIT ( * ) SI_UNIT ( .MILLI., .METRE. ) );
#50015=FACE_OUTER_BOUND ( 'NONE', #32911, .T. ) ;
#50019=CIRCLE ( 'NONE', #26393, 4.999999999999990230 ) ;
#50024=VERTEX_POINT ( 'NONE', #68690 ) ;
#50031=EDGE_LOOP ( 'NONE', ( #49561, #21813, #21459, #15466 ) ) ;
#50032=ORIENTED_EDGE ( 'NONE', *, *, #46911, .F. ) ;
#50037=SURFACE_SIDE_STYLE ('',( #7785 ) ) ;
#50044=DIRECTION ( 'NONE',  ( -7.816271194327172234E-17, -0.000000000000000000, -1.000000000000000000 ) ) ;
#50046=PRESENTATION_STYLE_ASSIGNMENT (( #38821 ) ) ;
#50053=COLOUR_RGB ( '', 0.72549020, 0.75294118, 0.79215686) ;
#50062=CIRCLE ( 'NONE', #61240, 1.000000000000000888 ) ;
#50068=CARTESIAN_POINT ( 'NONE',  ( 0.000000000000000000, 14.00000000000000000, -36.49999999999999289 ) ) ;
#50081=( GEOMETRIC_REPRESENTATION_CONTEXT ( 3 ) GLOBAL_UNCERTAINTY_ASSIGNED_CONTEXT ( ( #52458 ) ) GLOBAL_UNIT_ASSIGNED_CONTEXT ( ( #27915, #14132, #62308 ) ) REPRESENTATION_CONTEXT ( 'NONE', 'WORKASPACE' ) );
#50084=SURFACE_STYLE_USAGE ( .BOTH. , #28584 ) ;
#50094=COLOUR_RGB ( '', 0.66274510, 0.83137255, 0.94901961) ;
#50096=AXIS2_PLACEMENT_3D ( 'NONE', #7330, #22461, #55850 ) ;
#50107=SPHERICAL_SURFACE ( 'NONE', #35547, 1.000000000000000000 ) ;
#50112=EDGE_LOOP ( 'NONE', ( #26715, #61034, #30052, #616 ) ) ;
#50123=ORIENTED_EDGE ( 'NONE', *, *, #55822, .F. ) ;
#50125=DIRECTION ( 'NONE',  ( 0.000000000000000000, -1.000000000000000000, 0.000000000000000000 ) ) ;
#50144=ADVANCED_FACE ( 'NONE', ( #43038 ), #32773, .T. ) ;
#50151=FILL_AREA_STYLE_COLOUR ( '', #22223 ) ;
#50157=VECTOR ( 'NONE', #48899, 1000.000000000000000 ) ;
#50158=FILL_AREA_STYLE ('',( #28661 ) ) ;
#50160=DIRECTION ( 'NONE',  ( 0.000000000000000000, 0.000000000000000000, -1.000000000000000000 ) ) ;
#50165=SURFACE_STYLE_FILL_AREA ( #7242 ) ;
#50168=EDGE_LOOP ( 'NONE', ( #16616, #7811, #41404, #52673 ) ) ;
#50170=SURFACE_STYLE_USAGE ( .BOTH. , #6519 ) ;
#50175=ORIENTED_EDGE ( 'NONE', *, *, #62379, .F. ) ;
#50181=STYLED_ITEM ( 'NONE', ( #44600 ), #64946 ) ;
#50182=SURFACE_STYLE_USAGE ( .BOTH. , #23100 ) ;
#50183=ORIENTED_EDGE ( 'NONE', *, *, #56549, .F. ) ;
#50193=CARTESIAN_POINT ( 'NONE',  ( 3.414213562373124677, 42.99999999999999289, 79.58981420056515788 ) ) ;
#50203=EDGE_CURVE ( 'NONE', #62287, #24376, #39821, .T. ) ;
#50215=CARTESIAN_POINT ( 'NONE',  ( 23.50000000000001776, 24.55989583710066171, 27.18999999999999062 ) ) ;
#50216=( LENGTH_UNIT ( ) NAMED_UNIT ( * ) SI_UNIT ( .MILLI., .METRE. ) );
#50220=SURFACE_SIDE_STYLE ('',( #11529 ) ) ;
#50222=LINE ( 'NONE', #66377, #1156 ) ;
#50226=( GEOMETRIC_REPRESENTATION_CONTEXT ( 3 ) GLOBAL_UNCERTAINTY_ASSIGNED_CONTEXT ( ( #891 ) ) GLOBAL_UNIT_ASSIGNED_CONTEXT ( ( #17075, #12099, #49761 ) ) REPRESENTATION_CONTEXT ( 'NONE', 'WORKASPACE' ) );
#50236=FILL_AREA_STYLE ('',( #7324 ) ) ;
#50247=DIRECTION ( 'NONE',  ( -0.000000000000000000, -1.000000000000000000, -0.000000000000000000 ) ) ;
#50252=FILL_AREA_STYLE_COLOUR ( '', #22055 ) ;
#50257=CARTESIAN_POINT ( 'NONE',  ( 1.000000000000000000, 42.00000000000000000, -79.00402776293826435 ) ) ;
#50262=FILL_AREA_STYLE ('',( #11927 ) ) ;
#50269=DIRECTION ( 'NONE',  ( 1.000000000000000000, 0.000000000000000000, 0.000000000000000000 ) ) ;
#50271=EDGE_CURVE ( 'NONE', #19853, #20918, #8655, .T. ) ;
#50281=ORIENTED_EDGE ( 'NONE', *, *, #56214, .T. ) ;
#50311=DIRECTION ( 'NONE',  ( -0.000000000000000000, -1.000000000000000000, -0.000000000000000000 ) ) ;
#50315=ORIENTED_EDGE ( 'NONE', *, *, #48578, .T. ) ;
#50322=VECTOR ( 'NONE', #44842, 1000.000000000000114 ) ;
#50329=VERTEX_POINT ( 'NONE', #54722 ) ;
#50333=SURFACE_STYLE_FILL_AREA ( #66141 ) ;
#50335=ORIENTED_EDGE ( 'NONE', *, *, #57769, .T. ) ;
#50336=PRESENTATION_STYLE_ASSIGNMENT (( #7432 ) ) ;
#50347=VERTEX_POINT ( 'NONE', #54387 ) ;
#50355=FACE_OUTER_BOUND ( 'NONE', #34048, .T. ) ;
#50361=ORIENTED_EDGE ( 'NONE', *, *, #9064, .F. ) ;
#50368=CARTESIAN_POINT ( 'NONE',  ( 6.000000000000017764, 43.00000000000000000, -29.49447654986460776 ) ) ;
#50375=COLOUR_RGB ( '', 0.08235294, 0.09019608, 0.10196078) ;
#50376=EDGE_CURVE ( 'NONE', #17255, #53011, #33296, .T. ) ;
#50381=FACE_OUTER_BOUND ( 'NONE', #84, .T. ) ;
#50389=FILL_AREA_STYLE_COLOUR ( '', #65823 ) ;
#50399=SURFACE_SIDE_STYLE ('',( #22630 ) ) ;
#50401=VERTEX_POINT ( 'NONE', #68095 ) ;
#50403=VERTEX_POINT ( 'NONE', #39992 ) ;
#50405=FILL_AREA_STYLE ('',( #34226 ) ) ;
#50424=ADVANCED_FACE ( 'NONE', ( #40313 ), #8307, .T. ) ;
#50429=CARTESIAN_POINT ( 'NONE',  ( 6.117035285937317823, 43.00000000000000711, 28.67160620906787472 ) ) ;
#50430=CARTESIAN_POINT ( 'NONE',  ( 16.00000000000001776, -3.148064030671221758, -29.68999999999999417 ) ) ;
#50453=FILL_AREA_STYLE ('',( #28961 ) ) ;
#50458=DIRECTION ( 'NONE',  ( 0.000000000000000000, 0.000000000000000000, -1.000000000000000000 ) ) ;
#50469=LINE ( 'NONE', #7215, #65349 ) ;
#50473=MECHANICAL_DESIGN_GEOMETRIC_PRESENTATION_REPRESENTATION('',(#4387),#40381);
#50476=AXIS2_PLACEMENT_3D ( 'NONE', #20525, #24395, #30351 ) ;
#50477=CARTESIAN_POINT ( 'NONE',  ( 75.83633811589984930, 13.00000000000000178, -66.72655454856717938 ) ) ;
#50480=AXIS2_PLACEMENT_3D ( 'NONE', #2552, #29689, #34273 ) ;
#50488=SURFACE_STYLE_USAGE ( .BOTH. , #54701 ) ;
#50490=( NAMED_UNIT ( * ) PLANE_ANGLE_UNIT ( ) SI_UNIT ( $, .RADIAN. ) );
#50491=SURFACE_STYLE_USAGE ( .BOTH. , #50837 ) ;
#50492=MANIFOLD_SOLID_BREP ( 'Fillet3', #58736 ) ;
#50496=( GEOMETRIC_REPRESENTATION_CONTEXT ( 3 ) GLOBAL_UNCERTAINTY_ASSIGNED_CONTEXT ( ( #32724 ) ) GLOBAL_UNIT_ASSIGNED_CONTEXT ( ( #37859, #53307, #31466 ) ) REPRESENTATION_CONTEXT ( 'NONE', 'WORKASPACE' ) );
#50499=CARTESIAN_POINT ( 'NONE',  ( 10.00000000000001954, 43.00000000000000000, 28.38386403503541899 ) ) ;
#50515=VECTOR ( 'NONE', #3640, 1000.000000000000000 ) ;
#50522=SURFACE_SIDE_STYLE ('',( #24798 ) ) ;
#50524=EDGE_CURVE ( 'NONE', #12357, #47623, #904, .T. ) ;
#50540=LINE ( 'NONE', #45295, #49719 ) ;
#50563=LINE ( 'NONE', #18559, #15858 ) ;
#50568=LINE ( 'NONE', #39687, #66361 ) ;
#50573=ORIENTED_EDGE ( 'NONE', *, *, #54238, .F. ) ;
#50582=LINE ( 'NONE', #66763, #35541 ) ;
#50590=PLANE ( 'NONE',  #18705 ) ;
#50599=EDGE_CURVE ( 'NONE', #11349, #66584, #1830, .T. ) ;
#50615=AXIS2_PLACEMENT_3D ( 'NONE', #28566, #12393, #1798 ) ;
#50620=ORIENTED_EDGE ( 'NONE', *, *, #38094, .T. ) ;
#50632=FACE_OUTER_BOUND ( 'NONE', #31969, .T. ) ;
#50635=PRESENTATION_STYLE_ASSIGNMENT (( #12280 ) ) ;
#50643=( GEOMETRIC_REPRESENTATION_CONTEXT ( 3 ) GLOBAL_UNCERTAINTY_ASSIGNED_CONTEXT ( ( #67874 ) ) GLOBAL_UNIT_ASSIGNED_CONTEXT ( ( #53082, #42552, #17539 ) ) REPRESENTATION_CONTEXT ( 'NONE', 'WORKASPACE' ) );
#50645=EDGE_CURVE ( 'NONE', #46401, #48506, #28946, .T. ) ;
#50652=PRESENTATION_STYLE_ASSIGNMENT (( #54860 ) ) ;
#50660=DIRECTION ( 'NONE',  ( 0.000000000000000000, 0.000000000000000000, 1.000000000000000000 ) ) ;
#50669=EDGE_CURVE ( 'NONE', #33948, #40021, #65210, .T. ) ;
#50681=DIRECTION ( 'NONE',  ( -0.000000000000000000, -1.000000000000000000, 0.000000000000000000 ) ) ;
#50707=ORIENTED_EDGE ( 'NONE', *, *, #12624, .T. ) ;
#50709=LINE ( 'NONE', #7780, #51884 ) ;
#50710=( GEOMETRIC_REPRESENTATION_CONTEXT ( 3 ) GLOBAL_UNCERTAINTY_ASSIGNED_CONTEXT ( ( #32687 ) ) GLOBAL_UNIT_ASSIGNED_CONTEXT ( ( #24936, #67163, #67873 ) ) REPRESENTATION_CONTEXT ( 'NONE', 'WORKASPACE' ) );
#50716=( GEOMETRIC_REPRESENTATION_CONTEXT ( 3 ) GLOBAL_UNCERTAINTY_ASSIGNED_CONTEXT ( ( #27120 ) ) GLOBAL_UNIT_ASSIGNED_CONTEXT ( ( #2942, #14248, #34646 ) ) REPRESENTATION_CONTEXT ( 'NONE', 'WORKASPACE' ) );
#50719=( LENGTH_UNIT ( ) NAMED_UNIT ( * ) SI_UNIT ( .MILLI., .METRE. ) );
#50723=DIRECTION ( 'NONE',  ( 0.000000000000000000, 0.000000000000000000, -1.000000000000000000 ) ) ;
#50724=FILL_AREA_STYLE_COLOUR ( '', #23488 ) ;
#50730=VECTOR ( 'NONE', #33518, 1000.000000000000000 ) ;
#50738=SURFACE_STYLE_FILL_AREA ( #46187 ) ;
#50739=ORIENTED_EDGE ( 'NONE', *, *, #33504, .T. ) ;
#50757=STYLED_ITEM ( 'NONE', ( #15142 ), #22003 ) ;
#50759=CARTESIAN_POINT ( 'NONE',  ( 4.000000000000030198, 38.70020753820971748, 90.00000000000000000 ) ) ;
#50760=CARTESIAN_POINT ( 'NONE',  ( 98.00000000000000000, 16.00000000000000000, 0.000000000000000000 ) ) ;
#50765=EDGE_CURVE ( 'NONE', #58968, #54047, #6503, .T. ) ;
#50770=SURFACE_SIDE_STYLE ('',( #17729 ) ) ;
#50785=SURFACE_STYLE_USAGE ( .BOTH. , #55712 ) ;
#50800=CIRCLE ( 'NONE', #49698, 4.999999999999997335 ) ;
#50812=MECHANICAL_DESIGN_GEOMETRIC_PRESENTATION_REPRESENTATION('',(#12567),#63163);
#50819=STYLED_ITEM ( 'NONE', ( #37084 ), #28748 ) ;
#50834=ADVANCED_FACE ( 'NONE', ( #45545 ), #3223, .F. ) ;
#50836=CARTESIAN_POINT ( 'NONE',  ( 36.00000000000002842, 5.000000000000000000, 77.00402776293825013 ) ) ;
#50837=SURFACE_SIDE_STYLE ('',( #53759 ) ) ;
#50839=CARTESIAN_POINT ( 'NONE',  ( 57.00000000000000000, 14.00000000000000000, -60.00402776293827145 ) ) ;
#50841=VECTOR ( 'NONE', #54019, 1000.000000000000000 ) ;
#50851=LINE ( 'NONE', #18499, #16528 ) ;
#50857=ORIENTED_EDGE ( 'NONE', *, *, #25475, .T. ) ;
#50872=( NAMED_UNIT ( * ) PLANE_ANGLE_UNIT ( ) SI_UNIT ( $, .RADIAN. ) );
#50884=CARTESIAN_POINT ( 'NONE',  ( 26.00000000000001776, 42.00000000000000000, 29.68999999999999417 ) ) ;
#50897=PRESENTATION_STYLE_ASSIGNMENT (( #45311 ) ) ;
#50900=CIRCLE ( 'NONE', #59882, 18.99999999999998934 ) ;
#50906=VECTOR ( 'NONE', #53787, 1000.000000000000000 ) ;
#50907=CARTESIAN_POINT ( 'NONE',  ( 0.3542414993972760051, 42.77450856510287736, -45.47201648568073296 ) ) ;
#50909=VECTOR ( 'NONE', #24264, 1000.000000000000000 ) ;
#50920=EDGE_CURVE ( 'NONE', #20026, #56901, #10307, .T. ) ;
#50923=MECHANICAL_DESIGN_GEOMETRIC_PRESENTATION_REPRESENTATION('',(#9366),#18353);
#50926=DIRECTION ( 'NONE',  ( 0.000000000000000000, 0.000000000000000000, -1.000000000000000000 ) ) ;
#50928=VERTEX_POINT ( 'NONE', #35996 ) ;
#50933=ORIENTED_EDGE ( 'NONE', *, *, #29984, .T. ) ;
#50957=DIRECTION ( 'NONE',  ( 0.000000000000000000, 0.000000000000000000, -1.000000000000000000 ) ) ;
#50964=VERTEX_POINT ( 'NONE', #9625 ) ;
#50969=CARTESIAN_POINT ( 'NONE',  ( 23.50000000000001776, 15.00000000000000000, -27.18999999999999417 ) ) ;
#50973=SURFACE_STYLE_USAGE ( .BOTH. , #55553 ) ;
#50977=( NAMED_UNIT ( * ) PLANE_ANGLE_UNIT ( ) SI_UNIT ( $, .RADIAN. ) );
#50978=( GEOMETRIC_REPRESENTATION_CONTEXT ( 3 ) GLOBAL_UNCERTAINTY_ASSIGNED_CONTEXT ( ( #58069 ) ) GLOBAL_UNIT_ASSIGNED_CONTEXT ( ( #39270, #50490, #7912 ) ) REPRESENTATION_CONTEXT ( 'NONE', 'WORKASPACE' ) );
#50979=SURFACE_STYLE_FILL_AREA ( #13324 ) ;
#50982=( NAMED_UNIT ( * ) PLANE_ANGLE_UNIT ( ) SI_UNIT ( $, .RADIAN. ) );
#50988=STYLED_ITEM ( 'NONE', ( #25899 ), #48340 ) ;
#50996=ORIENTED_EDGE ( 'NONE', *, *, #19838, .F. ) ;
#51008=DIRECTION ( 'NONE',  ( -1.000000000000000000, 0.000000000000000000, 0.000000000000000000 ) ) ;
#51010=VECTOR ( 'NONE', #17618, 1000.000000000000000 ) ;
#51028=( NAMED_UNIT ( * ) PLANE_ANGLE_UNIT ( ) SI_UNIT ( $, .RADIAN. ) );
#51037=DIRECTION ( 'NONE',  ( 0.000000000000000000, 0.000000000000000000, -1.000000000000000000 ) ) ;
#51052=SURFACE_SIDE_STYLE ('',( #2447 ) ) ;
#51065=CIRCLE ( 'NONE', #52183, 3.499999999999999556 ) ;
#51067=( LENGTH_UNIT ( ) NAMED_UNIT ( * ) SI_UNIT ( .MILLI., .METRE. ) );
#51070=CIRCLE ( 'NONE', #31963, 1.000000000000000888 ) ;
#51084=EDGE_CURVE ( 'NONE', #53024, #35471, #55841, .T. ) ;
#51085=VECTOR ( 'NONE', #60993, 1000.000000000000000 ) ;
#51093=COLOUR_RGB ( '', 0.08235294, 0.09019608, 0.10196078) ;
#51094=VECTOR ( 'NONE', #32482, 1000.000000000000000 ) ;
#51095=DIRECTION ( 'NONE',  ( -0.000000000000000000, -1.000000000000000000, -0.000000000000000000 ) ) ;
#51100=CYLINDRICAL_SURFACE ( 'NONE', #58837, 1.000000000000000888 ) ;
#51101=ADVANCED_FACE ( 'NONE', ( #11793 ), #6170, .T. ) ;
#51106=( LENGTH_UNIT ( ) NAMED_UNIT ( * ) SI_UNIT ( .MILLI., .METRE. ) );
#51114=SURFACE_STYLE_USAGE ( .BOTH. , #61624 ) ;
#51124=UNCERTAINTY_MEASURE_WITH_UNIT (LENGTH_MEASURE( 1.000000000000000082E-05 ), #47660, 'distance_accuracy_value', 'NONE');
#51128=LINE ( 'NONE', #12416, #54445 ) ;
#51138=CARTESIAN_POINT ( 'NONE',  ( 22.99999999999995381, 5.000000000000000000, 32.00402776293825724 ) ) ;
#51139=FILL_AREA_STYLE_COLOUR ( '', #46526 ) ;
#51150=CIRCLE ( 'NONE', #12963, 24.00000000000001421 ) ;
#51156=FILL_AREA_STYLE ('',( #15280 ) ) ;
#51169=DIRECTION ( 'NONE',  ( 1.000000000000000000, 0.000000000000000000, -1.300977106640434891E-16 ) ) ;
#51177=CARTESIAN_POINT ( 'NONE',  ( 0.9999999999999991118, 43.00000000000000000, -74.38749456993816978 ) ) ;
#51189=CARTESIAN_POINT ( 'NONE',  ( 36.00000000000002842, 5.000000000000000000, -32.00402776293825724 ) ) ;
#51194=ADVANCED_FACE ( 'NONE', ( #13512 ), #63365, .T. ) ;
#51201=FILL_AREA_STYLE ('',( #34649 ) ) ;
#51204=DIRECTION ( 'NONE',  ( 0.000000000000000000, 0.000000000000000000, 1.000000000000000000 ) ) ;
#51211=AXIS2_PLACEMENT_3D ( 'NONE', #33178, #44118, #38834 ) ;
#51215=B_SPLINE_CURVE_WITH_KNOTS ( 'NONE', 3,
 ( #42970, #9195, #36990, #52117, #14820, #3872, #20059, #26384, #4576, #26031, #62978, #47568, #25354, #68978, #42292, #36300, #4211, #46874, #63677, #30969, #52467, #15521, #53142, #10227, #4933, #69316 ),
 .UNSPECIFIED., .F., .F.,
 ( 4, 2, 2, 2, 2, 2, 2, 2, 2, 2, 2, 2, 4 ),
 ( 0.000000000000000000, 0.0002642488042135191515, 0.0005284976084270383030, 0.0007927464126405575628, 0.001056995216854076606, 0.001585492825281106452, 0.002113990433708136298, 0.002642488042135166144, 0.002906736846348681718, 0.003170985650562197725, 0.003435234454775714166, 0.003699483258989229740, 0.004227980867416260453 ),
 .UNSPECIFIED. ) ;
#51220=CARTESIAN_POINT ( 'NONE',  ( 3.000000000000030198, 38.00000000000000711, 90.00000000000000000 ) ) ;
#51224=LINE ( 'NONE', #41043, #27473 ) ;
#51240=CIRCLE ( 'NONE', #20913, 1.000000000000000888 ) ;
#51241=AXIS2_PLACEMENT_3D ( 'NONE', #18887, #56896, #61793 ) ;
#51248=FACE_OUTER_BOUND ( 'NONE', #9298, .T. ) ;
#51249=EDGE_CURVE ( 'NONE', #60023, #46872, #38112, .T. ) ;
#51250=CIRCLE ( 'NONE', #23183, 1.000000000000000888 ) ;
#51255=DIRECTION ( 'NONE',  ( -1.298988366203102052E-16, 0.05527174654752588928, -0.9984713486292864371 ) ) ;
#51274=CARTESIAN_POINT ( 'NONE',  ( 33.00000000000002132, 14.00000000000000000, 79.00402776293826435 ) ) ;
#51291=SURFACE_STYLE_FILL_AREA ( #8724 ) ;
#51296=DIRECTION ( 'NONE',  ( 0.000000000000000000, 0.000000000000000000, 1.000000000000000000 ) ) ;
#51304=VERTEX_POINT ( 'NONE', #42642 ) ;
#51305=LINE ( 'NONE', #52010, #11855 ) ;
#51309=( GEOMETRIC_REPRESENTATION_CONTEXT ( 3 ) GLOBAL_UNCERTAINTY_ASSIGNED_CONTEXT ( ( #11484 ) ) GLOBAL_UNIT_ASSIGNED_CONTEXT ( ( #19867, #14974, #71 ) ) REPRESENTATION_CONTEXT ( 'NONE', 'WORKASPACE' ) );
#51317=CARTESIAN_POINT ( 'NONE',  ( 31.00000000000000355, 42.00000000000000000, -36.50000000000000000 ) ) ;
#51330=STYLED_ITEM ( 'NONE', ( #65227 ), #65333 ) ;
#51331=EDGE_CURVE ( 'NONE', #60430, #44784, #64404, .T. ) ;
#51336=PRESENTATION_STYLE_ASSIGNMENT (( #28456 ) ) ;
#51338=DIRECTION ( 'NONE',  ( 0.000000000000000000, -1.000000000000000000, 0.000000000000000000 ) ) ;
#51339=CARTESIAN_POINT ( 'NONE',  ( 27.99999999999999645, 5.000000000000000000, -72.00402776293822171 ) ) ;
#51347=FACE_OUTER_BOUND ( 'NONE', #15481, .T. ) ;
#51349=( LENGTH_UNIT ( ) NAMED_UNIT ( * ) SI_UNIT ( .MILLI., .METRE. ) );
#51353=CARTESIAN_POINT ( 'NONE',  ( 30.99999999999998579, 5.000000000000000000, 72.00402776293822171 ) ) ;
#51360=CARTESIAN_POINT ( 'NONE',  ( 33.00000000000001421, 15.00000000000000000, 36.49999999999999289 ) ) ;
#51365=FILL_AREA_STYLE_COLOUR ( '', #18628 ) ;
#51367=PRESENTATION_STYLE_ASSIGNMENT (( #30228 ) ) ;
#51369=CARTESIAN_POINT ( 'NONE',  ( 10.00000000000001776, 42.25685517452260598, -28.66913060635885913 ) ) ;
#51377=FACE_OUTER_BOUND ( 'NONE', #15062, .T. ) ;
#51383=EDGE_LOOP ( 'NONE', ( #63262, #10978, #7647, #67655 ) ) ;
#51384=DIRECTION ( 'NONE',  ( 1.000000000000000000, 0.000000000000000000, 0.000000000000000000 ) ) ;
#51395=VERTEX_POINT ( 'NONE', #16930 ) ;
#51396=STYLED_ITEM ( 'NONE', ( #31148 ), #67420 ) ;
#51403=ORIENTED_EDGE ( 'NONE', *, *, #67587, .T. ) ;
#51407=EDGE_CURVE ( 'NONE', #23681, #8511, #3263, .T. ) ;
#51411=ADVANCED_FACE ( 'NONE', ( #44725 ), #22391, .T. ) ;
#51414=CARTESIAN_POINT ( 'NONE',  ( 23.14659390890733448, 27.39756892443129743, -27.21001191564729282 ) ) ;
#51416=( NAMED_UNIT ( * ) SI_UNIT ( $, .STERADIAN. ) SOLID_ANGLE_UNIT ( ) );
#51421=AXIS2_PLACEMENT_3D ( 'NONE', #62475, #30444, #56151 ) ;
#51426=STYLED_ITEM ( 'NONE', ( #45947 ), #50492 ) ;
#51432=ORIENTED_EDGE ( 'NONE', *, *, #54628, .T. ) ;
#51434=ADVANCED_FACE ( 'NONE', ( #60484 ), #49623, .F. ) ;
#51439=( GEOMETRIC_REPRESENTATION_CONTEXT ( 3 ) GLOBAL_UNCERTAINTY_ASSIGNED_CONTEXT ( ( #58732 ) ) GLOBAL_UNIT_ASSIGNED_CONTEXT ( ( #28654, #29349, #59985 ) ) REPRESENTATION_CONTEXT ( 'NONE', 'WORKASPACE' ) );
#51442=EDGE_LOOP ( 'NONE', ( #6722, #38431, #5832, #42257 ) ) ;
#51443=CARTESIAN_POINT ( 'NONE',  ( 109.0067032876572171, 13.00000000000000178, 19.20378738324562917 ) ) ;
#51444=VERTEX_POINT ( 'NONE', #34464 ) ;
#51445=( LENGTH_UNIT ( ) NAMED_UNIT ( * ) SI_UNIT ( .MILLI., .METRE. ) );
#51447=DIRECTION ( 'NONE',  ( -1.000000000000000000, 0.000000000000000000, -0.000000000000000000 ) ) ;
#51461=VERTEX_POINT ( 'NONE', #61517 ) ;
#51462=DIRECTION ( 'NONE',  ( 1.000000000000000000, 0.000000000000000000, -0.000000000000000000 ) ) ;
#51467=DIRECTION ( 'NONE',  ( 0.000000000000000000, -1.000000000000000000, 0.000000000000000000 ) ) ;
#51469=( NAMED_UNIT ( * ) SI_UNIT ( $, .STERADIAN. ) SOLID_ANGLE_UNIT ( ) );
#51471=CARTESIAN_POINT ( 'NONE',  ( 179.4361977533476136, 0.000000000000000000, 103.7004518695250823 ) ) ;
#51486=( LENGTH_UNIT ( ) NAMED_UNIT ( * ) SI_UNIT ( .MILLI., .METRE. ) );
#51495=ORIENTED_EDGE ( 'NONE', *, *, #9987, .T. ) ;
#51502=DIRECTION ( 'NONE',  ( -0.000000000000000000, -1.000000000000000000, 0.000000000000000000 ) ) ;
#51514=FACE_OUTER_BOUND ( 'NONE', #54461, .T. ) ;
#51515=STYLED_ITEM ( 'NONE', ( #20877 ), #66640 ) ;
#51517=ORIENTED_EDGE ( 'NONE', *, *, #11357, .F. ) ;
#51524=FILL_AREA_STYLE ('',( #24774 ) ) ;
#51531=( NAMED_UNIT ( * ) SI_UNIT ( $, .STERADIAN. ) SOLID_ANGLE_UNIT ( ) );
#51534=ADVANCED_FACE ( 'NONE', ( #40817 ), #62234, .T. ) ;
#51535=CARTESIAN_POINT ( 'NONE',  ( 10.00000000000000711, 50.00000000000000000, -54.99999999999998579 ) ) ;
#51543=( LENGTH_UNIT ( ) NAMED_UNIT ( * ) SI_UNIT ( .MILLI., .METRE. ) );
#51544=AXIS2_PLACEMENT_3D ( 'NONE', #28447, #44705, #13682 ) ;
#51545=UNCERTAINTY_MEASURE_WITH_UNIT (LENGTH_MEASURE( 1.000000000000000082E-05 ), #11998, 'distance_accuracy_value', 'NONE');
#51568=VERTEX_POINT ( 'NONE', #575 ) ;
#51571=CIRCLE ( 'NONE', #32425, 1.000000000000000888 ) ;
#51576=DIRECTION ( 'NONE',  ( -0.000000000000000000, -1.000000000000000000, 0.000000000000000000 ) ) ;
#51598=FILL_AREA_STYLE ('',( #56883 ) ) ;
#51605=STYLED_ITEM ( 'NONE', ( #10005 ), #33625 ) ;
#51609=VECTOR ( 'NONE', #46988, 1000.000000000000000 ) ;
#51629=SURFACE_STYLE_USAGE ( .BOTH. , #57603 ) ;
#51638=ORIENTED_EDGE ( 'NONE', *, *, #43442, .F. ) ;
#51664=( NAMED_UNIT ( * ) SI_UNIT ( $, .STERADIAN. ) SOLID_ANGLE_UNIT ( ) );
#51678=( NAMED_UNIT ( * ) SI_UNIT ( $, .STERADIAN. ) SOLID_ANGLE_UNIT ( ) );
#51680=( NAMED_UNIT ( * ) SI_UNIT ( $, .STERADIAN. ) SOLID_ANGLE_UNIT ( ) );
#51686=( LENGTH_UNIT ( ) NAMED_UNIT ( * ) SI_UNIT ( .MILLI., .METRE. ) );
#51687=PRESENTATION_STYLE_ASSIGNMENT (( #18950 ) ) ;
#51696=SURFACE_STYLE_FILL_AREA ( #19674 ) ;
#51699=SURFACE_STYLE_USAGE ( .BOTH. , #52415 ) ;
#51700=FILL_AREA_STYLE_COLOUR ( '', #13676 ) ;
#51704=CIRCLE ( 'NONE', #57313, 1.000000000000000888 ) ;
#51736=EDGE_CURVE ( 'NONE', #38068, #34648, #13441, .T. ) ;
#51759=CARTESIAN_POINT ( 'NONE',  ( 2.999999999999993339, 5.000000000000000000, 24.00402776293822882 ) ) ;
#51767=STYLED_ITEM ( 'NONE', ( #48639 ), #45241 ) ;
#51772=MECHANICAL_DESIGN_GEOMETRIC_PRESENTATION_REPRESENTATION('',(#6801),#2270);
#51775=UNCERTAINTY_MEASURE_WITH_UNIT (LENGTH_MEASURE( 1.000000000000000082E-05 ), #65605, 'distance_accuracy_value', 'NONE');
#51782=CIRCLE ( 'NONE', #4556, 1.000000000000000888 ) ;
#51788=EDGE_LOOP ( 'NONE', ( #51403, #34044, #40133, #11396 ) ) ;
#51790=ORIENTED_EDGE ( 'NONE', *, *, #68383, .T. ) ;
#51801=EDGE_CURVE ( 'NONE', #53365, #31566, #57569, .T. ) ;
#51810=ORIENTED_EDGE ( 'NONE', *, *, #30853, .F. ) ;
#51812=ADVANCED_FACE ( 'NONE', ( #20271 ), #56880, .F. ) ;
#51815=LINE ( 'NONE', #24696, #63270 ) ;
#51817=VERTEX_POINT ( 'NONE', #67783 ) ;
#51821=CIRCLE ( 'NONE', #43955, 3.499999999999999556 ) ;
#51822=CARTESIAN_POINT ( 'NONE',  ( 27.99999999999999289, 34.36176364315826248, -80.00402776293826435 ) ) ;
#51835=DIRECTION ( 'NONE',  ( -0.000000000000000000, 1.000000000000000000, -0.000000000000000000 ) ) ;
#51837=AXIS2_PLACEMENT_3D ( 'NONE', #34039, #325, #1953 ) ;
#51839=DIRECTION ( 'NONE',  ( 0.000000000000000000, 0.3420201433256630508, -0.9396926207859105373 ) ) ;
#51841=VERTEX_POINT ( 'NONE', #26244 ) ;
#51843=AXIS2_PLACEMENT_3D ( 'NONE', #22754, #28336, #12168 ) ;
#51844=DIRECTION ( 'NONE',  ( 0.000000000000000000, 0.000000000000000000, 1.000000000000000000 ) ) ;
#51853=( NAMED_UNIT ( * ) PLANE_ANGLE_UNIT ( ) SI_UNIT ( $, .RADIAN. ) );
#51864=COLOUR_RGB ( '', 0.08235294, 0.09019608, 0.10196078) ;
#51869=PRESENTATION_STYLE_ASSIGNMENT (( #25805 ) ) ;
#51874=ORIENTED_EDGE ( 'NONE', *, *, #40014, .T. ) ;
#51884=VECTOR ( 'NONE', #35223, 1000.000000000000000 ) ;
#51885=DIRECTION ( 'NONE',  ( 0.000000000000000000, -1.000000000000000000, 0.000000000000000000 ) ) ;
#51893=MECHANICAL_DESIGN_GEOMETRIC_PRESENTATION_REPRESENTATION('',(#58603),#21554);
#51904=AXIS2_PLACEMENT_3D ( 'NONE', #59449, #64409, #6346 ) ;
#51910=VECTOR ( 'NONE', #44547, 1000.000000000000000 ) ;
#51911=DIRECTION ( 'NONE',  ( 0.000000000000000000, 0.000000000000000000, -1.000000000000000000 ) ) ;
#51933=DIRECTION ( 'NONE',  ( 0.000000000000000000, 0.000000000000000000, -1.000000000000000000 ) ) ;
#51943=DIRECTION ( 'NONE',  ( 0.000000000000000000, 0.000000000000000000, 1.000000000000000000 ) ) ;
#51947=FILL_AREA_STYLE_COLOUR ( '', #28101 ) ;
#51955=FACE_BOUND ( 'NONE', #1468, .T. ) ;
#51959=DIRECTION ( 'NONE',  ( 0.000000000000000000, 0.000000000000000000, 1.000000000000000000 ) ) ;
#51963=STYLED_ITEM ( 'NONE', ( #51367 ), #22745 ) ;
#51971=PRESENTATION_STYLE_ASSIGNMENT (( #9759 ) ) ;
#51974=DIRECTION ( 'NONE',  ( -1.000000000000000000, 0.000000000000000000, 1.300977106640434891E-16 ) ) ;
#51978=CARTESIAN_POINT ( 'NONE',  ( 27.00000000000001776, 43.00000000000000000, 34.49999999999999289 ) ) ;
#51983=ORIENTED_EDGE ( 'NONE', *, *, #51407, .F. ) ;
#51986=( NAMED_UNIT ( * ) PLANE_ANGLE_UNIT ( ) SI_UNIT ( $, .RADIAN. ) );
#51988=ORIENTED_EDGE ( 'NONE', *, *, #55760, .T. ) ;
#51994=ORIENTED_EDGE ( 'NONE', *, *, #58778, .F. ) ;
#51997=AXIS2_PLACEMENT_3D ( 'NONE', #19007, #60211, #49670 ) ;
#52010=CARTESIAN_POINT ( 'NONE',  ( 10.00000000000000888, 43.00000000000000000, -45.61250543006183733 ) ) ;
#52016=VERTEX_POINT ( 'NONE', #36510 ) ;
#52017=ORIENTED_EDGE ( 'NONE', *, *, #39651, .F. ) ;
#52018=CARTESIAN_POINT ( 'NONE',  ( 30.99999999999998579, 5.000000000000000000, -72.00402776293822171 ) ) ;
#52022=CARTESIAN_POINT ( 'NONE',  ( 3.000000000000030198, 42.00000000000000000, 89.00000000000000000 ) ) ;
#52026=SURFACE_STYLE_USAGE ( .BOTH. , #4481 ) ;
#52028=VECTOR ( 'NONE', #4918, 1000.000000000000000 ) ;
#52032=( NAMED_UNIT ( * ) PLANE_ANGLE_UNIT ( ) SI_UNIT ( $, .RADIAN. ) );
#52046=( NAMED_UNIT ( * ) SI_UNIT ( $, .STERADIAN. ) SOLID_ANGLE_UNIT ( ) );
#52058=( NAMED_UNIT ( * ) SI_UNIT ( $, .STERADIAN. ) SOLID_ANGLE_UNIT ( ) );
#52064=EDGE_LOOP ( 'NONE', ( #61150, #7997 ) ) ;
#52070=FILL_AREA_STYLE ('',( #42249 ) ) ;
#52074=FILL_AREA_STYLE_COLOUR ( '', #51093 ) ;
#52082=EDGE_CURVE ( 'NONE', #57372, #18616, #69640, .T. ) ;
#52086=DIRECTION ( 'NONE',  ( 0.000000000000000000, 0.000000000000000000, -1.000000000000000000 ) ) ;
#52087=VECTOR ( 'NONE', #7266, 1000.000000000000000 ) ;
#52088=ORIENTED_EDGE ( 'NONE', *, *, #96, .T. ) ;
#52092=CIRCLE ( 'NONE', #16143, 4.999999999999997335 ) ;
#52100=( NAMED_UNIT ( * ) SI_UNIT ( $, .STERADIAN. ) SOLID_ANGLE_UNIT ( ) );
#52103=CARTESIAN_POINT ( 'NONE',  ( 31.00000000000001421, 43.00000000000000000, 45.61250543006183022 ) ) ;
#52106=CARTESIAN_POINT ( 'NONE',  ( 11.00000000000001776, 42.00000000000000000, -28.00000000000000000 ) ) ;
#52117=CARTESIAN_POINT ( 'NONE',  ( 23.15216539473883373, 24.61138016253714156, 27.21282383882673983 ) ) ;
#52118=CARTESIAN_POINT ( 'NONE',  ( 3.000000000000002665, 38.70020753820971748, -89.00000000000000000 ) ) ;
#52122=DIRECTION ( 'NONE',  ( 0.000000000000000000, 0.000000000000000000, -1.000000000000000000 ) ) ;
#52125=MECHANICAL_DESIGN_GEOMETRIC_PRESENTATION_REPRESENTATION('',(#29595),#2631);
#52129=CIRCLE ( 'NONE', #44259, 5.000000000000000888 ) ;
#52134=ADVANCED_FACE ( 'NONE', ( #22712 ), #7565, .F. ) ;
#52141=CIRCLE ( 'NONE', #53237, 5.000000000000004441 ) ;
#52143=ORIENTED_EDGE ( 'NONE', *, *, #42538, .F. ) ;
#52145=VECTOR ( 'NONE', #67598, 1000.000000000000000 ) ;
#52153=EDGE_LOOP ( 'NONE', ( #20019, #9430, #57003, #43119, #37781, #22388, #8552, #60601 ) ) ;
#52176=DIRECTION ( 'NONE',  ( 0.000000000000000000, 0.000000000000000000, 1.000000000000000000 ) ) ;
#52183=AXIS2_PLACEMENT_3D ( 'NONE', #29893, #51008, #50660 ) ;
#52188=EDGE_LOOP ( 'NONE', ( #60702, #14541, #46291, #10989 ) ) ;
#52189=CARTESIAN_POINT ( 'NONE',  ( 31.00000000000001421, 43.00000000000000000, 45.61250543006183022 ) ) ;
#52193=MECHANICAL_DESIGN_GEOMETRIC_PRESENTATION_REPRESENTATION('',(#35351),#3821);
#52194=ORIENTED_EDGE ( 'NONE', *, *, #45624, .F. ) ;
#52201=SURFACE_STYLE_FILL_AREA ( #3963 ) ;
#52212=SURFACE_STYLE_USAGE ( .BOTH. , #46959 ) ;
#52216=EDGE_CURVE ( 'NONE', #69517, #54457, #2181, .T. ) ;
#52217=LINE ( 'NONE', #45571, #34743 ) ;
#52221=AXIS2_PLACEMENT_3D ( 'NONE', #59569, #32855, #11388 ) ;
#52223=VERTEX_POINT ( 'NONE', #2929 ) ;
#52226=EDGE_CURVE ( 'NONE', #38982, #51395, #24732, .T. ) ;
#52237=ORIENTED_EDGE ( 'NONE', *, *, #44874, .T. ) ;
#52245=CARTESIAN_POINT ( 'NONE',  ( 179.4361977533490347, 14.00000000000000000, 103.7004518695263044 ) ) ;
#52253=DIRECTION ( 'NONE',  ( 0.000000000000000000, 1.000000000000000000, -0.000000000000000000 ) ) ;
#52259=( LENGTH_UNIT ( ) NAMED_UNIT ( * ) SI_UNIT ( .MILLI., .METRE. ) );
#52265=CARTESIAN_POINT ( 'NONE',  ( 29.00000000000000000, 34.80256050929376954, -80.00402776293826435 ) ) ;
#52275=EDGE_LOOP ( 'NONE', ( #16011, #12970 ) ) ;
#52294=ORIENTED_EDGE ( 'NONE', *, *, #26170, .T. ) ;
#52311=UNCERTAINTY_MEASURE_WITH_UNIT (LENGTH_MEASURE( 1.000000000000000082E-05 ), #21671, 'distance_accuracy_value', 'NONE');
#52320=UNCERTAINTY_MEASURE_WITH_UNIT (LENGTH_MEASURE( 1.000000000000000082E-05 ), #40269, 'distance_accuracy_value', 'NONE');
#52330=FILL_AREA_STYLE ('',( #4800 ) ) ;
#52333=EDGE_CURVE ( 'NONE', #7256, #11976, #61835, .T. ) ;
#52338=EDGE_LOOP ( 'NONE', ( #11562, #29754, #47739, #38471 ) ) ;
#52348=CARTESIAN_POINT ( 'NONE',  ( 23.67688240327908389, 27.44010416289936316, -27.18999999999999062 ) ) ;
#52366=( LENGTH_UNIT ( ) NAMED_UNIT ( * ) SI_UNIT ( .MILLI., .METRE. ) );
#52378=CIRCLE ( 'NONE', #11924, 4.999999999999997335 ) ;
#52401=FILL_AREA_STYLE_COLOUR ( '', #18007 ) ;
#52412=SURFACE_SIDE_STYLE ('',( #21395 ) ) ;
#52415=SURFACE_SIDE_STYLE ('',( #3090 ) ) ;
#52416=CARTESIAN_POINT ( 'NONE',  ( 98.00000000000000000, 14.00000000000000000, 0.000000000000000000 ) ) ;
#52420=EDGE_CURVE ( 'NONE', #20391, #56887, #56219, .T. ) ;
#52426=SURFACE_STYLE_FILL_AREA ( #25645 ) ;
#52433=SURFACE_STYLE_FILL_AREA ( #30937 ) ;
#52444=DIRECTION ( 'NONE',  ( -0.000000000000000000, 1.000000000000000000, -0.000000000000000000 ) ) ;
#52448=DIRECTION ( 'NONE',  ( 1.000000000000000000, 0.000000000000000000, -1.300977106640434891E-16 ) ) ;
#52457=ORIENTED_EDGE ( 'NONE', *, *, #17978, .T. ) ;
#52458=UNCERTAINTY_MEASURE_WITH_UNIT (LENGTH_MEASURE( 1.000000000000000082E-05 ), #27915, 'distance_accuracy_value', 'NONE');
#52459=EDGE_CURVE ( 'NONE', #68594, #50928, #51782, .T. ) ;
#52466=EDGE_CURVE ( 'NONE', #4737, #49912, #22627, .T. ) ;
#52467=CARTESIAN_POINT ( 'NONE',  ( 22.70708736557406482, 27.11529135480144248, 27.31808320068521923 ) ) ;
#52468=MECHANICAL_DESIGN_GEOMETRIC_PRESENTATION_REPRESENTATION('',(#50181),#4087);
#52471=CARTESIAN_POINT ( 'NONE',  ( 22.00000000000002132, 50.00000000000000000, 60.00000000000000711 ) ) ;
#52477=VERTEX_POINT ( 'NONE', #49367 ) ;
#52479=EDGE_CURVE ( 'NONE', #50347, #58968, #60576, .T. ) ;
#52501=CARTESIAN_POINT ( 'NONE',  ( 109.0067032876572171, 14.00000000000000000, 19.20378738324562917 ) ) ;
#52516=VERTEX_POINT ( 'NONE', #49712 ) ;
#52517=EDGE_CURVE ( 'NONE', #40740, #15615, #44478, .T. ) ;
#52530=ORIENTED_EDGE ( 'NONE', *, *, #24839, .T. ) ;
#52535=VERTEX_POINT ( 'NONE', #23650 ) ;
#52547=FILL_AREA_STYLE ('',( #15273 ) ) ;
#52550=SURFACE_STYLE_USAGE ( .BOTH. , #57098 ) ;
#52569=ORIENTED_EDGE ( 'NONE', *, *, #39881, .T. ) ;
#52572=SURFACE_SIDE_STYLE ('',( #19837 ) ) ;
#52584=( LENGTH_UNIT ( ) NAMED_UNIT ( * ) SI_UNIT ( .MILLI., .METRE. ) );
#52595=( BOUNDED_CURVE ( )  B_SPLINE_CURVE ( 3, ( #40334, #24137, #50193, #2262 ),
 .UNSPECIFIED., .F., .F. ) 
 B_SPLINE_CURVE_WITH_KNOTS ( ( 4, 4 ),
 ( 3.141592653589793116, 4.712388980384689674 ),
 .UNSPECIFIED. ) 
 CURVE ( )  GEOMETRIC_REPRESENTATION_ITEM ( )  RATIONAL_B_SPLINE_CURVE ( ( 1.000000000000000000, 0.8047378541243649375, 0.8047378541243649375, 1.000000000000000000 ) ) 
 REPRESENTATION_ITEM ( '' )  );
#52601=FILL_AREA_STYLE ('',( #36452 ) ) ;
#52606=DIRECTION ( 'NONE',  ( 0.000000000000000000, 0.000000000000000000, -1.000000000000000000 ) ) ;
#52619=CARTESIAN_POINT ( 'NONE',  ( 8.000000000000030198, 0.000000000000000000, -32.00402776293825013 ) ) ;
#52653=EDGE_CURVE ( 'NONE', #16376, #59091, #9230, .T. ) ;
#52657=SURFACE_SIDE_STYLE ('',( #4082 ) ) ;
#52673=ORIENTED_EDGE ( 'NONE', *, *, #49747, .F. ) ;
#52676=ADVANCED_FACE ( 'NONE', ( #63376 ), #66389, .F. ) ;
#52679=ORIENTED_EDGE ( 'NONE', *, *, #21523, .F. ) ;
#52680=AXIS2_PLACEMENT_3D ( 'NONE', #16040, #54320, #58924 ) ;
#52688=AXIS2_PLACEMENT_3D ( 'NONE', #484, #61010, #33594 ) ;
#52689=STYLED_ITEM ( 'NONE', ( #22252 ), #66698 ) ;
#52691=EDGE_LOOP ( 'NONE', ( #27737, #1101, #67915, #66061 ) ) ;
#52696=MECHANICAL_DESIGN_GEOMETRIC_PRESENTATION_REPRESENTATION('',(#3164),#31325);
#52698=VECTOR ( 'NONE', #7534, 1000.000000000000000 ) ;
#52703=CARTESIAN_POINT ( 'NONE',  ( 2.999999999999997335, 5.000000000000000000, 72.00402776293822171 ) ) ;
#52714=( LENGTH_UNIT ( ) NAMED_UNIT ( * ) SI_UNIT ( .MILLI., .METRE. ) );
#52723=SURFACE_STYLE_FILL_AREA ( #25609 ) ;
#52738=ORIENTED_EDGE ( 'NONE', *, *, #36248, .F. ) ;
#52742=FACE_OUTER_BOUND ( 'NONE', #54813, .T. ) ;
#52762=FACE_OUTER_BOUND ( 'NONE', #18540, .T. ) ;
#52766=COLOUR_RGB ( '', 0.09019608, 0.27058824, 0.51372549) ;
#52771=LINE ( 'NONE', #62265, #61102 ) ;
#52782=LINE ( 'NONE', #3850, #36267 ) ;
#52793=ORIENTED_EDGE ( 'NONE', *, *, #12952, .F. ) ;
#52795=( BOUNDED_CURVE ( )  B_SPLINE_CURVE ( 3, ( #33933, #6492, #44884, #66289 ),
 .UNSPECIFIED., .F., .F. ) 
 B_SPLINE_CURVE_WITH_KNOTS ( ( 4, 4 ),
 ( 1.570796326794894116, 3.141592653589793116 ),
 .UNSPECIFIED. ) 
 CURVE ( )  GEOMETRIC_REPRESENTATION_ITEM ( )  RATIONAL_B_SPLINE_CURVE ( ( 1.000000000000000000, 0.8047378541243643824, 0.8047378541243643824, 1.000000000000000000 ) ) 
 REPRESENTATION_ITEM ( '' )  );
#52797=MECHANICAL_DESIGN_GEOMETRIC_PRESENTATION_REPRESENTATION('',(#6714),#55005);
#52801=AXIS2_PLACEMENT_3D ( 'NONE', #25975, #63957, #11187 ) ;
#52806=ORIENTED_EDGE ( 'NONE', *, *, #58778, .T. ) ;
#52807=CARTESIAN_POINT ( 'NONE',  ( 22.00000000000002132, 43.00000000000000000, 75.00000000000000000 ) ) ;
#52815=DIRECTION ( 'NONE',  ( 0.000000000000000000, 0.000000000000000000, -1.000000000000000000 ) ) ;
#52816=( NAMED_UNIT ( * ) PLANE_ANGLE_UNIT ( ) SI_UNIT ( $, .RADIAN. ) );
#52832=ADVANCED_FACE ( 'NONE', ( #41086 ), #41787, .T. ) ;
#52835=( GEOMETRIC_REPRESENTATION_CONTEXT ( 3 ) GLOBAL_UNCERTAINTY_ASSIGNED_CONTEXT ( ( #63128 ) ) GLOBAL_UNIT_ASSIGNED_CONTEXT ( ( #5209, #10521, #35860 ) ) REPRESENTATION_CONTEXT ( 'NONE', 'WORKASPACE' ) );
#52838=VERTEX_POINT ( 'NONE', #29805 ) ;
#52845=EDGE_CURVE ( 'NONE', #55122, #45002, #68488, .T. ) ;
#52846=FACE_OUTER_BOUND ( 'NONE', #22537, .T. ) ;
#52855=( NAMED_UNIT ( * ) SI_UNIT ( $, .STERADIAN. ) SOLID_ANGLE_UNIT ( ) );
#52866=CARTESIAN_POINT ( 'NONE',  ( 30.99999999999999289, 5.000000000000000000, 37.00402776293829277 ) ) ;
#52883=( LENGTH_UNIT ( ) NAMED_UNIT ( * ) SI_UNIT ( .MILLI., .METRE. ) );
#52888=AXIS2_PLACEMENT_3D ( 'NONE', #66042, #16856, #38329 ) ;
#52893=SURFACE_STYLE_FILL_AREA ( #32436 ) ;
#52895=( NAMED_UNIT ( * ) SI_UNIT ( $, .STERADIAN. ) SOLID_ANGLE_UNIT ( ) );
#52905=DIRECTION ( 'NONE',  ( 1.000000000000000000, 0.000000000000000000, 0.000000000000000000 ) ) ;
#52915=FILL_AREA_STYLE ('',( #26156 ) ) ;
#52917=STYLED_ITEM ( 'NONE', ( #19655 ), #12452 ) ;
#52930=CARTESIAN_POINT ( 'NONE',  ( 93.00000000000000000, 5.000000000000000000, 0.000000000000000000 ) ) ;
#52938=LINE ( 'NONE', #30761, #46767 ) ;
#52939=SURFACE_SIDE_STYLE ('',( #31805 ) ) ;
#52941=CYLINDRICAL_SURFACE ( 'NONE', #33336, 5.000000000000011546 ) ;
#52942=( GEOMETRIC_REPRESENTATION_CONTEXT ( 3 ) GLOBAL_UNCERTAINTY_ASSIGNED_CONTEXT ( ( #9591 ) ) GLOBAL_UNIT_ASSIGNED_CONTEXT ( ( #46047, #2711, #8034 ) ) REPRESENTATION_CONTEXT ( 'NONE', 'WORKASPACE' ) );
#52951=DIRECTION ( 'NONE',  ( 0.000000000000000000, 1.000000000000000000, 0.000000000000000000 ) ) ;
#52968=DIRECTION ( 'NONE',  ( 1.000000000000000000, -0.000000000000000000, 0.000000000000000000 ) ) ;
#52976=VERTEX_POINT ( 'NONE', #50477 ) ;
#52977=MECHANICAL_DESIGN_GEOMETRIC_PRESENTATION_REPRESENTATION('',(#36117),#23738);
#52998=SURFACE_SIDE_STYLE ('',( #824 ) ) ;
#53000=DIRECTION ( 'NONE',  ( 0.000000000000000000, 1.000000000000000000, 0.000000000000000000 ) ) ;
#53002=ORIENTED_EDGE ( 'NONE', *, *, #41490, .T. ) ;
#53003=FACE_OUTER_BOUND ( 'NONE', #41871, .T. ) ;
#53009=( NAMED_UNIT ( * ) SI_UNIT ( $, .STERADIAN. ) SOLID_ANGLE_UNIT ( ) );
#53010=( NAMED_UNIT ( * ) PLANE_ANGLE_UNIT ( ) SI_UNIT ( $, .RADIAN. ) );
#53011=VERTEX_POINT ( 'NONE', #51177 ) ;
#53015=DIRECTION ( 'NONE',  ( -0.000000000000000000, -1.000000000000000000, -0.000000000000000000 ) ) ;
#53016=DIRECTION ( 'NONE',  ( 1.000000000000000000, 0.000000000000000000, -0.000000000000000000 ) ) ;
#53022=DIRECTION ( 'NONE',  ( 0.000000000000000000, 0.000000000000000000, -1.000000000000000000 ) ) ;
#53024=VERTEX_POINT ( 'NONE', #18473 ) ;
#53027=LINE ( 'NONE', #37589, #40803 ) ;
#53028=UNCERTAINTY_MEASURE_WITH_UNIT (LENGTH_MEASURE( 1.000000000000000082E-05 ), #57161, 'distance_accuracy_value', 'NONE');
#53035=CARTESIAN_POINT ( 'NONE',  ( 3.000000000000002665, 37.76051491742381216, -89.34202014332566932 ) ) ;
#53036=ORIENTED_EDGE ( 'NONE', *, *, #41029, .T. ) ;
#53040=CARTESIAN_POINT ( 'NONE',  ( 32.00000000000001421, 14.00000000000000000, 34.49999999999998579 ) ) ;
#53041=( LENGTH_UNIT ( ) NAMED_UNIT ( * ) SI_UNIT ( .MILLI., .METRE. ) );
#53049=VERTEX_POINT ( 'NONE', #61360 ) ;
#53050=( NAMED_UNIT ( * ) SI_UNIT ( $, .STERADIAN. ) SOLID_ANGLE_UNIT ( ) );
#53060=( GEOMETRIC_REPRESENTATION_CONTEXT ( 3 ) GLOBAL_UNCERTAINTY_ASSIGNED_CONTEXT ( ( #15125 ) ) GLOBAL_UNIT_ASSIGNED_CONTEXT ( ( #41508, #10859, #43603 ) ) REPRESENTATION_CONTEXT ( 'NONE', 'WORKASPACE' ) );
#53082=( LENGTH_UNIT ( ) NAMED_UNIT ( * ) SI_UNIT ( .MILLI., .METRE. ) );
#53086=EDGE_CURVE ( 'NONE', #28375, #35982, #68056, .T. ) ;
#53088=AXIS2_PLACEMENT_3D ( 'NONE', #69148, #52968, #46699 ) ;
#53089=CARTESIAN_POINT ( 'NONE',  ( 32.00000000000001421, 15.00000000000000000, 36.49999999999999289 ) ) ;
#53094=UNCERTAINTY_MEASURE_WITH_UNIT (LENGTH_MEASURE( 1.000000000000000082E-05 ), #61105, 'distance_accuracy_value', 'NONE');
#53095=TOROIDAL_SURFACE ( 'NONE', #62052, 18.99999999999998934, 1.000000000000000000 ) ;
#53104=PRESENTATION_STYLE_ASSIGNMENT (( #47165 ) ) ;
#53123=MECHANICAL_DESIGN_GEOMETRIC_PRESENTATION_REPRESENTATION('',(#261),#56456);
#53142=CARTESIAN_POINT ( 'NONE',  ( 22.91109586540972032, 27.27678992330844920, 27.25908479965321263 ) ) ;
#53146=VERTEX_POINT ( 'NONE', #57124 ) ;
#53156=FILL_AREA_STYLE ('',( #20441 ) ) ;
#53164=CIRCLE ( 'NONE', #19397, 1.000000000000000888 ) ;
#53185=DIRECTION ( 'NONE',  ( 0.000000000000000000, 0.000000000000000000, -1.000000000000000000 ) ) ;
#53188=ORIENTED_EDGE ( 'NONE', *, *, #40293, .F. ) ;
#53198=CARTESIAN_POINT ( 'NONE',  ( 0.08961394468541400427, 42.48853604202994916, -74.70442749311222030 ) ) ;
#53200=VECTOR ( 'NONE', #23207, 1000.000000000000000 ) ;
#53202=( GEOMETRIC_REPRESENTATION_CONTEXT ( 3 ) GLOBAL_UNCERTAINTY_ASSIGNED_CONTEXT ( ( #25676 ) ) GLOBAL_UNIT_ASSIGNED_CONTEXT ( ( #28297, #11805, #44566 ) ) REPRESENTATION_CONTEXT ( 'NONE', 'WORKASPACE' ) );
#53209=UNCERTAINTY_MEASURE_WITH_UNIT (LENGTH_MEASURE( 1.000000000000000082E-05 ), #9470, 'distance_accuracy_value', 'NONE');
#53211=CARTESIAN_POINT ( 'NONE',  ( 10.00000000000002309, 43.00000000000000000, 90.00000000000000000 ) ) ;
#53220=VECTOR ( 'NONE', #28160, 1000.000000000000000 ) ;
#53231=EDGE_CURVE ( 'NONE', #56901, #1286, #61689, .T. ) ;
#53232=FILL_AREA_STYLE_COLOUR ( '', #20448 ) ;
#53234=( NAMED_UNIT ( * ) SI_UNIT ( $, .STERADIAN. ) SOLID_ANGLE_UNIT ( ) );
#53237=AXIS2_PLACEMENT_3D ( 'NONE', #65994, #32961, #59309 ) ;
#53242=SURFACE_STYLE_USAGE ( .BOTH. , #5356 ) ;
#53243=FILL_AREA_STYLE ('',( #27153 ) ) ;
#53252=CIRCLE ( 'NONE', #3784, 3.499999999999999556 ) ;
#53265=SURFACE_STYLE_USAGE ( .BOTH. , #32133 ) ;
#53271=DIRECTION ( 'NONE',  ( -0.7681514953298232973, 0.000000000000000000, 0.6402681315062906942 ) ) ;
#53272=DIRECTION ( 'NONE',  ( 0.000000000000000000, 0.000000000000000000, -1.000000000000000000 ) ) ;
#53283=MECHANICAL_DESIGN_GEOMETRIC_PRESENTATION_REPRESENTATION('',(#13951),#25147);
#53285=ORIENTED_EDGE ( 'NONE', *, *, #27475, .F. ) ;
#53287=CYLINDRICAL_SURFACE ( 'NONE', #18152, 1.000000000000000888 ) ;
#53288=CYLINDRICAL_SURFACE ( 'NONE', #38939, 22.00000000000001421 ) ;
#53295=CIRCLE ( 'NONE', #40970, 1.000000000000000888 ) ;
#53298=EDGE_CURVE ( 'NONE', #22897, #5819, #39544, .T. ) ;
#53307=( NAMED_UNIT ( * ) PLANE_ANGLE_UNIT ( ) SI_UNIT ( $, .RADIAN. ) );
#53308=DIRECTION ( 'NONE',  ( 0.000000000000000000, -0.000000000000000000, 1.000000000000000000 ) ) ;
#53312=ORIENTED_EDGE ( 'NONE', *, *, #10343, .F. ) ;
#53313=LINE ( 'NONE', #42795, #25460 ) ;
#53315=AXIS2_PLACEMENT_3D ( 'NONE', #756, #20923, #37494 ) ;
#53319=EDGE_CURVE ( 'NONE', #39971, #23974, #54615, .T. ) ;
#53325=FACE_BOUND ( 'NONE', #68171, .T. ) ;
#53327=CIRCLE ( 'NONE', #20722, 1.000000000000000888 ) ;
#53329=DIRECTION ( 'NONE',  ( -0.000000000000000000, -1.000000000000000000, 0.000000000000000000 ) ) ;
#53334=ORIENTED_EDGE ( 'NONE', *, *, #13091, .F. ) ;
#53349=CARTESIAN_POINT ( 'NONE',  ( 57.00000000000000000, 16.00000000000000000, -60.00402776293825724 ) ) ;
#53353=STYLED_ITEM ( 'NONE', ( #53104 ), #48973 ) ;
#53361=ORIENTED_EDGE ( 'NONE', *, *, #17349, .T. ) ;
#53363=CARTESIAN_POINT ( 'NONE',  ( 7.999999999999998224, 5.000000000000000000, -37.00402776293825724 ) ) ;
#53364=DIRECTION ( 'NONE',  ( 0.000000000000000000, 0.000000000000000000, -1.000000000000000000 ) ) ;
#53365=VERTEX_POINT ( 'NONE', #6427 ) ;
#53377=VECTOR ( 'NONE', #34702, 1000.000000000000000 ) ;
#53386=( LENGTH_UNIT ( ) NAMED_UNIT ( * ) SI_UNIT ( .MILLI., .METRE. ) );
#53389=CARTESIAN_POINT ( 'NONE',  ( 57.00000000000000000, 0.000000000000000000, -79.00402776293826435 ) ) ;
#53394=LINE ( 'NONE', #33568, #5805 ) ;
#53408=CARTESIAN_POINT ( 'NONE',  ( 32.00000000000001421, 43.00000000000000000, 36.49999999999999289 ) ) ;
#53418=CARTESIAN_POINT ( 'NONE',  ( 23.49527607712185073, 27.44009427658185984, 27.19000446309344809 ) ) ;
#53426=DIRECTION ( 'NONE',  ( -0.000000000000000000, -1.000000000000000000, 0.000000000000000000 ) ) ;
#53428=COLOUR_RGB ( '', 0.40784314, 0.44705882, 0.49803922) ;
#53429=ORIENTED_EDGE ( 'NONE', *, *, #19201, .T. ) ;
#53431=DIRECTION ( 'NONE',  ( 0.000000000000000000, 0.000000000000000000, -1.000000000000000000 ) ) ;
#53434=CARTESIAN_POINT ( 'NONE',  ( 1.000000000000000000, 0.9999999999999991118, -80.00402776293826435 ) ) ;
#53436=EDGE_LOOP ( 'NONE', ( #48958, #1890, #15868, #52806 ) ) ;
#53441=SURFACE_STYLE_FILL_AREA ( #65711 ) ;
#53461=DIRECTION ( 'NONE',  ( 0.000000000000000000, 0.000000000000000000, -1.000000000000000000 ) ) ;
#53463=ADVANCED_FACE ( 'NONE', ( #17015 ), #19314, .T. ) ;
#53466=CARTESIAN_POINT ( 'NONE',  ( 1.000000000000000000, 0.9999999999999991118, -79.00402776293826435 ) ) ;
#53468=PRESENTATION_STYLE_ASSIGNMENT (( #65028 ) ) ;
#53493=DIRECTION ( 'NONE',  ( 0.000000000000000000, -1.000000000000000000, 0.000000000000000000 ) ) ;
#53494=SURFACE_STYLE_USAGE ( .BOTH. , #1339 ) ;
#53495=FACE_OUTER_BOUND ( 'NONE', #3551, .T. ) ;
#53500=CARTESIAN_POINT ( 'NONE',  ( 2.999999999999996447, 0.000000000000000000, -37.00402776293829277 ) ) ;
#53502=CIRCLE ( 'NONE', #16428, 1.000000000000000888 ) ;
#53513=FILL_AREA_STYLE ('',( #64757 ) ) ;
#53519=DIRECTION ( 'NONE',  ( 1.000000000000000000, 0.000000000000000000, 0.000000000000000000 ) ) ;
#53538=DIRECTION ( 'NONE',  ( -0.000000000000000000, -1.000000000000000000, 0.000000000000000000 ) ) ;
#53543=CARTESIAN_POINT ( 'NONE',  ( 7.999999999999992895, 0.000000000000000000, 24.00402776293826079 ) ) ;
#53550=FILL_AREA_STYLE ('',( #20494 ) ) ;
#53562=ORIENTED_EDGE ( 'NONE', *, *, #22573, .T. ) ;
#53579=FILL_AREA_STYLE_COLOUR ( '', #67344 ) ;
#53590=DIRECTION ( 'NONE',  ( -1.000000000000000000, 0.000000000000000000, 0.000000000000000000 ) ) ;
#53600=ORIENTED_EDGE ( 'NONE', *, *, #21912, .T. ) ;
#53608=ORIENTED_EDGE ( 'NONE', *, *, #22312, .F. ) ;
#53611=LINE ( 'NONE', #69447, #25217 ) ;
#53617=DIRECTION ( 'NONE',  ( 0.000000000000000000, 1.000000000000000000, 0.000000000000000000 ) ) ;
#53619=( NAMED_UNIT ( * ) PLANE_ANGLE_UNIT ( ) SI_UNIT ( $, .RADIAN. ) );
#53625=ORIENTED_EDGE ( 'NONE', *, *, #24839, .F. ) ;
#53626=DIRECTION ( 'NONE',  ( 0.000000000000000000, 0.000000000000000000, -1.000000000000000000 ) ) ;
#53627=( GEOMETRIC_REPRESENTATION_CONTEXT ( 3 ) GLOBAL_UNCERTAINTY_ASSIGNED_CONTEXT ( ( #34796 ) ) GLOBAL_UNIT_ASSIGNED_CONTEXT ( ( #67458, #14005, #25574 ) ) REPRESENTATION_CONTEXT ( 'NONE', 'WORKASPACE' ) );
#53641=FILL_AREA_STYLE_COLOUR ( '', #5970 ) ;
#53652=ADVANCED_FACE ( 'NONE', ( #46901 ), #65699, .T. ) ;
#53654=CARTESIAN_POINT ( 'NONE',  ( 179.4361977533490347, 13.00000000000000178, 103.7004518695263044 ) ) ;
#53668=CARTESIAN_POINT ( 'NONE',  ( 31.00000000000000000, 42.00000000000000000, -79.00402776293826435 ) ) ;
#53669=AXIS2_PLACEMENT_3D ( 'NONE', #34580, #51467, #12784 ) ;
#53670=EDGE_CURVE ( 'NONE', #41380, #31338, #27022, .T. ) ;
#53679=CARTESIAN_POINT ( 'NONE',  ( 22.29422224269975672, 26.00000000000000355, -27.50000000000000711 ) ) ;
#53686=DIRECTION ( 'NONE',  ( -0.000000000000000000, 0.000000000000000000, -1.000000000000000000 ) ) ;
#53689=CARTESIAN_POINT ( 'NONE',  ( 10.00000000000000711, 50.00000000000000000, -60.00000000000000000 ) ) ;
#53698=FILL_AREA_STYLE ('',( #32250 ) ) ;
#53704=DIRECTION ( 'NONE',  ( 0.000000000000000000, 0.000000000000000000, 1.000000000000000000 ) ) ;
#53728=EDGE_CURVE ( 'NONE', #20856, #42614, #50568, .T. ) ;
#53742=UNCERTAINTY_MEASURE_WITH_UNIT (LENGTH_MEASURE( 1.000000000000000082E-05 ), #37382, 'distance_accuracy_value', 'NONE');
#53746=PRESENTATION_STYLE_ASSIGNMENT (( #21058 ) ) ;
#53754=CARTESIAN_POINT ( 'NONE',  ( 1.000000000000000000, 43.00000000000000000, 35.50000000000000000 ) ) ;
#53759=SURFACE_STYLE_FILL_AREA ( #22110 ) ;
#53761=CYLINDRICAL_SURFACE ( 'NONE', #62941, 1.000000000000000888 ) ;
#53775=FACE_OUTER_BOUND ( 'NONE', #52691, .T. ) ;
#53787=DIRECTION ( 'NONE',  ( -1.000000000000000000, 0.000000000000000000, -0.000000000000000000 ) ) ;
#53799=EDGE_LOOP ( 'NONE', ( #45676, #50361, #33527, #30295, #14831 ) ) ;
#53802=CIRCLE ( 'NONE', #23466, 110.0000000000000142 ) ;
#53803=SURFACE_STYLE_USAGE ( .BOTH. , #20427 ) ;
#53806=( LENGTH_UNIT ( ) NAMED_UNIT ( * ) SI_UNIT ( .MILLI., .METRE. ) );
#53818=CARTESIAN_POINT ( 'NONE',  ( 108.3664351561509562, 14.00000000000000000, -18.43563588791579377 ) ) ;
#53819=AXIS2_PLACEMENT_3D ( 'NONE', #13165, #34622, #2202 ) ;
#53820=FILL_AREA_STYLE ('',( #42985 ) ) ;
#53828=UNCERTAINTY_MEASURE_WITH_UNIT (LENGTH_MEASURE( 1.000000000000000082E-05 ), #15468, 'distance_accuracy_value', 'NONE');
#53841=ORIENTED_EDGE ( 'NONE', *, *, #67338, .F. ) ;
#53849=PRESENTATION_STYLE_ASSIGNMENT (( #17305 ) ) ;
#53861=AXIS2_PLACEMENT_3D ( 'NONE', #56808, #58186, #31426 ) ;
#53873=CARTESIAN_POINT ( 'NONE',  ( 57.00000000000000000, 0.9999999999999991118, -60.00402776293827145 ) ) ;
#53876=DIRECTION ( 'NONE',  ( 0.000000000000000000, 0.000000000000000000, -1.000000000000000000 ) ) ;
#53878=EDGE_LOOP ( 'NONE', ( #14711, #33047, #68143, #1710 ) ) ;
#53879=VECTOR ( 'NONE', #56695, 1000.000000000000000 ) ;
#53884=UNCERTAINTY_MEASURE_WITH_UNIT (LENGTH_MEASURE( 1.000000000000000082E-05 ), #50006, 'distance_accuracy_value', 'NONE');
#53888=STYLED_ITEM ( 'NONE', ( #61182 ), #69187 ) ;
#53893=VECTOR ( 'NONE', #65917, 1000.000000000000000 ) ;
#53905=STYLED_ITEM ( 'NONE', ( #42238 ), #20977 ) ;
#53907=LINE ( 'NONE', #27511, #16828 ) ;
#53908=STYLED_ITEM ( 'NONE', ( #44399 ), #34243 ) ;
#53910=( NAMED_UNIT ( * ) SI_UNIT ( $, .STERADIAN. ) SOLID_ANGLE_UNIT ( ) );
#53917=EDGE_CURVE ( 'NONE', #40178, #17236, #65263, .T. ) ;
#53921=CARTESIAN_POINT ( 'NONE',  ( 2.000000000000015099, 26.00000000000000355, 20.49999999999999645 ) ) ;
#53926=CIRCLE ( 'NONE', #41615, 1.000000000000000888 ) ;
#53935=CARTESIAN_POINT ( 'NONE',  ( 35.99999999999999289, 5.000000000000000000, -72.00402776293825013 ) ) ;
#53939=AXIS2_PLACEMENT_3D ( 'NONE', #45746, #67162, #61869 ) ;
#53946=SURFACE_STYLE_USAGE ( .BOTH. , #52939 ) ;
#53947=DIRECTION ( 'NONE',  ( -0.000000000000000000, 1.000000000000000000, -0.000000000000000000 ) ) ;
#53959=SURFACE_SIDE_STYLE ('',( #83 ) ) ;
#53961=ORIENTED_EDGE ( 'NONE', *, *, #43143, .F. ) ;
#53962=FACE_OUTER_BOUND ( 'NONE', #28398, .T. ) ;
#53979=( GEOMETRIC_REPRESENTATION_CONTEXT ( 3 ) GLOBAL_UNCERTAINTY_ASSIGNED_CONTEXT ( ( #41773 ) ) GLOBAL_UNIT_ASSIGNED_CONTEXT ( ( #63525, #69164, #44198 ) ) REPRESENTATION_CONTEXT ( 'NONE', 'WORKASPACE' ) );
#53990=ADVANCED_FACE ( 'NONE', ( #30466 ), #35436, .F. ) ;
#53997=MECHANICAL_DESIGN_GEOMETRIC_PRESENTATION_REPRESENTATION('',(#9075),#48430);
#53999=COLOUR_RGB ( '', 0.72549020, 0.75294118, 0.79215686) ;
#54001=CARTESIAN_POINT ( 'NONE',  ( 0.000000000000000000, 0.9999999999999991118, -79.00402776293826435 ) ) ;
#54007=EDGE_CURVE ( 'NONE', #44668, #53049, #64593, .T. ) ;
#54011=AXIS2_PLACEMENT_3D ( 'NONE', #54773, #49888, #45330 ) ;
#54015=MECHANICAL_DESIGN_GEOMETRIC_PRESENTATION_REPRESENTATION('',(#57397),#20327);
#54018=( NAMED_UNIT ( * ) PLANE_ANGLE_UNIT ( ) SI_UNIT ( $, .RADIAN. ) );
#54019=DIRECTION ( 'NONE',  ( -0.000000000000000000, -0.000000000000000000, 1.000000000000000000 ) ) ;
#54021=PLANE ( 'NONE',  #40925 ) ;
#54027=ORIENTED_EDGE ( 'NONE', *, *, #42064, .T. ) ;
#54029=( NAMED_UNIT ( * ) SI_UNIT ( $, .STERADIAN. ) SOLID_ANGLE_UNIT ( ) );
#54046=FILL_AREA_STYLE ('',( #42866 ) ) ;
#54047=VERTEX_POINT ( 'NONE', #10085 ) ;
#54048=CIRCLE ( 'NONE', #5737, 0.9999999999999995559 ) ;
#54064=EDGE_CURVE ( 'NONE', #49536, #55848, #6868, .T. ) ;
#54065=( LENGTH_UNIT ( ) NAMED_UNIT ( * ) SI_UNIT ( .MILLI., .METRE. ) );
#54076=CARTESIAN_POINT ( 'NONE',  ( 10.00000000000000178, 43.00000000000000000, -90.00000000000000000 ) ) ;
#54083=PRESENTATION_STYLE_ASSIGNMENT (( #65681 ) ) ;
#54092=CIRCLE ( 'NONE', #3542, 1.000000000000000888 ) ;
#54095=( NAMED_UNIT ( * ) SI_UNIT ( $, .STERADIAN. ) SOLID_ANGLE_UNIT ( ) );
#54102=AXIS2_PLACEMENT_3D ( 'NONE', #56191, #56546, #45355 ) ;
#54105=STYLED_ITEM ( 'NONE', ( #17375 ), #53463 ) ;
#54127=CARTESIAN_POINT ( 'NONE',  ( 1.000000000000000000, 43.00000000000000000, -35.50000000000000000 ) ) ;
#54131=ORIENTED_EDGE ( 'NONE', *, *, #55677, .F. ) ;
#54132=EDGE_LOOP ( 'NONE', ( #49137, #43532, #35884, #17242, #53036, #64795, #32303, #54398, #61673, #46698, #46551, #59744, #14970 ) ) ;
#54139=CARTESIAN_POINT ( 'NONE',  ( 6.750018943533632410, 42.91041480136897945, -27.90050555725692405 ) ) ;
#54150=CARTESIAN_POINT ( 'NONE',  ( 11.00000000000001776, 42.00000000000000000, -28.38386403503541899 ) ) ;
#54154=PRESENTATION_STYLE_ASSIGNMENT (( #32698 ) ) ;
#54160=DIRECTION ( 'NONE',  ( -0.000000000000000000, -1.000000000000000000, -0.000000000000000000 ) ) ;
#54166=( NAMED_UNIT ( * ) SI_UNIT ( $, .STERADIAN. ) SOLID_ANGLE_UNIT ( ) );
#54167=( LENGTH_UNIT ( ) NAMED_UNIT ( * ) SI_UNIT ( .MILLI., .METRE. ) );
#54168=CARTESIAN_POINT ( 'NONE',  ( 179.4361977533490347, 14.00000000000000000, -103.7004518695263044 ) ) ;
#54171=VECTOR ( 'NONE', #23357, 1000.000000000000000 ) ;
#54178=VECTOR ( 'NONE', #64873, 1000.000000000000000 ) ;
#54186=ORIENTED_EDGE ( 'NONE', *, *, #34620, .F. ) ;
#54188=VECTOR ( 'NONE', #8363, 1000.000000000000000 ) ;
#54193=( NAMED_UNIT ( * ) SI_UNIT ( $, .STERADIAN. ) SOLID_ANGLE_UNIT ( ) );
#54195=FILL_AREA_STYLE ('',( #48975 ) ) ;
#54210=CARTESIAN_POINT ( 'NONE',  ( 0.9999999999999991118, 43.00000000000000000, -74.38749456993816978 ) ) ;
#54221=PRESENTATION_STYLE_ASSIGNMENT (( #12334 ) ) ;
#54222=VECTOR ( 'NONE', #46784, 1000.000000000000000 ) ;
#54230=CIRCLE ( 'NONE', #64386, 1.000000000000000000 ) ;
#54231=ADVANCED_FACE ( 'NONE', ( #60668 ), #3454, .T. ) ;
#54234=DIRECTION ( 'NONE',  ( -0.000000000000000000, -1.000000000000000000, 0.000000000000000000 ) ) ;
#54236=( GEOMETRIC_REPRESENTATION_CONTEXT ( 3 ) GLOBAL_UNCERTAINTY_ASSIGNED_CONTEXT ( ( #432 ) ) GLOBAL_UNIT_ASSIGNED_CONTEXT ( ( #8140, #29581, #24299 ) ) REPRESENTATION_CONTEXT ( 'NONE', 'WORKASPACE' ) );
#54238=EDGE_CURVE ( 'NONE', #37266, #29977, #45923, .T. ) ;
#54245=STYLED_ITEM ( 'NONE', ( #24198 ), #46516 ) ;
#54246=CARTESIAN_POINT ( 'NONE',  ( 3.000000000000002665, 42.00000000000000000, 3.772833609257260986E-15 ) ) ;
#54247=ORIENTED_EDGE ( 'NONE', *, *, #40690, .T. ) ;
#54259=CARTESIAN_POINT ( 'NONE',  ( 28.58578643762692550, 42.99999999999999289, 90.00000000000000000 ) ) ;
#54261=VECTOR ( 'NONE', #42248, 1000.000000000000000 ) ;
#54268=( NAMED_UNIT ( * ) PLANE_ANGLE_UNIT ( ) SI_UNIT ( $, .RADIAN. ) );
#54274=CARTESIAN_POINT ( 'NONE',  ( 22.00000000000000711, 50.00000000000000000, -65.00000000000000000 ) ) ;
#54275=AXIS2_PLACEMENT_3D ( 'NONE', #52471, #20065, #25357 ) ;
#54276=( BOUNDED_CURVE ( )  B_SPLINE_CURVE ( 3, ( #59027, #22085, #21737, #43249 ),
 .UNSPECIFIED., .F., .F. ) 
 B_SPLINE_CURVE_WITH_KNOTS ( ( 4, 4 ),
 ( 4.712388980384689674, 6.283185307179586232 ),
 .UNSPECIFIED. ) 
 CURVE ( )  GEOMETRIC_REPRESENTATION_ITEM ( )  RATIONAL_B_SPLINE_CURVE ( ( 1.000000000000000000, 0.8047378541243649375, 0.8047378541243649375, 1.000000000000000000 ) ) 
 REPRESENTATION_ITEM ( '' )  );
#54303=( GEOMETRIC_REPRESENTATION_CONTEXT ( 3 ) GLOBAL_UNCERTAINTY_ASSIGNED_CONTEXT ( ( #7439 ) ) GLOBAL_UNIT_ASSIGNED_CONTEXT ( ( #17248, #39050, #11933 ) ) REPRESENTATION_CONTEXT ( 'NONE', 'WORKASPACE' ) );
#54320=DIRECTION ( 'NONE',  ( -0.000000000000000000, 1.000000000000000000, -0.000000000000000000 ) ) ;
#54322=FACE_OUTER_BOUND ( 'NONE', #64940, .T. ) ;
#54332=FILL_AREA_STYLE ('',( #53641 ) ) ;
#54339=DIRECTION ( 'NONE',  ( -0.000000000000000000, -0.3420201433256629953, 0.9396926207859104263 ) ) ;
#54352=FILL_AREA_STYLE_COLOUR ( '', #14459 ) ;
#54366=FACE_BOUND ( 'NONE', #32375, .T. ) ;
#54373=SURFACE_SIDE_STYLE ('',( #28674 ) ) ;
#54374=LINE ( 'NONE', #29011, #49603 ) ;
#54380=CIRCLE ( 'NONE', #24071, 0.9999999999999995559 ) ;
#54387=CARTESIAN_POINT ( 'NONE',  ( 86.21825843581743243, 5.000000000000000000, -39.83014742847162637 ) ) ;
#54398=ORIENTED_EDGE ( 'NONE', *, *, #52653, .T. ) ;
#54405=MECHANICAL_DESIGN_GEOMETRIC_PRESENTATION_REPRESENTATION('',(#16303),#45486);
#54426=CARTESIAN_POINT ( 'NONE',  ( 24.50817055128190347, 25.15492634751250733, 27.39952695552187478 ) ) ;
#54427=( NAMED_UNIT ( * ) PLANE_ANGLE_UNIT ( ) SI_UNIT ( $, .RADIAN. ) );
#54437=FILL_AREA_STYLE_COLOUR ( '', #65172 ) ;
#54438=PRESENTATION_STYLE_ASSIGNMENT (( #10165 ) ) ;
#54445=VECTOR ( 'NONE', #13462, 1000.000000000000000 ) ;
#54450=CARTESIAN_POINT ( 'NONE',  ( 1.000000000000000888, 14.00000000000000533, -35.50000000000000000 ) ) ;
#54451=CARTESIAN_POINT ( 'NONE',  ( 1.000000000000000000, -60.04052944165106709, 36.50000000000000000 ) ) ;
#54452=VECTOR ( 'NONE', #47258, 1000.000000000000000 ) ;
#54456=DIRECTION ( 'NONE',  ( 1.000000000000000000, 0.000000000000000000, 0.000000000000000000 ) ) ;
#54457=VERTEX_POINT ( 'NONE', #46848 ) ;
#54461=EDGE_LOOP ( 'NONE', ( #60844, #39212, #44987, #46590 ) ) ;
#54471=CIRCLE ( 'NONE', #55585, 0.9999999999999986677 ) ;
#54473=FILL_AREA_STYLE ('',( #42943 ) ) ;
#54494=EDGE_CURVE ( 'NONE', #46872, #26109, #41896, .T. ) ;
#54496=VERTEX_POINT ( 'NONE', #42586 ) ;
#54507=AXIS2_PLACEMENT_3D ( 'NONE', #59145, #15905, #53876 ) ;
#54508=DIRECTION ( 'NONE',  ( 0.000000000000000000, 0.000000000000000000, -1.000000000000000000 ) ) ;
#54512=SURFACE_STYLE_FILL_AREA ( #33076 ) ;
#54515=FILL_AREA_STYLE_COLOUR ( '', #66850 ) ;
#54524=CARTESIAN_POINT ( 'NONE',  ( 32.00000000000000711, 42.00000000000000000, -36.50000000000000000 ) ) ;
#54536=ORIENTED_EDGE ( 'NONE', *, *, #56423, .F. ) ;
#54537=VERTEX_POINT ( 'NONE', #47177 ) ;
#54542=SPHERICAL_SURFACE ( 'NONE', #39337, 1.000000000000000000 ) ;
#54545=ORIENTED_EDGE ( 'NONE', *, *, #9112, .T. ) ;
#54570=EDGE_CURVE ( 'NONE', #62177, #60780, #55270, .T. ) ;
#54571=CARTESIAN_POINT ( 'NONE',  ( 33.00000000000000000, 15.00000000000000000, -80.00402776293826435 ) ) ;
#54575=ORIENTED_EDGE ( 'NONE', *, *, #17978, .F. ) ;
#54591=ORIENTED_EDGE ( 'NONE', *, *, #57243, .T. ) ;
#54601=FACE_OUTER_BOUND ( 'NONE', #15759, .T. ) ;
#54612=LINE ( 'NONE', #32452, #45112 ) ;
#54614=CARTESIAN_POINT ( 'NONE',  ( 25.00000000000001421, 43.00000000000000000, -29.68999999999999417 ) ) ;
#54615=LINE ( 'NONE', #55308, #55274 ) ;
#54619=CARTESIAN_POINT ( 'NONE',  ( 3.000000000000002665, 43.00000000000000000, -90.00000000000000000 ) ) ;
#54628=EDGE_CURVE ( 'NONE', #67437, #52838, #56951, .T. ) ;
#54631=CARTESIAN_POINT ( 'NONE',  ( 57.00000000000000000, 16.00000000000000000, 60.00402776293825724 ) ) ;
#54632=CARTESIAN_POINT ( 'NONE',  ( 31.00000000000001421, 42.00000000000000000, 36.50000000000000000 ) ) ;
#54639=ORIENTED_EDGE ( 'NONE', *, *, #6663, .F. ) ;
#54643=CARTESIAN_POINT ( 'NONE',  ( 8.000000000000030198, 5.000000000000000000, -29.00402776293826079 ) ) ;
#54649=CARTESIAN_POINT ( 'NONE',  ( 75.83633811589984930, 0.9999999999999991118, 66.72655454856716517 ) ) ;
#54651=CARTESIAN_POINT ( 'NONE',  ( 33.00000000000000000, 15.00000000000000000, -79.00402776293826435 ) ) ;
#54653=EDGE_LOOP ( 'NONE', ( #30130, #5916, #29821 ) ) ;
#54658=SURFACE_STYLE_FILL_AREA ( #32873 ) ;
#54665=ADVANCED_FACE ( 'NONE', ( #6123 ), #30852, .F. ) ;
#54675=ORIENTED_EDGE ( 'NONE', *, *, #14378, .T. ) ;
#54686=DIRECTION ( 'NONE',  ( 0.000000000000000000, -0.000000000000000000, 1.000000000000000000 ) ) ;
#54700=DIRECTION ( 'NONE',  ( -1.000000000000000000, 0.000000000000000000, 0.000000000000000000 ) ) ;
#54701=SURFACE_SIDE_STYLE ('',( #28998 ) ) ;
#54706=FACE_OUTER_BOUND ( 'NONE', #4291, .T. ) ;
#54709=MECHANICAL_DESIGN_GEOMETRIC_PRESENTATION_REPRESENTATION('',(#3003),#53627);
#54717=DIRECTION ( 'NONE',  ( 0.000000000000000000, 0.000000000000000000, 1.000000000000000000 ) ) ;
#54721=DIRECTION ( 'NONE',  ( -6.122553444624043322E-15, 0.8823529411764708952, -0.4705882352941173630 ) ) ;
#54722=CARTESIAN_POINT ( 'NONE',  ( 1.000000000000000888, 0.000000000000000000, -79.00402776293826435 ) ) ;
#54724=ORIENTED_EDGE ( 'NONE', *, *, #34379, .F. ) ;
#54728=DIRECTION ( 'NONE',  ( -1.300977106640435137E-16, 0.000000000000000000, -1.000000000000000000 ) ) ;
#54756=FILL_AREA_STYLE_COLOUR ( '', #39409 ) ;
#54764=( NAMED_UNIT ( * ) PLANE_ANGLE_UNIT ( ) SI_UNIT ( $, .RADIAN. ) );
#54767=VERTEX_POINT ( 'NONE', #54649 ) ;
#54771=ADVANCED_FACE ( 'NONE', ( #44157 ), #33545, .T. ) ;
#54773=CARTESIAN_POINT ( 'NONE',  ( 7.999999999999998224, 0.000000000000000000, -37.00402776293825724 ) ) ;
#54793=SURFACE_STYLE_USAGE ( .BOTH. , #44657 ) ;
#54798=ORIENTED_EDGE ( 'NONE', *, *, #9081, .T. ) ;
#54800=ORIENTED_EDGE ( 'NONE', *, *, #62642, .T. ) ;
#54807=CARTESIAN_POINT ( 'NONE',  ( 31.00000000000002132, 42.00000000000000000, 79.00402776293823592 ) ) ;
#54813=EDGE_LOOP ( 'NONE', ( #27564, #27431, #10745, #7963 ) ) ;
#54816=SURFACE_STYLE_USAGE ( .BOTH. , #270 ) ;
#54826=COLOUR_RGB ( '', 0.09019608, 0.27058824, 0.51372549) ;
#54844=AXIS2_PLACEMENT_3D ( 'NONE', #60221, #22592, #61256 ) ;
#54853=AXIS2_PLACEMENT_3D ( 'NONE', #61060, #55447, #12519 ) ;
#54854=EDGE_CURVE ( 'NONE', #60539, #21950, #10462, .T. ) ;
#54860=SURFACE_STYLE_USAGE ( .BOTH. , #17946 ) ;
#54867=ORIENTED_EDGE ( 'NONE', *, *, #49935, .F. ) ;
#54875=EDGE_LOOP ( 'NONE', ( #41910, #19411 ) ) ;
#54877=ORIENTED_EDGE ( 'NONE', *, *, #60264, .T. ) ;
#54879=CARTESIAN_POINT ( 'NONE',  ( 1.000000000000000000, 0.9999999999999991118, -79.00402776293826435 ) ) ;
#54892=FILL_AREA_STYLE_COLOUR ( '', #34402 ) ;
#54894=ORIENTED_EDGE ( 'NONE', *, *, #41680, .T. ) ;
#54897=ORIENTED_EDGE ( 'NONE', *, *, #54238, .T. ) ;
#54898=AXIS2_PLACEMENT_3D ( 'NONE', #60763, #17880, #17558 ) ;
#54904=( GEOMETRIC_REPRESENTATION_CONTEXT ( 3 ) GLOBAL_UNCERTAINTY_ASSIGNED_CONTEXT ( ( #3667 ) ) GLOBAL_UNIT_ASSIGNED_CONTEXT ( ( #15354, #14996, #41381 ) ) REPRESENTATION_CONTEXT ( 'NONE', 'WORKASPACE' ) );
#54914=EDGE_LOOP ( 'NONE', ( #8487, #66385, #10536, #66692 ) ) ;
#54915=( NAMED_UNIT ( * ) PLANE_ANGLE_UNIT ( ) SI_UNIT ( $, .RADIAN. ) );
#54919=VECTOR ( 'NONE', #24232, 1000.000000000000000 ) ;
#54922=CARTESIAN_POINT ( 'NONE',  ( 22.00000000000002132, 43.00000000000000000, 45.61250543006183733 ) ) ;
#54924=DIRECTION ( 'NONE',  ( 0.000000000000000000, 1.000000000000000000, 0.000000000000000000 ) ) ;
#54925=SURFACE_SIDE_STYLE ('',( #44108 ) ) ;
#54930=CARTESIAN_POINT ( 'NONE',  ( 8.000000000000030198, 5.000000000000000000, -29.00402776293826079 ) ) ;
#54937=AXIS2_PLACEMENT_3D ( 'NONE', #784, #64191, #32894 ) ;
#54938=( NAMED_UNIT ( * ) SI_UNIT ( $, .STERADIAN. ) SOLID_ANGLE_UNIT ( ) );
#54954=VECTOR ( 'NONE', #15897, 1000.000000000000000 ) ;
#54969=AXIS2_PLACEMENT_3D ( 'NONE', #25448, #34606, #66641 ) ;
#54973=DIRECTION ( 'NONE',  ( 0.000000000000000000, 0.000000000000000000, 1.000000000000000000 ) ) ;
#54974=CARTESIAN_POINT ( 'NONE',  ( 31.00000000000001066, 42.00000000000000000, -4.033029030585349936E-15 ) ) ;
#54977=DIRECTION ( 'NONE',  ( -0.000000000000000000, -1.000000000000000000, -0.000000000000000000 ) ) ;
#54978=CIRCLE ( 'NONE', #21300, 16.00000000000000000 ) ;
#54984=CARTESIAN_POINT ( 'NONE',  ( 0.000000000000000000, 0.9999999999999991118, 79.00402776293826435 ) ) ;
#54992=DIRECTION ( 'NONE',  ( -0.000000000000000000, -1.000000000000000000, 0.000000000000000000 ) ) ;
#54996=STYLED_ITEM ( 'NONE', ( #3445 ), #20903 ) ;
#55005=( GEOMETRIC_REPRESENTATION_CONTEXT ( 3 ) GLOBAL_UNCERTAINTY_ASSIGNED_CONTEXT ( ( #15843 ) ) GLOBAL_UNIT_ASSIGNED_CONTEXT ( ( #14527, #2890, #57807 ) ) REPRESENTATION_CONTEXT ( 'NONE', 'WORKASPACE' ) );
#55010=SURFACE_STYLE_FILL_AREA ( #21634 ) ;
#55014=( NAMED_UNIT ( * ) SI_UNIT ( $, .STERADIAN. ) SOLID_ANGLE_UNIT ( ) );
#55045=( NAMED_UNIT ( * ) PLANE_ANGLE_UNIT ( ) SI_UNIT ( $, .RADIAN. ) );
#55053=SURFACE_STYLE_USAGE ( .BOTH. , #33277 ) ;
#55060=ORIENTED_EDGE ( 'NONE', *, *, #1626, .F. ) ;
#55061=FACE_OUTER_BOUND ( 'NONE', #38635, .T. ) ;
#55062=ORIENTED_EDGE ( 'NONE', *, *, #31773, .F. ) ;
#55076=LINE ( 'NONE', #23773, #48058 ) ;
#55085=DIRECTION ( 'NONE',  ( 0.000000000000000000, 0.000000000000000000, -1.000000000000000000 ) ) ;
#55091=ORIENTED_EDGE ( 'NONE', *, *, #26440, .T. ) ;
#55105=( GEOMETRIC_REPRESENTATION_CONTEXT ( 3 ) GLOBAL_UNCERTAINTY_ASSIGNED_CONTEXT ( ( #33467 ) ) GLOBAL_UNIT_ASSIGNED_CONTEXT ( ( #55590, #46375, #17962 ) ) REPRESENTATION_CONTEXT ( 'NONE', 'WORKASPACE' ) );
#55120=DIRECTION ( 'NONE',  ( -1.000000000000000000, 0.000000000000000000, 1.300977106640434644E-16 ) ) ;
#55122=VERTEX_POINT ( 'NONE', #23949 ) ;
#55140=LINE ( 'NONE', #44315, #42211 ) ;
#55142=VERTEX_POINT ( 'NONE', #52103 ) ;
#55151=COLOUR_RGB ( '', 0.09019608, 0.27058824, 0.51372549) ;
#55160=FACE_OUTER_BOUND ( 'NONE', #38858, .T. ) ;
#55164=EDGE_CURVE ( 'NONE', #1567, #63720, #40507, .T. ) ;
#55169=SURFACE_STYLE_FILL_AREA ( #33722 ) ;
#55175=ORIENTED_EDGE ( 'NONE', *, *, #1245, .F. ) ;
#55179=CARTESIAN_POINT ( 'NONE',  ( 179.4361977533490631, 5.000000000000000000, -103.7004518695262192 ) ) ;
#55188=EDGE_CURVE ( 'NONE', #44668, #47418, #519, .T. ) ;
#55192=LINE ( 'NONE', #28445, #54919 ) ;
#55195=VECTOR ( 'NONE', #34695, 1000.000000000000000 ) ;
#55199=FILL_AREA_STYLE_COLOUR ( '', #12352 ) ;
#55223=ORIENTED_EDGE ( 'NONE', *, *, #20248, .F. ) ;
#55243=LINE ( 'NONE', #17316, #64299 ) ;
#55257=( NAMED_UNIT ( * ) SI_UNIT ( $, .STERADIAN. ) SOLID_ANGLE_UNIT ( ) );
#55260=AXIS2_PLACEMENT_3D ( 'NONE', #30478, #51974, #4803 ) ;
#55267=FILL_AREA_STYLE ('',( #28156 ) ) ;
#55268=UNCERTAINTY_MEASURE_WITH_UNIT (LENGTH_MEASURE( 1.000000000000000082E-05 ), #16031, 'distance_accuracy_value', 'NONE');
#55270=CIRCLE ( 'NONE', #28322, 1.000000000000000888 ) ;
#55271=DIRECTION ( 'NONE',  ( -0.000000000000000000, 0.000000000000000000, 1.000000000000000000 ) ) ;
#55274=VECTOR ( 'NONE', #1795, 1000.000000000000000 ) ;
#55276=EDGE_CURVE ( 'NONE', #50329, #60715, #37506, .T. ) ;
#55287=DIRECTION ( 'NONE',  ( -0.000000000000000000, -1.000000000000000000, -0.000000000000000000 ) ) ;
#55293=CARTESIAN_POINT ( 'NONE',  ( 96.10348817448824832, 5.000000000000000000, -27.38099488609876531 ) ) ;
#55308=CARTESIAN_POINT ( 'NONE',  ( 2.999999999999998668, 0.000000000000000000, 72.00402776293822171 ) ) ;
#55319=LINE ( 'NONE', #33191, #66734 ) ;
#55320=ORIENTED_EDGE ( 'NONE', *, *, #27291, .F. ) ;
#55337=SURFACE_STYLE_USAGE ( .BOTH. , #12072 ) ;
#55340=EDGE_CURVE ( 'NONE', #59244, #33888, #26366, .T. ) ;
#55351=EDGE_CURVE ( 'NONE', #2410, #50347, #26186, .T. ) ;
#55352=AXIS2_PLACEMENT_3D ( 'NONE', #19255, #24527, #29477 ) ;
#55365=STYLED_ITEM ( 'NONE', ( #33703 ), #22907 ) ;
#55379=FILL_AREA_STYLE_COLOUR ( '', #50375 ) ;
#55383=CARTESIAN_POINT ( 'NONE',  ( 22.00000000000000355, 42.00000000000000000, -75.00000000000001421 ) ) ;
#55389=DIRECTION ( 'NONE',  ( 0.000000000000000000, 0.000000000000000000, -1.000000000000000000 ) ) ;
#55391=DIRECTION ( 'NONE',  ( -0.000000000000000000, 1.000000000000000000, -0.000000000000000000 ) ) ;
#55408=DIRECTION ( 'NONE',  ( 1.000000000000000000, -0.000000000000000000, 0.000000000000000000 ) ) ;
#55421=PRESENTATION_STYLE_ASSIGNMENT (( #1200 ) ) ;
#55423=COLOUR_RGB ( '', 0.09019608, 0.27058824, 0.51372549) ;
#55427=CARTESIAN_POINT ( 'NONE',  ( 11.00000000000001776, 26.00000000000000355, 23.99999999999999645 ) ) ;
#55437=ORIENTED_EDGE ( 'NONE', *, *, #37757, .T. ) ;
#55444=CARTESIAN_POINT ( 'NONE',  ( 3.000000000000030198, 34.36176364315826248, 80.00402776293826435 ) ) ;
#55447=DIRECTION ( 'NONE',  ( -1.000000000000000000, 0.000000000000000000, 0.000000000000000000 ) ) ;
#55452=SURFACE_SIDE_STYLE ('',( #60033 ) ) ;
#55457=CARTESIAN_POINT ( 'NONE',  ( 0.7152604538204497819, 42.96841842781390852, 45.59272046071829010 ) ) ;
#55468=ADVANCED_FACE ( 'NONE', ( #28779 ), #39383, .T. ) ;
#55473=VECTOR ( 'NONE', #34884, 1000.000000000000000 ) ;
#55481=STYLED_ITEM ( 'NONE', ( #50336 ), #2820 ) ;
#55484=DIRECTION ( 'NONE',  ( 1.300977106640437603E-16, 0.000000000000000000, 1.000000000000000000 ) ) ;
#55485=STYLED_ITEM ( 'NONE', ( #8308 ), #7259 ) ;
#55489=FILL_AREA_STYLE_COLOUR ( '', #32863 ) ;
#55513=CARTESIAN_POINT ( 'NONE',  ( 0.000000000000000000, 13.00000000000000178, 80.00402776293826435 ) ) ;
#55519=DIRECTION ( 'NONE',  ( 0.000000000000000000, -1.000000000000000000, -0.000000000000000000 ) ) ;
#55525=COLOUR_RGB ( '', 0.40784314, 0.44705882, 0.49803922) ;
#55528=( NAMED_UNIT ( * ) SI_UNIT ( $, .STERADIAN. ) SOLID_ANGLE_UNIT ( ) );
#55535=DIRECTION ( 'NONE',  ( 0.000000000000000000, 0.000000000000000000, 1.000000000000000000 ) ) ;
#55545=PRESENTATION_STYLE_ASSIGNMENT (( #55890 ) ) ;
#55547=CARTESIAN_POINT ( 'NONE',  ( 2.999999999999998668, 5.000000000000000000, -37.00402776293829277 ) ) ;
#55551=STYLED_ITEM ( 'NONE', ( #9511 ), #48817 ) ;
#55553=SURFACE_SIDE_STYLE ('',( #29138 ) ) ;
#55557=LINE ( 'NONE', #10665, #3222 ) ;
#55579=EDGE_CURVE ( 'NONE', #56002, #18424, #37559, .T. ) ;
#55584=( GEOMETRIC_REPRESENTATION_CONTEXT ( 3 ) GLOBAL_UNCERTAINTY_ASSIGNED_CONTEXT ( ( #53209 ) ) GLOBAL_UNIT_ASSIGNED_CONTEXT ( ( #9470, #30186, #51678 ) ) REPRESENTATION_CONTEXT ( 'NONE', 'WORKASPACE' ) );
#55585=AXIS2_PLACEMENT_3D ( 'NONE', #58998, #26617, #42190 ) ;
#55590=( LENGTH_UNIT ( ) NAMED_UNIT ( * ) SI_UNIT ( .MILLI., .METRE. ) );
#55595=EDGE_CURVE ( 'NONE', #63408, #63380, #30700, .T. ) ;
#55608=( LENGTH_UNIT ( ) NAMED_UNIT ( * ) SI_UNIT ( .MILLI., .METRE. ) );
#55610=EDGE_CURVE ( 'NONE', #15954, #66584, #9399, .T. ) ;
#55621=EDGE_LOOP ( 'NONE', ( #66602, #4842, #3175, #18251, #33464, #35414, #31611, #24958 ) ) ;
#55638=CARTESIAN_POINT ( 'NONE',  ( 57.00000000000000000, 16.00000000000000000, -47.50402776293824303 ) ) ;
#55668=DIRECTION ( 'NONE',  ( -0.000000000000000000, -1.000000000000000000, -0.000000000000000000 ) ) ;
#55670=EDGE_CURVE ( 'NONE', #65056, #19539, #31903, .T. ) ;
#55671=AXIS2_PLACEMENT_3D ( 'NONE', #4318, #63098, #26494 ) ;
#55677=EDGE_CURVE ( 'NONE', #33374, #27703, #36880, .T. ) ;
#55681=CARTESIAN_POINT ( 'NONE',  ( 57.00000000000000000, 14.00000000000000000, -60.00402776293827145 ) ) ;
#55683=PLANE ( 'NONE',  #62349 ) ;
#55712=SURFACE_SIDE_STYLE ('',( #62011 ) ) ;
#55717=ORIENTED_EDGE ( 'NONE', *, *, #67741, .F. ) ;
#55734=CARTESIAN_POINT ( 'NONE',  ( 93.00000000000000000, 13.00000000000000178, 0.000000000000000000 ) ) ;
#55743=FILL_AREA_STYLE_COLOUR ( '', #4209 ) ;
#55756=( BOUNDED_CURVE ( )  B_SPLINE_CURVE ( 3, ( #25248, #46766, #11495, #43221 ),
 .UNSPECIFIED., .F., .F. ) 
 B_SPLINE_CURVE_WITH_KNOTS ( ( 4, 4 ),
 ( 0.000000000000000000, 1.570796326794896558 ),
 .UNSPECIFIED. ) 
 CURVE ( )  GEOMETRIC_REPRESENTATION_ITEM ( )  RATIONAL_B_SPLINE_CURVE ( ( 1.000000000000000000, 0.8047378541243649375, 0.8047378541243649375, 1.000000000000000000 ) ) 
 REPRESENTATION_ITEM ( '' )  );
#55760=EDGE_CURVE ( 'NONE', #23764, #40740, #52141, .T. ) ;
#55762=CIRCLE ( 'NONE', #46835, 1.499999999999997780 ) ;
#55764=FACE_OUTER_BOUND ( 'NONE', #48427, .T. ) ;
#55765=ADVANCED_FACE ( 'NONE', ( #39297 ), #44593, .T. ) ;
#55770=SURFACE_SIDE_STYLE ('',( #50165 ) ) ;
#55774=EDGE_LOOP ( 'NONE', ( #32168, #59044, #45087, #52237, #25058, #28314, #66056, #60068 ) ) ;
#55777=CARTESIAN_POINT ( 'NONE',  ( 30.99999999999999289, 0.000000000000000000, -24.00402776293822171 ) ) ;
#55781=ORIENTED_EDGE ( 'NONE', *, *, #44979, .F. ) ;
#55784=SURFACE_STYLE_FILL_AREA ( #28686 ) ;
#55787=VERTEX_POINT ( 'NONE', #38623 ) ;
#55790=MECHANICAL_DESIGN_GEOMETRIC_PRESENTATION_REPRESENTATION('',(#17619),#24316);
#55793=CARTESIAN_POINT ( 'NONE',  ( 0.000000000000000000, 42.00000000000000000, -79.00402776293826435 ) ) ;
#55798=EDGE_CURVE ( 'NONE', #44275, #34188, #49835, .T. ) ;
#55799=DIRECTION ( 'NONE',  ( -1.000000000000000000, 0.000000000000000000, 0.000000000000000000 ) ) ;
#55803=CARTESIAN_POINT ( 'NONE',  ( -4.099639464710813641E-16, 42.24290439781479733, 45.14575947097794284 ) ) ;
#55822=EDGE_CURVE ( 'NONE', #53024, #47418, #16470, .T. ) ;
#55826=CARTESIAN_POINT ( 'NONE',  ( -1.018511207705687038E-14, 42.00000000000000000, 28.38386403503541899 ) ) ;
#55841=( BOUNDED_CURVE ( )  B_SPLINE_CURVE ( 3, ( #63866, #20263, #15707, #20622 ),
 .UNSPECIFIED., .F., .F. ) 
 B_SPLINE_CURVE_WITH_KNOTS ( ( 4, 4 ),
 ( 3.141592653589794004, 4.712388980384689674 ),
 .UNSPECIFIED. ) 
 CURVE ( )  GEOMETRIC_REPRESENTATION_ITEM ( )  RATIONAL_B_SPLINE_CURVE ( ( 1.000000000000000000, 0.8047378541243652705, 0.8047378541243652705, 1.000000000000000000 ) ) 
 REPRESENTATION_ITEM ( '' )  );
#55844=DIRECTION ( 'NONE',  ( 0.000000000000000000, 0.000000000000000000, 1.000000000000000000 ) ) ;
#55846=CARTESIAN_POINT ( 'NONE',  ( 26.00000000000001776, -3.148064030671221758, 29.68999999999999417 ) ) ;
#55848=VERTEX_POINT ( 'NONE', #12874 ) ;
#55850=DIRECTION ( 'NONE',  ( 0.000000000000000000, 0.000000000000000000, -1.000000000000000000 ) ) ;
#55851=ORIENTED_EDGE ( 'NONE', *, *, #36509, .T. ) ;
#55867=DIRECTION ( 'NONE',  ( -1.734723475976805517E-15, 0.000000000000000000, -1.000000000000000000 ) ) ;
#55872=ORIENTED_EDGE ( 'NONE', *, *, #60811, .F. ) ;
#55879=FILL_AREA_STYLE_COLOUR ( '', #48556 ) ;
#55882=CARTESIAN_POINT ( 'NONE',  ( 6.000000000000017764, 16.44305403005404287, -2.635024667321593109E-15 ) ) ;
#55884=EDGE_LOOP ( 'NONE', ( #63252, #49947, #6603, #56032 ) ) ;
#55886=ORIENTED_EDGE ( 'NONE', *, *, #59422, .T. ) ;
#55890=SURFACE_STYLE_USAGE ( .BOTH. , #33400 ) ;
#55895=CARTESIAN_POINT ( 'NONE',  ( 4.000000000000030198, 34.36176364315826248, 80.00402776293826435 ) ) ;
#55898=CARTESIAN_POINT ( 'NONE',  ( 22.99999999999995026, 5.000000000000000000, -32.00402776293824303 ) ) ;
#55904=FILL_AREA_STYLE_COLOUR ( '', #53999 ) ;
#55915=UNCERTAINTY_MEASURE_WITH_UNIT (LENGTH_MEASURE( 1.000000000000000082E-05 ), #24364, 'distance_accuracy_value', 'NONE');
#55916=DIRECTION ( 'NONE',  ( -1.000000000000000000, 0.000000000000000000, 0.000000000000000000 ) ) ;
#55939=DIRECTION ( 'NONE',  ( 0.000000000000000000, 0.000000000000000000, 1.000000000000000000 ) ) ;
#55945=PRESENTATION_STYLE_ASSIGNMENT (( #23584 ) ) ;
#55957=ORIENTED_EDGE ( 'NONE', *, *, #37095, .T. ) ;
#55986=FILL_AREA_STYLE ('',( #50724 ) ) ;
#55992=PRESENTATION_STYLE_ASSIGNMENT (( #45499 ) ) ;
#55999=SURFACE_SIDE_STYLE ('',( #50738 ) ) ;
#56002=VERTEX_POINT ( 'NONE', #63829 ) ;
#56008=TOROIDAL_SURFACE ( 'NONE', #54844, 2.000000000000000000, 1.000000000000000000 ) ;
#56011=EDGE_LOOP ( 'NONE', ( #35384, #21786, #41094, #69462 ) ) ;
#56024=AXIS2_PLACEMENT_3D ( 'NONE', #63083, #64118, #36749 ) ;
#56032=ORIENTED_EDGE ( 'NONE', *, *, #48246, .F. ) ;
#56034=COLOUR_RGB ( '', 0.09019608, 0.27058824, 0.51372549) ;
#56060=CARTESIAN_POINT ( 'NONE',  ( 2.000000000000008438, 26.00000000000000355, -27.50000000000000355 ) ) ;
#56069=EDGE_CURVE ( 'NONE', #51444, #44068, #39282, .T. ) ;
#56074=DIRECTION ( 'NONE',  ( 0.000000000000000000, -1.000000000000000000, 0.000000000000000000 ) ) ;
#56076=ORIENTED_EDGE ( 'NONE', *, *, #9407, .F. ) ;
#56079=SURFACE_SIDE_STYLE ('',( #29701 ) ) ;
#56083=DIRECTION ( 'NONE',  ( -1.000000000000000000, -0.000000000000000000, 0.000000000000000000 ) ) ;
#56084=AXIS2_PLACEMENT_3D ( 'NONE', #18302, #23911, #8084 ) ;
#56087=COLOUR_RGB ( '', 0.08235294, 0.09019608, 0.10196078) ;
#56091=STYLED_ITEM ( 'NONE', ( #50897 ), #15826 ) ;
#56102=CIRCLE ( 'NONE', #40414, 19.99999999999998934 ) ;
#56104=CARTESIAN_POINT ( 'NONE',  ( 3.000000000000030198, 43.00000000000000000, 89.00000000000000000 ) ) ;
#56108=( NAMED_UNIT ( * ) SI_UNIT ( $, .STERADIAN. ) SOLID_ANGLE_UNIT ( ) );
#56110=MECHANICAL_DESIGN_GEOMETRIC_PRESENTATION_REPRESENTATION('',(#54996),#34775);
#56116=SURFACE_SIDE_STYLE ('',( #23766 ) ) ;
#56119=SURFACE_STYLE_USAGE ( .BOTH. , #50522 ) ;
#56136=STYLED_ITEM ( 'NONE', ( #57287 ), #69261 ) ;
#56140=FILL_AREA_STYLE_COLOUR ( '', #20858 ) ;
#56144=EDGE_CURVE ( 'NONE', #31434, #35184, #14118, .T. ) ;
#56146=MECHANICAL_DESIGN_GEOMETRIC_PRESENTATION_REPRESENTATION('',(#22467),#43849);
#56150=CARTESIAN_POINT ( 'NONE',  ( 27.99999999999999645, 0.000000000000000000, 24.00402776293821816 ) ) ;
#56151=DIRECTION ( 'NONE',  ( -2.168404344971007882E-16, 0.000000000000000000, -1.000000000000000000 ) ) ;
#56153=EDGE_CURVE ( 'NONE', #48456, #66133, #44382, .T. ) ;
#56160=CIRCLE ( 'NONE', #22494, 14.00000000000000533 ) ;
#56165=DIRECTION ( 'NONE',  ( 0.000000000000000000, 1.000000000000000000, 0.000000000000000000 ) ) ;
#56177=PRESENTATION_STYLE_ASSIGNMENT (( #28389 ) ) ;
#56178=ORIENTED_EDGE ( 'NONE', *, *, #67119, .F. ) ;
#56180=DIRECTION ( 'NONE',  ( 0.000000000000000000, 1.000000000000000000, 0.000000000000000000 ) ) ;
#56186=AXIS2_PLACEMENT_3D ( 'NONE', #35516, #56960, #9486 ) ;
#56191=CARTESIAN_POINT ( 'NONE',  ( 1.709458476932651091E-14, -60.04052944165106709, 35.50000000000000000 ) ) ;
#56199=EDGE_CURVE ( 'NONE', #52477, #39971, #67953, .T. ) ;
#56201=PRESENTATION_STYLE_ASSIGNMENT (( #8028 ) ) ;
#56202=EDGE_CURVE ( 'NONE', #36334, #49504, #13997, .T. ) ;
#56214=EDGE_CURVE ( 'NONE', #10996, #15405, #25478, .T. ) ;
#56219=CIRCLE ( 'NONE', #50615, 1.000000000000000888 ) ;
#56225=EDGE_LOOP ( 'NONE', ( #56981, #39916, #66927, #5629 ) ) ;
#56226=DIRECTION ( 'NONE',  ( 0.000000000000000000, 1.000000000000000000, 0.000000000000000000 ) ) ;
#56246=SURFACE_STYLE_FILL_AREA ( #7030 ) ;
#56248=VECTOR ( 'NONE', #405, 1000.000000000000000 ) ;
#56249=DIRECTION ( 'NONE',  ( 1.982541115402068561E-16, 0.000000000000000000, -1.000000000000000000 ) ) ;
#56254=ORIENTED_EDGE ( 'NONE', *, *, #24301, .T. ) ;
#56256=TOROIDAL_SURFACE ( 'NONE', #32648, 2.000000000000000000, 1.000000000000000000 ) ;
#56258=MECHANICAL_DESIGN_GEOMETRIC_PRESENTATION_REPRESENTATION('',(#59666),#1166);
#56265=CARTESIAN_POINT ( 'NONE',  ( 32.00000000000000000, 42.00000000000000000, -75.00000000000001421 ) ) ;
#56268=COLOUR_RGB ( '', 0.09019608, 0.27058824, 0.51372549) ;
#56284=EDGE_LOOP ( 'NONE', ( #32435, #8544, #58075, #18971, #50933, #16533, #40709, #25234 ) ) ;
#56285=EDGE_CURVE ( 'NONE', #22594, #5489, #51070, .T. ) ;
#56290=ORIENTED_EDGE ( 'NONE', *, *, #28312, .F. ) ;
#56294=ADVANCED_FACE ( 'NONE', ( #69108 ), #35362, .T. ) ;
#56311=EDGE_LOOP ( 'NONE', ( #14446, #18222, #1997, #49597 ) ) ;
#56317=ORIENTED_EDGE ( 'NONE', *, *, #58695, .T. ) ;
#56320=VECTOR ( 'NONE', #26248, 1000.000000000000000 ) ;
#56322=( LENGTH_UNIT ( ) NAMED_UNIT ( * ) SI_UNIT ( .MILLI., .METRE. ) );
#56324=CARTESIAN_POINT ( 'NONE',  ( 22.29422224269976027, 26.17759303819800820, -27.50000000000001066 ) ) ;
#56327=LINE ( 'NONE', #62312, #53879 ) ;
#56331=CYLINDRICAL_SURFACE ( 'NONE', #24041, 0.9999999999999995559 ) ;
#56336=CARTESIAN_POINT ( 'NONE',  ( 27.00000000000001776, 14.00000000000000000, -60.00402776293827145 ) ) ;
#56337=LINE ( 'NONE', #62643, #6673 ) ;
#56341=VECTOR ( 'NONE', #34428, 1000.000000000000227 ) ;
#56345=ORIENTED_EDGE ( 'NONE', *, *, #16332, .F. ) ;
#56346=AXIS2_PLACEMENT_3D ( 'NONE', #62682, #24362, #56749 ) ;
#56347=( GEOMETRIC_REPRESENTATION_CONTEXT ( 3 ) GLOBAL_UNCERTAINTY_ASSIGNED_CONTEXT ( ( #16558 ) ) GLOBAL_UNIT_ASSIGNED_CONTEXT ( ( #802, #64899, #65249 ) ) REPRESENTATION_CONTEXT ( 'NONE', 'WORKASPACE' ) );
#56349=CARTESIAN_POINT ( 'NONE',  ( 6.000000000000017764, -35.45414562583513884, -57.63767942241966580 ) ) ;
#56353=MECHANICAL_DESIGN_GEOMETRIC_PRESENTATION_REPRESENTATION('',(#9076),#46163);
#56354=ORIENTED_EDGE ( 'NONE', *, *, #12298, .F. ) ;
#56361=EDGE_LOOP ( 'NONE', ( #1999, #14691, #46470, #1444 ) ) ;
#56364=DIRECTION ( 'NONE',  ( 0.000000000000000000, 0.000000000000000000, 1.000000000000000000 ) ) ;
#56375=DIRECTION ( 'NONE',  ( 0.000000000000000000, 0.000000000000000000, 1.000000000000000000 ) ) ;
#56386=DIRECTION ( 'NONE',  ( 0.000000000000000000, -0.000000000000000000, 1.000000000000000000 ) ) ;
#56423=EDGE_CURVE ( 'NONE', #50024, #11058, #41045, .T. ) ;
#56441=COLOUR_RGB ( '', 0.31764706, 0.68627451, 0.89019608) ;
#56444=VECTOR ( 'NONE', #21897, 1000.000000000000000 ) ;
#56445=ORIENTED_EDGE ( 'NONE', *, *, #12392, .T. ) ;
#56456=( GEOMETRIC_REPRESENTATION_CONTEXT ( 3 ) GLOBAL_UNCERTAINTY_ASSIGNED_CONTEXT ( ( #38528 ) ) GLOBAL_UNIT_ASSIGNED_CONTEXT ( ( #6453, #53619, #5407 ) ) REPRESENTATION_CONTEXT ( 'NONE', 'WORKASPACE' ) );
#56462=CARTESIAN_POINT ( 'NONE',  ( 2.999999999999993339, 5.000000000000000000, 24.00402776293822882 ) ) ;
#56472=SURFACE_SIDE_STYLE ('',( #4031 ) ) ;
#56478=ADVANCED_FACE ( 'NONE', ( #34229 ), #55683, .F. ) ;
#56479=DIRECTION ( 'NONE',  ( 0.000000000000000000, 0.000000000000000000, -1.000000000000000000 ) ) ;
#56481=VERTEX_POINT ( 'NONE', #41613 ) ;
#56484=CARTESIAN_POINT ( 'NONE',  ( 27.00000000000001776, 42.00000000000000000, 34.49999999999999289 ) ) ;
#56507=DIRECTION ( 'NONE',  ( 0.000000000000000000, 0.000000000000000000, 1.000000000000000000 ) ) ;
#56516=STYLED_ITEM ( 'NONE', ( #14486 ), #30408 ) ;
#56517=( NAMED_UNIT ( * ) PLANE_ANGLE_UNIT ( ) SI_UNIT ( $, .RADIAN. ) );
#56522=CARTESIAN_POINT ( 'NONE',  ( 36.00000000000002842, 5.000000000000000000, 29.00402776293825724 ) ) ;
#56526=EDGE_CURVE ( 'NONE', #30954, #26439, #68676, .T. ) ;
#56531=DIRECTION ( 'NONE',  ( 1.000000000000000000, 0.000000000000000000, 0.000000000000000000 ) ) ;
#56534=EDGE_CURVE ( 'NONE', #52976, #50401, #69095, .T. ) ;
#56546=DIRECTION ( 'NONE',  ( -0.000000000000000000, 0.000000000000000000, 1.000000000000000000 ) ) ;
#56549=EDGE_CURVE ( 'NONE', #9757, #21109, #41981, .T. ) ;
#56555=FACE_OUTER_BOUND ( 'NONE', #50031, .T. ) ;
#56560=VERTEX_POINT ( 'NONE', #19429 ) ;
#56563=DIRECTION ( 'NONE',  ( 0.000000000000000000, 0.000000000000000000, -1.000000000000000000 ) ) ;
#56577=ORIENTED_EDGE ( 'NONE', *, *, #23293, .F. ) ;
#56587=CARTESIAN_POINT ( 'NONE',  ( 6.000000000000017764, 14.00000000000000533, -35.50000000000000000 ) ) ;
#56593=VERTEX_POINT ( 'NONE', #35973 ) ;
#56601=SURFACE_STYLE_FILL_AREA ( #7709 ) ;
#56607=CARTESIAN_POINT ( 'NONE',  ( 33.00000000000000711, 14.00000000000000000, -36.50000000000000000 ) ) ;
#56621=CARTESIAN_POINT ( 'NONE',  ( 57.00000000000000000, 0.000000000000000000, -60.00402776293827145 ) ) ;
#56631=DIRECTION ( 'NONE',  ( 1.000000000000000000, 0.000000000000000000, 0.000000000000000000 ) ) ;
#56633=CARTESIAN_POINT ( 'NONE',  ( 8.000000000000030198, 5.000000000000000000, 29.00402776293826079 ) ) ;
#56637=ORIENTED_EDGE ( 'NONE', *, *, #49481, .F. ) ;
#56643=CARTESIAN_POINT ( 'NONE',  ( 108.3664351561509278, 0.000000000000000000, 18.43563588791581509 ) ) ;
#56644=ORIENTED_EDGE ( 'NONE', *, *, #6820, .F. ) ;
#56646=CYLINDRICAL_SURFACE ( 'NONE', #25388, 113.0000000000030127 ) ;
#56656=CARTESIAN_POINT ( 'NONE',  ( 2.999999999999996447, 5.000000000000000000, -37.00402776293829277 ) ) ;
#56657=UNCERTAINTY_MEASURE_WITH_UNIT (LENGTH_MEASURE( 1.000000000000000082E-05 ), #59207, 'distance_accuracy_value', 'NONE');
#56661=ORIENTED_EDGE ( 'NONE', *, *, #41018, .T. ) ;
#56665=AXIS2_PLACEMENT_3D ( 'NONE', #49808, #22721, #64918 ) ;
#56672=UNCERTAINTY_MEASURE_WITH_UNIT (LENGTH_MEASURE( 1.000000000000000082E-05 ), #53806, 'distance_accuracy_value', 'NONE');
#56682=( GEOMETRIC_REPRESENTATION_CONTEXT ( 3 ) GLOBAL_UNCERTAINTY_ASSIGNED_CONTEXT ( ( #2432 ) ) GLOBAL_UNIT_ASSIGNED_CONTEXT ( ( #24097, #7913, #61700 ) ) REPRESENTATION_CONTEXT ( 'NONE', 'WORKASPACE' ) );
#56683=ORIENTED_EDGE ( 'NONE', *, *, #4864, .F. ) ;
#56688=EDGE_CURVE ( 'NONE', #45031, #31418, #47967, .T. ) ;
#56689=FILL_AREA_STYLE_COLOUR ( '', #44808 ) ;
#56691=CYLINDRICAL_SURFACE ( 'NONE', #28747, 1.000000000000000888 ) ;
#56692=ORIENTED_EDGE ( 'NONE', *, *, #21264, .T. ) ;
#56695=DIRECTION ( 'NONE',  ( -0.000000000000000000, -1.000000000000000000, -0.000000000000000000 ) ) ;
#56696=COLOUR_RGB ( '', 0.66274510, 0.83137255, 0.94901961) ;
#56699=SURFACE_STYLE_USAGE ( .BOTH. , #40541 ) ;
#56709=AXIS2_PLACEMENT_3D ( 'NONE', #32201, #3067, #59252 ) ;
#56734=FILL_AREA_STYLE_COLOUR ( '', #1161 ) ;
#56735=DIRECTION ( 'NONE',  ( 0.3361263392814427542, -0.000000000000000000, 0.9418169057949938860 ) ) ;
#56749=DIRECTION ( 'NONE',  ( 1.000000000000000000, 0.000000000000000000, 0.000000000000000000 ) ) ;
#56751=ORIENTED_EDGE ( 'NONE', *, *, #667, .T. ) ;
#56756=DIRECTION ( 'NONE',  ( 0.000000000000000000, 1.000000000000000000, 0.000000000000000000 ) ) ;
#56757=AXIS2_PLACEMENT_3D ( 'NONE', #207, #47850, #32618 ) ;
#56758=CIRCLE ( 'NONE', #490, 1.000000000000000888 ) ;
#56767=CARTESIAN_POINT ( 'NONE',  ( 28.00000000000002842, 37.76051491742381216, 89.34202014332566932 ) ) ;
#56774=DIRECTION ( 'NONE',  ( 1.000000000000000000, 0.000000000000000000, 0.000000000000000000 ) ) ;
#56777=SPHERICAL_SURFACE ( 'NONE', #50476, 1.000000000000000000 ) ;
#56789=( NAMED_UNIT ( * ) SI_UNIT ( $, .STERADIAN. ) SOLID_ANGLE_UNIT ( ) );
#56805=COLOUR_RGB ( '', 0.40784314, 0.44705882, 0.49803922) ;
#56808=CARTESIAN_POINT ( 'NONE',  ( 32.00000000000001421, -60.04052944165106709, -35.50000000000000000 ) ) ;
#56811=VERTEX_POINT ( 'NONE', #49643 ) ;
#56814=AXIS2_PLACEMENT_3D ( 'NONE', #24785, #45940, #23404 ) ;
#56815=ORIENTED_EDGE ( 'NONE', *, *, #68416, .F. ) ;
#56824=DIRECTION ( 'NONE',  ( -1.000000000000000000, 0.000000000000000000, 0.000000000000000000 ) ) ;
#56825=EDGE_LOOP ( 'NONE', ( #56254, #312, #2819, #9788 ) ) ;
#56828=( NAMED_UNIT ( * ) PLANE_ANGLE_UNIT ( ) SI_UNIT ( $, .RADIAN. ) );
#56831=AXIS2_PLACEMENT_3D ( 'NONE', #1043, #54234, #65489 ) ;
#56835=VERTEX_POINT ( 'NONE', #33789 ) ;
#56837=FACE_OUTER_BOUND ( 'NONE', #28431, .T. ) ;
#56838=VERTEX_POINT ( 'NONE', #66506 ) ;
#56856=DIRECTION ( 'NONE',  ( 1.000000000000000000, -0.000000000000000000, 0.000000000000000000 ) ) ;
#56863=AXIS2_PLACEMENT_3D ( 'NONE', #54807, #6617, #60777 ) ;
#56868=ADVANCED_FACE ( 'NONE', ( #18327 ), #33185, .F. ) ;
#56871=CYLINDRICAL_SURFACE ( 'NONE', #17940, 2.499999999999998668 ) ;
#56880=PLANE ( 'NONE',  #43873 ) ;
#56883=FILL_AREA_STYLE_COLOUR ( '', #1229 ) ;
#56887=VERTEX_POINT ( 'NONE', #19340 ) ;
#56891=PLANE ( 'NONE',  #61114 ) ;
#56896=DIRECTION ( 'NONE',  ( 0.000000000000000000, 0.000000000000000000, 1.000000000000000000 ) ) ;
#56900=( GEOMETRIC_REPRESENTATION_CONTEXT ( 3 ) GLOBAL_UNCERTAINTY_ASSIGNED_CONTEXT ( ( #59500 ) ) GLOBAL_UNIT_ASSIGNED_CONTEXT ( ( #18231, #60431, #18897 ) ) REPRESENTATION_CONTEXT ( 'NONE', 'WORKASPACE' ) );
#56901=VERTEX_POINT ( 'NONE', #41527 ) ;
#56909=DIRECTION ( 'NONE',  ( 1.000000000000000000, -1.734723475976812222E-15, -1.926605602187847311E-15 ) ) ;
#56911=CIRCLE ( 'NONE', #36736, 16.00000000000000000 ) ;
#56912=CARTESIAN_POINT ( 'NONE',  ( 1.000000000000000000, -60.04052944165106709, -35.50000000000000000 ) ) ;
#56922=DIRECTION ( 'NONE',  ( 1.000000000000000000, 0.000000000000000000, 0.000000000000000000 ) ) ;
#56924=MECHANICAL_DESIGN_GEOMETRIC_PRESENTATION_REPRESENTATION('',(#61419),#64810);
#56929=ORIENTED_EDGE ( 'NONE', *, *, #9081, .F. ) ;
#56943=CARTESIAN_POINT ( 'NONE',  ( 2.999999999999994671, 5.000000000000000000, -24.00402776293822527 ) ) ;
#56944=SURFACE_STYLE_FILL_AREA ( #35501 ) ;
#56951=B_SPLINE_CURVE_WITH_KNOTS ( 'NONE', 3,
 ( #39717, #40075, #61463, #8386, #23494, #66416, #18233, #17565, #43476, #48383, #52348, #26845 ),
 .UNSPECIFIED., .F., .F.,
 ( 4, 2, 2, 2, 2, 4 ),
 ( 0.004228563614865340353, 0.004757664776855344800, 0.005286765938845350114, 0.005551316519840357976, 0.005815867100835366704, 0.006344968262825391968 ),
 .UNSPECIFIED. ) ;
#56957=CARTESIAN_POINT ( 'NONE',  ( 16.00000000000001776, 42.00000000000000000, 34.68999999999999062 ) ) ;
#56960=DIRECTION ( 'NONE',  ( 0.000000000000000000, 0.3420201433256693790, -0.9396926207859082059 ) ) ;
#56969=ORIENTED_EDGE ( 'NONE', *, *, #39727, .F. ) ;
#56978=ORIENTED_EDGE ( 'NONE', *, *, #29866, .T. ) ;
#56981=ORIENTED_EDGE ( 'NONE', *, *, #53319, .T. ) ;
#56984=ORIENTED_EDGE ( 'NONE', *, *, #35447, .F. ) ;
#56988=SURFACE_SIDE_STYLE ('',( #19700 ) ) ;
#56996=DIRECTION ( 'NONE',  ( 1.000000000000000000, 0.000000000000000000, 0.000000000000000000 ) ) ;
#56999=PLANE ( 'NONE',  #35121 ) ;
#57003=ORIENTED_EDGE ( 'NONE', *, *, #42088, .F. ) ;
#57021=ORIENTED_EDGE ( 'NONE', *, *, #1698, .F. ) ;
#57030=SURFACE_STYLE_USAGE ( .BOTH. , #45491 ) ;
#57032=LINE ( 'NONE', #18711, #4442 ) ;
#57035=ADVANCED_FACE ( 'NONE', ( #9518 ), #56646, .T. ) ;
#57036=FILL_AREA_STYLE_COLOUR ( '', #18429 ) ;
#57046=DIRECTION ( 'NONE',  ( 0.000000000000000000, 0.000000000000000000, -1.000000000000000000 ) ) ;
#57051=SURFACE_SIDE_STYLE ('',( #35613 ) ) ;
#57055=( NAMED_UNIT ( * ) SI_UNIT ( $, .STERADIAN. ) SOLID_ANGLE_UNIT ( ) );
#57059=ORIENTED_EDGE ( 'NONE', *, *, #67266, .F. ) ;
#57068=LINE ( 'NONE', #46920, #22960 ) ;
#57081=ORIENTED_EDGE ( 'NONE', *, *, #26347, .F. ) ;
#57086=SURFACE_SIDE_STYLE ('',( #68348 ) ) ;
#57088=DIRECTION ( 'NONE',  ( -0.000000000000000000, -1.000000000000000000, -0.000000000000000000 ) ) ;
#57089=ORIENTED_EDGE ( 'NONE', *, *, #61237, .F. ) ;
#57095=SURFACE_STYLE_USAGE ( .BOTH. , #47999 ) ;
#57096=CARTESIAN_POINT ( 'NONE',  ( 23.49527607712185073, 27.44009427658185984, 27.19000446309344809 ) ) ;
#57098=SURFACE_SIDE_STYLE ('',( #35660 ) ) ;
#57111=EDGE_CURVE ( 'NONE', #52223, #67044, #69185, .T. ) ;
#57113=DIRECTION ( 'NONE',  ( 0.000000000000000000, 0.000000000000000000, -1.000000000000000000 ) ) ;
#57114=ORIENTED_EDGE ( 'NONE', *, *, #50920, .F. ) ;
#57117=AXIS2_PLACEMENT_3D ( 'NONE', #21471, #20795, #52815 ) ;
#57124=CARTESIAN_POINT ( 'NONE',  ( 96.10348817448819148, 5.000000000000000000, 27.38099488609881149 ) ) ;
#57140=( LENGTH_UNIT ( ) NAMED_UNIT ( * ) SI_UNIT ( .MILLI., .METRE. ) );
#57141=EDGE_CURVE ( 'NONE', #10038, #29168, #24230, .T. ) ;
#57142=ORIENTED_EDGE ( 'NONE', *, *, #24584, .F. ) ;
#57146=ORIENTED_EDGE ( 'NONE', *, *, #26347, .T. ) ;
#57147=SURFACE_STYLE_FILL_AREA ( #51201 ) ;
#57148=DIRECTION ( 'NONE',  ( 0.000000000000000000, 0.000000000000000000, 1.000000000000000000 ) ) ;
#57150=FILL_AREA_STYLE ('',( #36793 ) ) ;
#57159=UNCERTAINTY_MEASURE_WITH_UNIT (LENGTH_MEASURE( 1.000000000000000082E-05 ), #57173, 'distance_accuracy_value', 'NONE');
#57161=( LENGTH_UNIT ( ) NAMED_UNIT ( * ) SI_UNIT ( .MILLI., .METRE. ) );
#57171=CARTESIAN_POINT ( 'NONE',  ( 10.00000000000001776, 17.78868675966041835, -1.300977106640437060E-15 ) ) ;
#57173=( LENGTH_UNIT ( ) NAMED_UNIT ( * ) SI_UNIT ( .MILLI., .METRE. ) );
#57194=CARTESIAN_POINT ( 'NONE',  ( 30.99999999999999289, 5.000000000000000000, -24.00402776293822171 ) ) ;
#57195=( NAMED_UNIT ( * ) SI_UNIT ( $, .STERADIAN. ) SOLID_ANGLE_UNIT ( ) );
#57199=CIRCLE ( 'NONE', #54969, 4.999999999999997335 ) ;
#57213=( GEOMETRIC_REPRESENTATION_CONTEXT ( 3 ) GLOBAL_UNCERTAINTY_ASSIGNED_CONTEXT ( ( #24981 ) ) GLOBAL_UNIT_ASSIGNED_CONTEXT ( ( #50719, #1058, #18371 ) ) REPRESENTATION_CONTEXT ( 'NONE', 'WORKASPACE' ) );
#57214=PRESENTATION_STYLE_ASSIGNMENT (( #35772 ) ) ;
#57222=FILL_AREA_STYLE_COLOUR ( '', #45082 ) ;
#57226=( NAMED_UNIT ( * ) PLANE_ANGLE_UNIT ( ) SI_UNIT ( $, .RADIAN. ) );
#57229=VERTEX_POINT ( 'NONE', #60767 ) ;
#57243=EDGE_CURVE ( 'NONE', #16376, #8059, #22124, .T. ) ;
#57247=PLANE ( 'NONE',  #31271 ) ;
#57251=ORIENTED_EDGE ( 'NONE', *, *, #21523, .T. ) ;
#57259=AXIS2_PLACEMENT_3D ( 'NONE', #64942, #43893, #7262 ) ;
#57264=CARTESIAN_POINT ( 'NONE',  ( 27.99999999999999645, 0.000000000000000000, -72.00402776293822171 ) ) ;
#57269=FILL_AREA_STYLE_COLOUR ( '', #50053 ) ;
#57273=ORIENTED_EDGE ( 'NONE', *, *, #10042, .T. ) ;
#57287=PRESENTATION_STYLE_ASSIGNMENT (( #9471 ) ) ;
#57305=FILL_AREA_STYLE_COLOUR ( '', #23540 ) ;
#57306=MECHANICAL_DESIGN_GEOMETRIC_PRESENTATION_REPRESENTATION('',(#56136),#31484);
#57313=AXIS2_PLACEMENT_3D ( 'NONE', #67504, #3080, #62225 ) ;
#57316=DIRECTION ( 'NONE',  ( 0.000000000000000000, -1.000000000000000000, 0.000000000000000000 ) ) ;
#57320=DIRECTION ( 'NONE',  ( 0.000000000000000000, 0.000000000000000000, 1.000000000000000000 ) ) ;
#57322=ORIENTED_EDGE ( 'NONE', *, *, #45068, .T. ) ;
#57328=( GEOMETRIC_REPRESENTATION_CONTEXT ( 3 ) GLOBAL_UNCERTAINTY_ASSIGNED_CONTEXT ( ( #6037 ) ) GLOBAL_UNIT_ASSIGNED_CONTEXT ( ( #21068, #15817, #37298 ) ) REPRESENTATION_CONTEXT ( 'NONE', 'WORKASPACE' ) );
#57330=( NAMED_UNIT ( * ) PLANE_ANGLE_UNIT ( ) SI_UNIT ( $, .RADIAN. ) );
#57335=AXIS2_PLACEMENT_3D ( 'NONE', #53349, #10774, #5129 ) ;
#57347=STYLED_ITEM ( 'NONE', ( #36612 ), #17422 ) ;
#57356=ORIENTED_EDGE ( 'NONE', *, *, #64224, .T. ) ;
#57362=DIRECTION ( 'NONE',  ( -1.982541115402069054E-16, -0.000000000000000000, -1.000000000000000000 ) ) ;
#57372=VERTEX_POINT ( 'NONE', #29814 ) ;
#57373=CARTESIAN_POINT ( 'NONE',  ( 1.000000000000000000, 42.00000000000000000, 79.00402776293826435 ) ) ;
#57375=( NAMED_UNIT ( * ) PLANE_ANGLE_UNIT ( ) SI_UNIT ( $, .RADIAN. ) );
#57378=MECHANICAL_DESIGN_GEOMETRIC_PRESENTATION_REPRESENTATION('',(#51767),#67450);
#57379=( GEOMETRIC_REPRESENTATION_CONTEXT ( 3 ) GLOBAL_UNCERTAINTY_ASSIGNED_CONTEXT ( ( #61566 ) ) GLOBAL_UNIT_ASSIGNED_CONTEXT ( ( #18940, #25279, #35143 ) ) REPRESENTATION_CONTEXT ( 'NONE', 'WORKASPACE' ) );
#57397=STYLED_ITEM ( 'NONE', ( #51971 ), #52832 ) ;
#57403=EDGE_LOOP ( 'NONE', ( #57858, #22227, #51432 ) ) ;
#57407=LINE ( 'NONE', #56349, #67460 ) ;
#57418=FACE_OUTER_BOUND ( 'NONE', #27053, .T. ) ;
#57429=UNCERTAINTY_MEASURE_WITH_UNIT (LENGTH_MEASURE( 1.000000000000000082E-05 ), #66831, 'distance_accuracy_value', 'NONE');
#57444=CARTESIAN_POINT ( 'NONE',  ( 32.00000000000000000, 42.24290439782119932, 45.14575947096723496 ) ) ;
#57446=EDGE_CURVE ( 'NONE', #62287, #1278, #50019, .T. ) ;
#57469=ORIENTED_EDGE ( 'NONE', *, *, #66827, .T. ) ;
#57480=FACE_OUTER_BOUND ( 'NONE', #56011, .T. ) ;
#57489=SURFACE_STYLE_USAGE ( .BOTH. , #24763 ) ;
#57495=STYLED_ITEM ( 'NONE', ( #37437 ), #18292 ) ;
#57505=AXIS2_PLACEMENT_3D ( 'NONE', #28424, #29490, #55535 ) ;
#57506=EDGE_LOOP ( 'NONE', ( #8366, #58430, #6294, #55851 ) ) ;
#57512=DIRECTION ( 'NONE',  ( 0.000000000000000000, 0.000000000000000000, -1.000000000000000000 ) ) ;
#57515=VERTEX_POINT ( 'NONE', #48735 ) ;
#57521=SURFACE_STYLE_USAGE ( .BOTH. , #56472 ) ;
#57522=EDGE_CURVE ( 'NONE', #61983, #11976, #27884, .T. ) ;
#57524=DIRECTION ( 'NONE',  ( -0.000000000000000000, -1.000000000000000000, -0.000000000000000000 ) ) ;
#57555=STYLED_ITEM ( 'NONE', ( #22670 ), #25491 ) ;
#57559=CIRCLE ( 'NONE', #36136, 14.00000000000000533 ) ;
#57569=LINE ( 'NONE', #45671, #35918 ) ;
#57571=ADVANCED_FACE ( 'NONE', ( #1112 ), #53288, .F. ) ;
#57573=EDGE_CURVE ( 'NONE', #65761, #45031, #51128, .T. ) ;
#57577=ORIENTED_EDGE ( 'NONE', *, *, #60947, .F. ) ;
#57578=( NAMED_UNIT ( * ) PLANE_ANGLE_UNIT ( ) SI_UNIT ( $, .RADIAN. ) );
#57584=CARTESIAN_POINT ( 'NONE',  ( 22.70977904271739334, 24.88203576750890988, -27.31717988970180500 ) ) ;
#57587=EDGE_LOOP ( 'NONE', ( #29336, #47964, #69123, #30416 ) ) ;
#57589=AXIS2_PLACEMENT_3D ( 'NONE', #48470, #49149, #17814 ) ;
#57591=FILL_AREA_STYLE_COLOUR ( '', #32001 ) ;
#57592=CIRCLE ( 'NONE', #67735, 5.000000000000000888 ) ;
#57602=PRESENTATION_STYLE_ASSIGNMENT (( #19948 ) ) ;
#57603=SURFACE_SIDE_STYLE ('',( #42177 ) ) ;
#57609=FILL_AREA_STYLE ('',( #3035 ) ) ;
#57626=CARTESIAN_POINT ( 'NONE',  ( 35.99999999999999289, 0.000000000000000000, -72.00402776293825013 ) ) ;
#57629=FACE_OUTER_BOUND ( 'NONE', #9199, .T. ) ;
#57635=( GEOMETRIC_REPRESENTATION_CONTEXT ( 3 ) GLOBAL_UNCERTAINTY_ASSIGNED_CONTEXT ( ( #12412 ) ) GLOBAL_UNIT_ASSIGNED_CONTEXT ( ( #24972, #57330, #58369 ) ) REPRESENTATION_CONTEXT ( 'NONE', 'WORKASPACE' ) );
#57636=FILL_AREA_STYLE ('',( #46792 ) ) ;
#57642=FILL_AREA_STYLE ('',( #30530 ) ) ;
#57652=VECTOR ( 'NONE', #39235, 1000.000000000000000 ) ;
#57655=DIRECTION ( 'NONE',  ( -1.000000000000000000, 0.000000000000000000, 0.000000000000000000 ) ) ;
#57674=FILL_AREA_STYLE ('',( #36249 ) ) ;
#57683=AXIS2_PLACEMENT_3D ( 'NONE', #14577, #18803, #13520 ) ;
#57685=( LENGTH_UNIT ( ) NAMED_UNIT ( * ) SI_UNIT ( .MILLI., .METRE. ) );
#57692=ORIENTED_EDGE ( 'NONE', *, *, #28505, .F. ) ;
#57721=CARTESIAN_POINT ( 'NONE',  ( 8.000000000000035527, 0.000000000000000000, -77.00402776293825013 ) ) ;
#57725=ORIENTED_EDGE ( 'NONE', *, *, #25475, .F. ) ;
#57727=DIRECTION ( 'NONE',  ( -0.000000000000000000, -1.000000000000000000, 0.000000000000000000 ) ) ;
#57729=STYLED_ITEM ( 'NONE', ( #18878 ), #48321 ) ;
#57730=AXIS2_PLACEMENT_3D ( 'NONE', #55846, #56531, #50926 ) ;
#57732=DIRECTION ( 'NONE',  ( -0.000000000000000000, -1.000000000000000000, -0.000000000000000000 ) ) ;
#57733=VERTEX_POINT ( 'NONE', #51822 ) ;
#57735=( LENGTH_UNIT ( ) NAMED_UNIT ( * ) SI_UNIT ( .MILLI., .METRE. ) );
#57742=DIRECTION ( 'NONE',  ( -0.000000000000000000, 0.3420201433256630508, 0.9396926207859105373 ) ) ;
#57744=CARTESIAN_POINT ( 'NONE',  ( 11.00000000000001599, 42.74314482547740113, 27.71473342867655987 ) ) ;
#57746=ORIENTED_EDGE ( 'NONE', *, *, #46261, .F. ) ;
#57753=STYLED_ITEM ( 'NONE', ( #8543 ), #30249 ) ;
#57757=CARTESIAN_POINT ( 'NONE',  ( 26.00000000000001776, 15.00000000000000000, -29.68999999999999417 ) ) ;
#57760=COLOUR_RGB ( '', 0.09019608, 0.27058824, 0.51372549) ;
#57764=COLOUR_RGB ( '', 0.72549020, 0.75294118, 0.79215686) ;
#57768=CARTESIAN_POINT ( 'NONE',  ( 57.00000000000000000, 0.000000000000000000, 79.00402776293826435 ) ) ;
#57769=EDGE_CURVE ( 'NONE', #33888, #50928, #50062, .T. ) ;
#57773=EDGE_LOOP ( 'NONE', ( #14119, #14243, #25465, #9942 ) ) ;
#57774=LINE ( 'NONE', #20829, #26776 ) ;
#57776=EDGE_LOOP ( 'NONE', ( #18851, #41833, #62624, #30658 ) ) ;
#57778=DIRECTION ( 'NONE',  ( 0.000000000000000000, 0.000000000000000000, -1.000000000000000000 ) ) ;
#57797=CARTESIAN_POINT ( 'NONE',  ( 10.00000000000001954, 43.00000000000000000, 45.61250543006183733 ) ) ;
#57807=( NAMED_UNIT ( * ) SI_UNIT ( $, .STERADIAN. ) SOLID_ANGLE_UNIT ( ) );
#57810=( NAMED_UNIT ( * ) SI_UNIT ( $, .STERADIAN. ) SOLID_ANGLE_UNIT ( ) );
#57832=CARTESIAN_POINT ( 'NONE',  ( 29.00000000000000000, 42.00000000000000000, -80.00402776293826435 ) ) ;
#57836=FILL_AREA_STYLE_COLOUR ( '', #66851 ) ;
#57837=AXIS2_PLACEMENT_3D ( 'NONE', #39190, #44142, #1460 ) ;
#57840=PLANE ( 'NONE',  #9610 ) ;
#57850=AXIS2_PLACEMENT_3D ( 'NONE', #9604, #56735, #35629 ) ;
#57855=CARTESIAN_POINT ( 'NONE',  ( 30.99999999999999289, 5.000000000000000000, -24.00402776293822171 ) ) ;
#57858=ORIENTED_EDGE ( 'NONE', *, *, #12007, .T. ) ;
#57866=CARTESIAN_POINT ( 'NONE',  ( 10.00000000000001954, 42.00000000000000000, -35.50000000000000000 ) ) ;
#57872=VERTEX_POINT ( 'NONE', #37059 ) ;
#57875=FILL_AREA_STYLE ('',( #15658 ) ) ;
#57881=ORIENTED_EDGE ( 'NONE', *, *, #28726, .T. ) ;
#57882=DIRECTION ( 'NONE',  ( 0.000000000000000000, 0.000000000000000000, 1.000000000000000000 ) ) ;
#57909=EDGE_CURVE ( 'NONE', #9284, #66764, #5094, .T. ) ;
#57919=FILL_AREA_STYLE ('',( #21289 ) ) ;
#57920=DIRECTION ( 'NONE',  ( 0.000000000000000000, 0.000000000000000000, 1.000000000000000000 ) ) ;
#57923=SURFACE_SIDE_STYLE ('',( #4066 ) ) ;
#57931=UNCERTAINTY_MEASURE_WITH_UNIT (LENGTH_MEASURE( 1.000000000000000082E-05 ), #35758, 'distance_accuracy_value', 'NONE');
#57943=VERTEX_POINT ( 'NONE', #33136 ) ;
#57953=SURFACE_SIDE_STYLE ('',( #10451 ) ) ;
#57967=DIRECTION ( 'NONE',  ( 0.000000000000000000, 0.000000000000000000, -1.000000000000000000 ) ) ;
#57968=( NAMED_UNIT ( * ) PLANE_ANGLE_UNIT ( ) SI_UNIT ( $, .RADIAN. ) );
#57978=PRESENTATION_STYLE_ASSIGNMENT (( #29116 ) ) ;
#57979=SURFACE_STYLE_USAGE ( .BOTH. , #10476 ) ;
#57983=CARTESIAN_POINT ( 'NONE',  ( 98.00000000000000000, 14.00000000000000000, 0.000000000000000000 ) ) ;
#57987=CARTESIAN_POINT ( 'NONE',  ( 4.000000000000002665, 42.00000000000000000, 0.000000000000000000 ) ) ;
#57992=ORIENTED_EDGE ( 'NONE', *, *, #40482, .T. ) ;
#58008=DIRECTION ( 'NONE',  ( 0.000000000000000000, 1.000000000000000000, -0.000000000000000000 ) ) ;
#58032=UNCERTAINTY_MEASURE_WITH_UNIT (LENGTH_MEASURE( 1.000000000000000082E-05 ), #51349, 'distance_accuracy_value', 'NONE');
#58033=FACE_OUTER_BOUND ( 'NONE', #10907, .T. ) ;
#58055=LINE ( 'NONE', #9862, #43557 ) ;
#58061=EDGE_LOOP ( 'NONE', ( #56290, #42253, #27170, #68010 ) ) ;
#58063=ORIENTED_EDGE ( 'NONE', *, *, #18505, .T. ) ;
#58069=UNCERTAINTY_MEASURE_WITH_UNIT (LENGTH_MEASURE( 1.000000000000000082E-05 ), #39270, 'distance_accuracy_value', 'NONE');
#58075=ORIENTED_EDGE ( 'NONE', *, *, #49255, .T. ) ;
#58079=PRESENTATION_STYLE_ASSIGNMENT (( #53803 ) ) ;
#58093=EDGE_CURVE ( 'NONE', #44784, #23681, #42226, .T. ) ;
#58098=DIRECTION ( 'NONE',  ( 1.000000000000000000, -9.122956858292678705E-34, -1.300977106640434891E-16 ) ) ;
#58108=LINE ( 'NONE', #57757, #41738 ) ;
#58143=ORIENTED_EDGE ( 'NONE', *, *, #32988, .F. ) ;
#58144=CARTESIAN_POINT ( 'NONE',  ( 31.14385391401492598, 43.00000000000000711, 45.61250543006183022 ) ) ;
#58145=DIRECTION ( 'NONE',  ( 1.000000000000000000, 0.000000000000000000, -1.300977106640434891E-16 ) ) ;
#58153=SURFACE_STYLE_FILL_AREA ( #21546 ) ;
#58165=COLOUR_RGB ( '', 0.40784314, 0.44705882, 0.49803922) ;
#58168=FILL_AREA_STYLE ('',( #14924 ) ) ;
#58171=( GEOMETRIC_REPRESENTATION_CONTEXT ( 3 ) GLOBAL_UNCERTAINTY_ASSIGNED_CONTEXT ( ( #58748 ) ) GLOBAL_UNIT_ASSIGNED_CONTEXT ( ( #25205, #18866, #29794 ) ) REPRESENTATION_CONTEXT ( 'NONE', 'WORKASPACE' ) );
#58172=CARTESIAN_POINT ( 'NONE',  ( 31.00000000000000355, 42.47058823529412308, -74.11764705882353610 ) ) ;
#58174=ORIENTED_EDGE ( 'NONE', *, *, #39727, .T. ) ;
#58186=DIRECTION ( 'NONE',  ( -0.000000000000000000, 0.000000000000000000, -1.000000000000000000 ) ) ;
#58189=DIRECTION ( 'NONE',  ( -8.673617379884040402E-17, 0.000000000000000000, -1.000000000000000000 ) ) ;
#58201=MECHANICAL_DESIGN_GEOMETRIC_PRESENTATION_REPRESENTATION('',(#51426),#62647);
#58205=FACE_OUTER_BOUND ( 'NONE', #16261, .T. ) ;
#58211=ORIENTED_EDGE ( 'NONE', *, *, #23434, .T. ) ;
#58219=CARTESIAN_POINT ( 'NONE',  ( 86.21825843581743243, 0.000000000000000000, -39.83014742847162637 ) ) ;
#58234=ORIENTED_EDGE ( 'NONE', *, *, #68020, .F. ) ;
#58270=CARTESIAN_POINT ( 'NONE',  ( 35.99999999999999289, 5.000000000000000000, -29.00402776293825724 ) ) ;
#58273=ORIENTED_EDGE ( 'NONE', *, *, #65103, .T. ) ;
#58274=AXIS2_PLACEMENT_3D ( 'NONE', #66176, #2092, #23618 ) ;
#58281=PLANE ( 'NONE',  #59168 ) ;
#58286=ORIENTED_EDGE ( 'NONE', *, *, #7955, .T. ) ;
#58287=CIRCLE ( 'NONE', #52680, 4.999999999999997335 ) ;
#58292=( NAMED_UNIT ( * ) PLANE_ANGLE_UNIT ( ) SI_UNIT ( $, .RADIAN. ) );
#58297=DIRECTION ( 'NONE',  ( 1.000000000000000000, 3.011817513800517074E-33, -1.300977106640435384E-16 ) ) ;
#58299=ORIENTED_EDGE ( 'NONE', *, *, #4379, .F. ) ;
#58324=CARTESIAN_POINT ( 'NONE',  ( 10.00000000000001954, 42.00000000000000000, -35.50000000000000000 ) ) ;
#58325=( NAMED_UNIT ( * ) PLANE_ANGLE_UNIT ( ) SI_UNIT ( $, .RADIAN. ) );
#58338=STYLED_ITEM ( 'NONE', ( #16649 ), #4931 ) ;
#58343=( NAMED_UNIT ( * ) PLANE_ANGLE_UNIT ( ) SI_UNIT ( $, .RADIAN. ) );
#58351=MECHANICAL_DESIGN_GEOMETRIC_PRESENTATION_REPRESENTATION('',(#66226),#25763);
#58353=PRESENTATION_STYLE_ASSIGNMENT (( #15479 ) ) ;
#58363=SURFACE_STYLE_USAGE ( .BOTH. , #47525 ) ;
#58366=( GEOMETRIC_REPRESENTATION_CONTEXT ( 3 ) GLOBAL_UNCERTAINTY_ASSIGNED_CONTEXT ( ( #61391 ) ) GLOBAL_UNIT_ASSIGNED_CONTEXT ( ( #60699, #1216, #38961 ) ) REPRESENTATION_CONTEXT ( 'NONE', 'WORKASPACE' ) );
#58369=( NAMED_UNIT ( * ) SI_UNIT ( $, .STERADIAN. ) SOLID_ANGLE_UNIT ( ) );
#58375=VECTOR ( 'NONE', #32365, 1000.000000000000000 ) ;
#58376=LINE ( 'NONE', #38001, #29618 ) ;
#58388=MECHANICAL_DESIGN_GEOMETRIC_PRESENTATION_REPRESENTATION('',(#43818),#68485);
#58392=( GEOMETRIC_REPRESENTATION_CONTEXT ( 3 ) GLOBAL_UNCERTAINTY_ASSIGNED_CONTEXT ( ( #23595 ) ) GLOBAL_UNIT_ASSIGNED_CONTEXT ( ( #58794, #32060, #11289 ) ) REPRESENTATION_CONTEXT ( 'NONE', 'WORKASPACE' ) );
#58398=FILL_AREA_STYLE_COLOUR ( '', #67405 ) ;
#58408=PLANE ( 'NONE',  #34845 ) ;
#58411=CARTESIAN_POINT ( 'NONE',  ( 98.00000000000000000, 16.00000000000000000, 12.50000000000000178 ) ) ;
#58429=CIRCLE ( 'NONE', #53939, 5.000000000000004441 ) ;
#58430=ORIENTED_EDGE ( 'NONE', *, *, #53298, .T. ) ;
#58437=EDGE_LOOP ( 'NONE', ( #13062, #12093, #18891, #44836 ) ) ;
#58438=ORIENTED_EDGE ( 'NONE', *, *, #19549, .F. ) ;
#58448=( GEOMETRIC_REPRESENTATION_CONTEXT ( 3 ) GLOBAL_UNCERTAINTY_ASSIGNED_CONTEXT ( ( #68646 ) ) GLOBAL_UNIT_ASSIGNED_CONTEXT ( ( #67084, #56517, #3001 ) ) REPRESENTATION_CONTEXT ( 'NONE', 'WORKASPACE' ) );
#58457=AXIS2_PLACEMENT_3D ( 'NONE', #2767, #19320, #36240 ) ;
#58477=VECTOR ( 'NONE', #10480, 1000.000000000000000 ) ;
#58480=DIRECTION ( 'NONE',  ( -7.816271194327172234E-17, -0.000000000000000000, -1.000000000000000000 ) ) ;
#58484=CARTESIAN_POINT ( 'NONE',  ( 28.00000000000002842, 43.00000000000000000, 79.00402776293826435 ) ) ;
#58495=( NAMED_UNIT ( * ) PLANE_ANGLE_UNIT ( ) SI_UNIT ( $, .RADIAN. ) );
#58501=( NAMED_UNIT ( * ) PLANE_ANGLE_UNIT ( ) SI_UNIT ( $, .RADIAN. ) );
#58503=CYLINDRICAL_SURFACE ( 'NONE', #41514, 5.000000000000004441 ) ;
#58508=COLOUR_RGB ( '', 0.31764706, 0.68627451, 0.89019608) ;
#58514=DIRECTION ( 'NONE',  ( 1.300977106640434891E-16, 0.000000000000000000, 1.000000000000000000 ) ) ;
#58517=( LENGTH_UNIT ( ) NAMED_UNIT ( * ) SI_UNIT ( .MILLI., .METRE. ) );
#58528=DIRECTION ( 'NONE',  ( 0.6402681315062906942, 0.000000000000000000, -0.7681514953298230752 ) ) ;
#58532=PRESENTATION_STYLE_ASSIGNMENT (( #16689 ) ) ;
#58541=CARTESIAN_POINT ( 'NONE',  ( 2.999999999999993339, 0.000000000000000000, 24.00402776293822882 ) ) ;
#58546=EDGE_CURVE ( 'NONE', #41012, #8636, #3392, .T. ) ;
#58549=CARTESIAN_POINT ( 'NONE',  ( 28.58578643762690419, 34.36176364315825538, -80.00402776293826435 ) ) ;
#58550=ORIENTED_EDGE ( 'NONE', *, *, #52216, .T. ) ;
#58551=CYLINDRICAL_SURFACE ( 'NONE', #27210, 1.000000000000000888 ) ;
#58557=FILL_AREA_STYLE_COLOUR ( '', #46558 ) ;
#58559=FILL_AREA_STYLE ('',( #37150 ) ) ;
#58564=VERTEX_POINT ( 'NONE', #29826 ) ;
#58575=STYLED_ITEM ( 'NONE', ( #64607 ), #45568 ) ;
#58583=SURFACE_STYLE_FILL_AREA ( #16408 ) ;
#58585=AXIS2_PLACEMENT_3D ( 'NONE', #68233, #47514, #68931 ) ;
#58599=ADVANCED_FACE ( 'NONE', ( #14339 ), #46762, .T. ) ;
#58603=STYLED_ITEM ( 'NONE', ( #32004 ), #25107 ) ;
#58605=DIRECTION ( 'NONE',  ( 0.000000000000000000, 0.000000000000000000, 1.000000000000000000 ) ) ;
#58608=EDGE_CURVE ( 'NONE', #51568, #65703, #58643, .T. ) ;
#58609=DIRECTION ( 'NONE',  ( 1.000000000000000000, 0.000000000000000000, 0.000000000000000000 ) ) ;
#58618=AXIS2_PLACEMENT_3D ( 'NONE', #48047, #15334, #10028 ) ;
#58619=ADVANCED_FACE ( 'NONE', ( #31193 ), #4454, .F. ) ;
#58626=EDGE_LOOP ( 'NONE', ( #1920, #68842, #5005, #35789 ) ) ;
#58637=ORIENTED_EDGE ( 'NONE', *, *, #39976, .F. ) ;
#58643=LINE ( 'NONE', #15079, #6418 ) ;
#58648=FACE_OUTER_BOUND ( 'NONE', #39563, .T. ) ;
#58655=EDGE_LOOP ( 'NONE', ( #11549, #43379, #64516, #49680 ) ) ;
#58658=PRESENTATION_STYLE_ASSIGNMENT (( #196 ) ) ;
#58677=DIRECTION ( 'NONE',  ( 0.000000000000000000, 0.6691306063588591257, -0.7431448254773933559 ) ) ;
#58694=AXIS2_PLACEMENT_3D ( 'NONE', #59007, #26624, #64277 ) ;
#58695=EDGE_CURVE ( 'NONE', #37203, #52477, #55076, .T. ) ;
#58696=LINE ( 'NONE', #43271, #38660 ) ;
#58703=( GEOMETRIC_REPRESENTATION_CONTEXT ( 3 ) GLOBAL_UNCERTAINTY_ASSIGNED_CONTEXT ( ( #30757 ) ) GLOBAL_UNIT_ASSIGNED_CONTEXT ( ( #51067, #66543, #34522 ) ) REPRESENTATION_CONTEXT ( 'NONE', 'WORKASPACE' ) );
#58704=ADVANCED_FACE ( 'NONE', ( #1906 ), #38274, .T. ) ;
#58706=( LENGTH_UNIT ( ) NAMED_UNIT ( * ) SI_UNIT ( .MILLI., .METRE. ) );
#58718=DIRECTION ( 'NONE',  ( 1.000000000000000000, 0.000000000000000000, 0.000000000000000000 ) ) ;
#58719=ORIENTED_EDGE ( 'NONE', *, *, #44618, .F. ) ;
#58722=SURFACE_STYLE_FILL_AREA ( #63651 ) ;
#58732=UNCERTAINTY_MEASURE_WITH_UNIT (LENGTH_MEASURE( 1.000000000000000082E-05 ), #28654, 'distance_accuracy_value', 'NONE');
#58734=DIRECTION ( 'NONE',  ( 1.000000000000000000, 0.000000000000000000, -0.000000000000000000 ) ) ;
#58736=CLOSED_SHELL ( 'NONE', ( #68551, #13584, #21316, #63851, #32799, #36477, #10190, #46507, #69261, #48321, #51534, #22015, #66640, #15754, #42644, #10110, #23236, #48453, #31854, #37626, #43504, #12899, #24383, #3197, #23057, #17692, #21188, #14808, #20414, #17443, #49889, #25659, #9057, #60130, #33588, #1385, #69042, #5852, #13966, #50144, #32479, #48817, #25726, #9473, #43661, #17422, #29309, #25798, #47383, #37898, #58619, #9068, #65596, #48973, #57035, #23739, #56478, #43186, #27294, #22745, #5776, #19692, #2613, #20903, #67535, #52676, #62726, #3109, #45142, #34932, #19793, #29078, #57571, #43263, #7960, #28790, #27374, #15066, #23760, #51434, #17664, #46922, #37537, #62457, #22725, #40275, #52134, #11833, #22800, #51812, #61877, #732, #13575, #8539, #69613, #24852, #5862, #7177, #15209, #62484, #959, #59214, #66381, #67261, #35265, #31599, #62816, #22304, #46275, #4500, #25491, #33355, #8923, #7361, #58704, #28748, #30249, #58599, #13842, #12013, #51194, #87, #18292, #16864, #48340, #33625, #68252, #45568, #26213, #35453, #53990, #50834, #15826, #44200, #61803, #15305, #17272, #49528, #22003, #7259, #46516, #9331, #413, #12291, #69187, #54771, #46912, #1191, #14500, #52832, #10344, #16349, #34621, #25220, #61678, #31604, #8127, #44851, #63878, #25107, #54231, #34703, #35614, #55468, #2820, #54665, #18531, #33429, #16655, #62279, #11186, #51411, #1461, #3494, #31034, #19990, #56868, #26993, #8754, #8442, #1111, #67420, #66698, #19852, #45798, #25963, #41344, #58971, #68163, #59718, #45663, #20977, #55765, #4039, #64946, #20668, #41887, #38953, #11347, #21041, #46200, #17817, #62157, #12423, #12452, #34175, #53463, #69178, #18149, #2245, #44302, #34550, #38644, #65509, #45224, #61675, #16682, #15907, #2839, #8523, #27529, #48348, #10844, #23705, #18116, #9839, #34243, #15583, #60579, #50424, #49411, #67510, #41731, #65333, #51101, #38079, #5139, #22907, #42953, #45982, #1027, #4931, #56294, #19538, #53652, #45241, #31262, #30408, #17773, #60351, #60805, #14878 ) ) ;
#58738=( GEOMETRIC_REPRESENTATION_CONTEXT ( 3 ) GLOBAL_UNCERTAINTY_ASSIGNED_CONTEXT ( ( #27190 ) ) GLOBAL_UNIT_ASSIGNED_CONTEXT ( ( #43620, #27372, #59749 ) ) REPRESENTATION_CONTEXT ( 'NONE', 'WORKASPACE' ) );
#58748=UNCERTAINTY_MEASURE_WITH_UNIT (LENGTH_MEASURE( 1.000000000000000082E-05 ), #25205, 'distance_accuracy_value', 'NONE');
#58751=( NAMED_UNIT ( * ) PLANE_ANGLE_UNIT ( ) SI_UNIT ( $, .RADIAN. ) );
#58753=ORIENTED_EDGE ( 'NONE', *, *, #48692, .T. ) ;
#58756=CARTESIAN_POINT ( 'NONE',  ( 75.83633811589984930, 14.00000000000000000, 66.72655454856716517 ) ) ;
#58759=DIRECTION ( 'NONE',  ( 0.000000000000000000, -0.000000000000000000, -1.000000000000000000 ) ) ;
#58775=CIRCLE ( 'NONE', #5986, 5.000000000000004441 ) ;
#58778=EDGE_CURVE ( 'NONE', #57229, #20856, #56102, .T. ) ;
#58787=( NAMED_UNIT ( * ) PLANE_ANGLE_UNIT ( ) SI_UNIT ( $, .RADIAN. ) );
#58789=EDGE_LOOP ( 'NONE', ( #47998, #37655, #62463, #46022, #53285 ) ) ;
#58791=CARTESIAN_POINT ( 'NONE',  ( 27.99999999999998224, 5.000000000000000000, 72.00402776293822171 ) ) ;
#58794=( LENGTH_UNIT ( ) NAMED_UNIT ( * ) SI_UNIT ( .MILLI., .METRE. ) );
#58796=VECTOR ( 'NONE', #38449, 1000.000000000000000 ) ;
#58800=AXIS2_PLACEMENT_3D ( 'NONE', #45394, #23209, #1333 ) ;
#58802=FILL_AREA_STYLE ('',( #37396 ) ) ;
#58821=DIRECTION ( 'NONE',  ( 0.000000000000000000, -1.000000000000000000, 0.000000000000000000 ) ) ;
#58824=COLOUR_RGB ( '', 0.40784314, 0.44705882, 0.49803922) ;
#58835=CARTESIAN_POINT ( 'NONE',  ( 22.99999999999995381, 0.000000000000000000, 32.00402776293825724 ) ) ;
#58837=AXIS2_PLACEMENT_3D ( 'NONE', #45833, #61972, #37386 ) ;
#58842=AXIS2_PLACEMENT_3D ( 'NONE', #40410, #66790, #8397 ) ;
#58852=CYLINDRICAL_SURFACE ( 'NONE', #56024, 12.50000000000000178 ) ;
#58863=AXIS2_PLACEMENT_3D ( 'NONE', #31840, #53329, #27235 ) ;
#58867=EDGE_CURVE ( 'NONE', #58564, #58968, #10079, .T. ) ;
#58868=ORIENTED_EDGE ( 'NONE', *, *, #17969, .T. ) ;
#58911=AXIS2_PLACEMENT_3D ( 'NONE', #55734, #33917, #50458 ) ;
#58918=CARTESIAN_POINT ( 'NONE',  ( 16.00000000000001776, 42.00000000000000000, -29.68999999999999417 ) ) ;
#58924=DIRECTION ( 'NONE',  ( 0.000000000000000000, 0.000000000000000000, -1.000000000000000000 ) ) ;
#58927=COLOUR_RGB ( '', 0.40784314, 0.44705882, 0.49803922) ;
#58942=( NAMED_UNIT ( * ) PLANE_ANGLE_UNIT ( ) SI_UNIT ( $, .RADIAN. ) );
#58958=PLANE ( 'NONE',  #14738 ) ;
#58959=AXIS2_PLACEMENT_3D ( 'NONE', #27652, #534, #6223 ) ;
#58961=PRESENTATION_STYLE_ASSIGNMENT (( #10434 ) ) ;
#58962=AXIS2_PLACEMENT_3D ( 'NONE', #16411, #24558, #64200 ) ;
#58968=VERTEX_POINT ( 'NONE', #58219 ) ;
#58971=ADVANCED_FACE ( 'NONE', ( #53962 ), #20146, .T. ) ;
#58975=ORIENTED_EDGE ( 'NONE', *, *, #2497, .F. ) ;
#58984=EDGE_LOOP ( 'NONE', ( #56178, #27985, #42834, #4810 ) ) ;
#58992=SURFACE_SIDE_STYLE ('',( #69539 ) ) ;
#58998=CARTESIAN_POINT ( 'NONE',  ( 74.89452121010485541, 13.00000000000000178, 66.39042820928573008 ) ) ;
#58999=PRESENTATION_STYLE_ASSIGNMENT (( #57979 ) ) ;
#59007=CARTESIAN_POINT ( 'NONE',  ( 0.000000000000000000, 50.00000000000000000, 60.00000000000000000 ) ) ;
#59010=VECTOR ( 'NONE', #22690, 1000.000000000000000 ) ;
#59027=CARTESIAN_POINT ( 'NONE',  ( 0.000000000000000000, 42.00000000000000000, -36.49999999999999289 ) ) ;
#59034=LINE ( 'NONE', #16152, #64043 ) ;
#59044=ORIENTED_EDGE ( 'NONE', *, *, #16095, .T. ) ;
#59053=DIRECTION ( 'NONE',  ( 1.300977106640434891E-16, -0.000000000000000000, 1.000000000000000000 ) ) ;
#59055=ORIENTED_EDGE ( 'NONE', *, *, #6581, .T. ) ;
#59059=AXIS2_PLACEMENT_3D ( 'NONE', #53363, #37578, #20289 ) ;
#59063=DIRECTION ( 'NONE',  ( -0.000000000000000000, -1.000000000000000000, -0.000000000000000000 ) ) ;
#59064=EDGE_LOOP ( 'NONE', ( #48624, #1214, #68938, #19701 ) ) ;
#59071=FILL_AREA_STYLE ('',( #5940 ) ) ;
#59087=CARTESIAN_POINT ( 'NONE',  ( 7.000000000000017764, 43.00000000000000000, -28.00000000000000000 ) ) ;
#59091=VERTEX_POINT ( 'NONE', #16722 ) ;
#59096=SURFACE_SIDE_STYLE ('',( #6314 ) ) ;
#59099=EDGE_CURVE ( 'NONE', #1731, #46991, #38185, .T. ) ;
#59102=ORIENTED_EDGE ( 'NONE', *, *, #47560, .T. ) ;
#59111=DIRECTION ( 'NONE',  ( 0.000000000000000000, 0.000000000000000000, 1.000000000000000000 ) ) ;
#59121=FILL_AREA_STYLE ('',( #28384 ) ) ;
#59123=SURFACE_STYLE_FILL_AREA ( #54195 ) ;
#59125=ORIENTED_EDGE ( 'NONE', *, *, #14449, .T. ) ;
#59131=CARTESIAN_POINT ( 'NONE',  ( 3.000000000000030198, 38.70020753820971748, 89.00000000000000000 ) ) ;
#59135=ORIENTED_EDGE ( 'NONE', *, *, #30476, .T. ) ;
#59142=( NAMED_UNIT ( * ) SI_UNIT ( $, .STERADIAN. ) SOLID_ANGLE_UNIT ( ) );
#59145=CARTESIAN_POINT ( 'NONE',  ( 92.41620014002536720, 5.000000000000000000, -24.00402776293825369 ) ) ;
#59159=( NAMED_UNIT ( * ) PLANE_ANGLE_UNIT ( ) SI_UNIT ( $, .RADIAN. ) );
#59163=( NAMED_UNIT ( * ) SI_UNIT ( $, .STERADIAN. ) SOLID_ANGLE_UNIT ( ) );
#59168=AXIS2_PLACEMENT_3D ( 'NONE', #514, #27633, #65977 ) ;
#59170=CARTESIAN_POINT ( 'NONE',  ( 22.00000000000000355, 42.47058823529412308, -74.11764705882353610 ) ) ;
#59172=DIRECTION ( 'NONE',  ( 1.000000000000000000, 0.000000000000000000, -4.625929269271505635E-16 ) ) ;
#59191=DIRECTION ( 'NONE',  ( 1.000000000000000000, 0.000000000000000000, -1.300977106640435137E-16 ) ) ;
#59200=CYLINDRICAL_SURFACE ( 'NONE', #8942, 4.999999999999997335 ) ;
#59202=DIRECTION ( 'NONE',  ( -1.000000000000000000, -0.000000000000000000, 1.300977106640434891E-16 ) ) ;
#59207=( LENGTH_UNIT ( ) NAMED_UNIT ( * ) SI_UNIT ( .MILLI., .METRE. ) );
#59212=EDGE_CURVE ( 'NONE', #53146, #33379, #5571, .T. ) ;
#59214=ADVANCED_FACE ( 'NONE', ( #65410 ), #47913, .F. ) ;
#59220=EDGE_LOOP ( 'NONE', ( #64334, #28133, #705, #52679 ) ) ;
#59228=CARTESIAN_POINT ( 'NONE',  ( 26.00000000000001776, 42.00000000000000000, 29.68999999999999417 ) ) ;
#59244=VERTEX_POINT ( 'NONE', #66084 ) ;
#59246=SURFACE_SIDE_STYLE ('',( #55010 ) ) ;
#59248=VECTOR ( 'NONE', #63316, 1000.000000000000000 ) ;
#59252=DIRECTION ( 'NONE',  ( 0.000000000000000000, 0.000000000000000000, 1.000000000000000000 ) ) ;
#59258=UNCERTAINTY_MEASURE_WITH_UNIT (LENGTH_MEASURE( 1.000000000000000082E-05 ), #23074, 'distance_accuracy_value', 'NONE');
#59282=VECTOR ( 'NONE', #1432, 1000.000000000000000 ) ;
#59287=AXIS2_PLACEMENT_3D ( 'NONE', #6499, #1175, #22710 ) ;
#59302=ORIENTED_EDGE ( 'NONE', *, *, #30726, .F. ) ;
#59309=DIRECTION ( 'NONE',  ( 0.000000000000000000, 0.000000000000000000, 1.000000000000000000 ) ) ;
#59310=ORIENTED_EDGE ( 'NONE', *, *, #1622, .F. ) ;
#59313=FILL_AREA_STYLE_COLOUR ( '', #18729 ) ;
#59314=MECHANICAL_DESIGN_GEOMETRIC_PRESENTATION_REPRESENTATION('',(#41401),#25631);
#59315=DIRECTION ( 'NONE',  ( 0.000000000000000000, 0.000000000000000000, -1.000000000000000000 ) ) ;
#59344=FACE_OUTER_BOUND ( 'NONE', #10115, .T. ) ;
#59349=UNCERTAINTY_MEASURE_WITH_UNIT (LENGTH_MEASURE( 1.000000000000000082E-05 ), #22062, 'distance_accuracy_value', 'NONE');
#59352=CARTESIAN_POINT ( 'NONE',  ( 96.10348817448819148, 0.000000000000000000, 27.38099488609881149 ) ) ;
#59356=CARTESIAN_POINT ( 'NONE',  ( 28.00000000000000000, 42.00000000000000000, 3.902931319921305165E-16 ) ) ;
#59360=FACE_OUTER_BOUND ( 'NONE', #32597, .T. ) ;
#59361=UNCERTAINTY_MEASURE_WITH_UNIT (LENGTH_MEASURE( 1.000000000000000082E-05 ), #10081, 'distance_accuracy_value', 'NONE');
#59368=CARTESIAN_POINT ( 'NONE',  ( 32.00000000000001421, 42.00000000000000000, -36.50000000000000000 ) ) ;
#59369=EDGE_LOOP ( 'NONE', ( #19133, #11494, #9013, #6641 ) ) ;
#59371=ORIENTED_EDGE ( 'NONE', *, *, #822, .T. ) ;
#59384=ORIENTED_EDGE ( 'NONE', *, *, #3307, .T. ) ;
#59385=CARTESIAN_POINT ( 'NONE',  ( 92.41620014002536720, 5.000000000000000000, -29.00402776293825724 ) ) ;
#59386=( LENGTH_UNIT ( ) NAMED_UNIT ( * ) SI_UNIT ( .MILLI., .METRE. ) );
#59387=CARTESIAN_POINT ( 'NONE',  ( 31.00000000000001421, 42.00000000000000000, 36.49999999999999289 ) ) ;
#59399=ORIENTED_EDGE ( 'NONE', *, *, #55822, .T. ) ;
#59404=( NAMED_UNIT ( * ) PLANE_ANGLE_UNIT ( ) SI_UNIT ( $, .RADIAN. ) );
#59405=UNCERTAINTY_MEASURE_WITH_UNIT (LENGTH_MEASURE( 1.000000000000000082E-05 ), #15878, 'distance_accuracy_value', 'NONE');
#59406=CIRCLE ( 'NONE', #29067, 5.000000000000004441 ) ;
#59410=VERTEX_POINT ( 'NONE', #10817 ) ;
#59417=( NAMED_UNIT ( * ) PLANE_ANGLE_UNIT ( ) SI_UNIT ( $, .RADIAN. ) );
#59422=EDGE_CURVE ( 'NONE', #8099, #40740, #48841, .T. ) ;
#59426=FILL_AREA_STYLE ('',( #39075 ) ) ;
#59427=PLANE ( 'NONE',  #61207 ) ;
#59428=SURFACE_SIDE_STYLE ('',( #38037 ) ) ;
#59436=VECTOR ( 'NONE', #64119, 1000.000000000000000 ) ;
#59440=( GEOMETRIC_REPRESENTATION_CONTEXT ( 3 ) GLOBAL_UNCERTAINTY_ASSIGNED_CONTEXT ( ( #29356 ) ) GLOBAL_UNIT_ASSIGNED_CONTEXT ( ( #60467, #63766, #21195 ) ) REPRESENTATION_CONTEXT ( 'NONE', 'WORKASPACE' ) );
#59449=CARTESIAN_POINT ( 'NONE',  ( 4.000000000000030198, 42.00000000000000000, 0.000000000000000000 ) ) ;
#59453=AXIS2_PLACEMENT_3D ( 'NONE', #32177, #21617, #43133 ) ;
#59458=CARTESIAN_POINT ( 'NONE',  ( 0.000000000000000000, 0.9999999999999991118, -79.00402776293826435 ) ) ;
#59461=DIRECTION ( 'NONE',  ( 0.000000000000000000, 0.000000000000000000, -1.000000000000000000 ) ) ;
#59476=CIRCLE ( 'NONE', #60571, 5.999999999999998224 ) ;
#59500=UNCERTAINTY_MEASURE_WITH_UNIT (LENGTH_MEASURE( 1.000000000000000082E-05 ), #18231, 'distance_accuracy_value', 'NONE');
#59501=VECTOR ( 'NONE', #21205, 1000.000000000000000 ) ;
#59510=DIRECTION ( 'NONE',  ( 0.000000000000000000, -0.000000000000000000, 1.000000000000000000 ) ) ;
#59530=CARTESIAN_POINT ( 'NONE',  ( 6.000000000000017764, 13.99999999999997691, 35.50000000000000000 ) ) ;
#59531=SURFACE_STYLE_FILL_AREA ( #37463 ) ;
#59539=LINE ( 'NONE', #22266, #56248 ) ;
#59556=CARTESIAN_POINT ( 'NONE',  ( 35.99999999999999289, 5.000000000000000000, 37.00402776293825724 ) ) ;
#59568=UNCERTAINTY_MEASURE_WITH_UNIT (LENGTH_MEASURE( 1.000000000000000082E-05 ), #52366, 'distance_accuracy_value', 'NONE');
#59569=CARTESIAN_POINT ( 'NONE',  ( 22.00000000000002132, 42.00000000000000000, 29.68999999999999417 ) ) ;
#59577=ORIENTED_EDGE ( 'NONE', *, *, #61369, .F. ) ;
#59586=( NAMED_UNIT ( * ) PLANE_ANGLE_UNIT ( ) SI_UNIT ( $, .RADIAN. ) );
#59588=CARTESIAN_POINT ( 'NONE',  ( 3.000000000000002665, 38.70020753820971748, -90.00000000000000000 ) ) ;
#59591=DIRECTION ( 'NONE',  ( 1.300977106640435137E-16, 0.000000000000000000, 1.000000000000000000 ) ) ;
#59606=FACE_BOUND ( 'NONE', #52275, .T. ) ;
#59617=( GEOMETRIC_REPRESENTATION_CONTEXT ( 3 ) GLOBAL_UNCERTAINTY_ASSIGNED_CONTEXT ( ( #47395 ) ) GLOBAL_UNIT_ASSIGNED_CONTEXT ( ( #51445, #46916, #19778 ) ) REPRESENTATION_CONTEXT ( 'NONE', 'WORKASPACE' ) );
#59618=SURFACE_SIDE_STYLE ('',( #49117 ) ) ;
#59636=AXIS2_PLACEMENT_3D ( 'NONE', #47064, #15049, #30474 ) ;
#59637=ORIENTED_EDGE ( 'NONE', *, *, #64894, .T. ) ;
#59648=EDGE_CURVE ( 'NONE', #33374, #29900, #60709, .T. ) ;
#59653=CYLINDRICAL_SURFACE ( 'NONE', #23128, 1.000000000000000888 ) ;
#59666=STYLED_ITEM ( 'NONE', ( #51687 ), #13575 ) ;
#59680=CARTESIAN_POINT ( 'NONE',  ( 11.00000000000001776, 15.00000000000000000, -29.68999999999999417 ) ) ;
#59693=COLOUR_RGB ( '', 0.31764706, 0.68627451, 0.89019608) ;
#59696=VECTOR ( 'NONE', #59191, 1000.000000000000000 ) ;
#59700=VECTOR ( 'NONE', #56922, 1000.000000000000000 ) ;
#59714=( LENGTH_UNIT ( ) NAMED_UNIT ( * ) SI_UNIT ( .MILLI., .METRE. ) );
#59718=ADVANCED_FACE ( 'NONE', ( #16844 ), #40569, .F. ) ;
#59726=EDGE_CURVE ( 'NONE', #15864, #34648, #50222, .T. ) ;
#59736=FACE_OUTER_BOUND ( 'NONE', #53878, .T. ) ;
#59742=FACE_OUTER_BOUND ( 'NONE', #44393, .T. ) ;
#59744=ORIENTED_EDGE ( 'NONE', *, *, #42387, .T. ) ;
#59747=VECTOR ( 'NONE', #1325, 1000.000000000000000 ) ;
#59749=( NAMED_UNIT ( * ) SI_UNIT ( $, .STERADIAN. ) SOLID_ANGLE_UNIT ( ) );
#59756=CARTESIAN_POINT ( 'NONE',  ( 57.00000000000000000, 14.00000000000000000, -60.00402776293825724 ) ) ;
#59759=DIRECTION ( 'NONE',  ( -1.000000000000000000, 0.000000000000000000, 0.000000000000000000 ) ) ;
#59762=CYLINDRICAL_SURFACE ( 'NONE', #41893, 3.499999999999999556 ) ;
#59764=ORIENTED_EDGE ( 'NONE', *, *, #11354, .T. ) ;
#59766=ORIENTED_EDGE ( 'NONE', *, *, #9987, .F. ) ;
#59775=ORIENTED_EDGE ( 'NONE', *, *, #36687, .T. ) ;
#59776=MECHANICAL_DESIGN_GEOMETRIC_PRESENTATION_REPRESENTATION('',(#63143),#68784);
#59789=SURFACE_STYLE_USAGE ( .BOTH. , #64022 ) ;
#59798=PLANE ( 'NONE',  #51544 ) ;
#59826=CARTESIAN_POINT ( 'NONE',  ( 0.000000000000000000, 42.00000000000000000, 35.50000000000000000 ) ) ;
#59834=DIRECTION ( 'NONE',  ( 0.000000000000000000, 0.000000000000000000, -1.000000000000000000 ) ) ;
#59844=ORIENTED_EDGE ( 'NONE', *, *, #56688, .F. ) ;
#59845=FACE_BOUND ( 'NONE', #17317, .T. ) ;
#59858=ORIENTED_EDGE ( 'NONE', *, *, #11928, .T. ) ;
#59882=AXIS2_PLACEMENT_3D ( 'NONE', #22826, #44324, #65722 ) ;
#59888=CARTESIAN_POINT ( 'NONE',  ( 1.000000000000000888, 0.9999999999999991118, 80.00402776293826435 ) ) ;
#59902=CIRCLE ( 'NONE', #19431, 1.000000000000000888 ) ;
#59907=ORIENTED_EDGE ( 'NONE', *, *, #6104, .F. ) ;
#59910=ORIENTED_EDGE ( 'NONE', *, *, #60560, .T. ) ;
#59911=( NAMED_UNIT ( * ) PLANE_ANGLE_UNIT ( ) SI_UNIT ( $, .RADIAN. ) );
#59918=AXIS2_PLACEMENT_3D ( 'NONE', #67302, #25426, #66968 ) ;
#59921=( LENGTH_UNIT ( ) NAMED_UNIT ( * ) SI_UNIT ( .MILLI., .METRE. ) );
#59924=CARTESIAN_POINT ( 'NONE',  ( 7.999999999999989342, 5.000000000000000000, 37.00402776293825724 ) ) ;
#59941=ORIENTED_EDGE ( 'NONE', *, *, #2902, .T. ) ;
#59942=FILL_AREA_STYLE ('',( #36888 ) ) ;
#59943=CARTESIAN_POINT ( 'NONE',  ( 31.00000000000000355, 43.00000000000000000, -45.61250543006184444 ) ) ;
#59945=DIRECTION ( 'NONE',  ( 1.000000000000000000, -0.000000000000000000, -0.000000000000000000 ) ) ;
#59955=EDGE_CURVE ( 'NONE', #33110, #35954, #66387, .T. ) ;
#59956=AXIS2_PLACEMENT_3D ( 'NONE', #12843, #19854, #13529 ) ;
#59961=LINE ( 'NONE', #69150, #68403 ) ;
#59969=( GEOMETRIC_REPRESENTATION_CONTEXT ( 3 ) GLOBAL_UNCERTAINTY_ASSIGNED_CONTEXT ( ( #44632 ) ) GLOBAL_UNIT_ASSIGNED_CONTEXT ( ( #60415, #3014, #12930 ) ) REPRESENTATION_CONTEXT ( 'NONE', 'WORKASPACE' ) );
#59977=CARTESIAN_POINT ( 'NONE',  ( 0.000000000000000000, 0.000000000000000000, 0.000000000000000000 ) ) ;
#59985=( NAMED_UNIT ( * ) SI_UNIT ( $, .STERADIAN. ) SOLID_ANGLE_UNIT ( ) );
#59995=DIRECTION ( 'NONE',  ( 0.000000000000000000, 0.000000000000000000, -1.000000000000000000 ) ) ;
#60003=ORIENTED_EDGE ( 'NONE', *, *, #12836, .F. ) ;
#60005=VECTOR ( 'NONE', #35228, 1000.000000000000000 ) ;
#60008=FILL_AREA_STYLE ('',( #6198 ) ) ;
#60011=DIRECTION ( 'NONE',  ( 0.000000000000000000, 1.000000000000000000, -0.000000000000000000 ) ) ;
#60023=VERTEX_POINT ( 'NONE', #43087 ) ;
#60024=( LENGTH_UNIT ( ) NAMED_UNIT ( * ) SI_UNIT ( .MILLI., .METRE. ) );
#60025=EDGE_CURVE ( 'NONE', #4230, #4136, #59539, .T. ) ;
#60033=SURFACE_STYLE_FILL_AREA ( #38978 ) ;
#60039=ORIENTED_EDGE ( 'NONE', *, *, #53917, .T. ) ;
#60046=CARTESIAN_POINT ( 'NONE',  ( 28.00000000000000000, 38.70020753820971748, -90.00000000000000000 ) ) ;
#60053=AXIS2_PLACEMENT_3D ( 'NONE', #37336, #21806, #26702 ) ;
#60054=EDGE_CURVE ( 'NONE', #53146, #33110, #54612, .T. ) ;
#60057=CARTESIAN_POINT ( 'NONE',  ( 24.08751298501318772, 24.72230729296544993, 27.25873204504173231 ) ) ;
#60063=STYLED_ITEM ( 'NONE', ( #47344 ), #62279 ) ;
#60065=DIRECTION ( 'NONE',  ( 0.000000000000000000, 0.000000000000000000, 1.000000000000000000 ) ) ;
#60066=UNCERTAINTY_MEASURE_WITH_UNIT (LENGTH_MEASURE( 1.000000000000000082E-05 ), #42293, 'distance_accuracy_value', 'NONE');
#60068=ORIENTED_EDGE ( 'NONE', *, *, #50271, .T. ) ;
#60071=( GEOMETRIC_REPRESENTATION_CONTEXT ( 3 ) GLOBAL_UNCERTAINTY_ASSIGNED_CONTEXT ( ( #57159 ) ) GLOBAL_UNIT_ASSIGNED_CONTEXT ( ( #57173, #40329, #30421 ) ) REPRESENTATION_CONTEXT ( 'NONE', 'WORKASPACE' ) );
#60074=COLOUR_RGB ( '', 0.66274510, 0.83137255, 0.94901961) ;
#60091=( NAMED_UNIT ( * ) PLANE_ANGLE_UNIT ( ) SI_UNIT ( $, .RADIAN. ) );
#60096=CIRCLE ( 'NONE', #63477, 4.000000000000000000 ) ;
#60105=LINE ( 'NONE', #33042, #25369 ) ;
#60119=STYLED_ITEM ( 'NONE', ( #31214 ), #5139 ) ;
#60122=DIRECTION ( 'NONE',  ( 0.000000000000000000, 0.000000000000000000, -1.000000000000000000 ) ) ;
#60123=UNCERTAINTY_MEASURE_WITH_UNIT (LENGTH_MEASURE( 1.000000000000000082E-05 ), #50216, 'distance_accuracy_value', 'NONE');
#60128=ORIENTED_EDGE ( 'NONE', *, *, #7013, .F. ) ;
#60130=ADVANCED_FACE ( 'NONE', ( #40199 ), #23997, .T. ) ;
#60137=CARTESIAN_POINT ( 'NONE',  ( 25.00000000000001421, 42.00000000000000000, -29.68999999999999417 ) ) ;
#60141=CARTESIAN_POINT ( 'NONE',  ( 179.4361977533476136, 5.000000000000000000, 103.7004518695250823 ) ) ;
#60143=MECHANICAL_DESIGN_GEOMETRIC_PRESENTATION_REPRESENTATION('',(#27526),#61284);
#60157=UNCERTAINTY_MEASURE_WITH_UNIT (LENGTH_MEASURE( 1.000000000000000082E-05 ), #39117, 'distance_accuracy_value', 'NONE');
#60191=FILL_AREA_STYLE_COLOUR ( '', #69009 ) ;
#60199=UNCERTAINTY_MEASURE_WITH_UNIT (LENGTH_MEASURE( 1.000000000000000082E-05 ), #57140, 'distance_accuracy_value', 'NONE');
#60210=ORIENTED_EDGE ( 'NONE', *, *, #19773, .T. ) ;
#60211=DIRECTION ( 'NONE',  ( -0.000000000000000000, -1.000000000000000000, -0.000000000000000000 ) ) ;
#60213=STYLED_ITEM ( 'NONE', ( #49771 ), #8754 ) ;
#60219=EDGE_CURVE ( 'NONE', #52535, #50964, #58108, .T. ) ;
#60220=AXIS2_PLACEMENT_3D ( 'NONE', #30506, #2714, #66791 ) ;
#60221=CARTESIAN_POINT ( 'NONE',  ( 33.00000000000002132, 15.00000000000000000, 79.00402776293826435 ) ) ;
#60224=VECTOR ( 'NONE', #14886, 1000.000000000000000 ) ;
#60226=COLOUR_RGB ( '', 0.40784314, 0.44705882, 0.49803922) ;
#60235=CIRCLE ( 'NONE', #44564, 1.000000000000000888 ) ;
#60240=FILL_AREA_STYLE ('',( #12730 ) ) ;
#60253=CARTESIAN_POINT ( 'NONE',  ( 1.000000000000000888, 14.00000000000000000, -60.00402776293827145 ) ) ;
#60264=EDGE_CURVE ( 'NONE', #21109, #58564, #6891, .T. ) ;
#60265=DIRECTION ( 'NONE',  ( -1.000000000000000000, 0.000000000000000000, 6.938893903907222067E-15 ) ) ;
#60271=PLANE ( 'NONE',  #48484 ) ;
#60274=DIRECTION ( 'NONE',  ( 4.625929269271505635E-16, 0.000000000000000000, -1.000000000000000000 ) ) ;
#60277=FILL_AREA_STYLE ('',( #65552 ) ) ;
#60289=( LENGTH_UNIT ( ) NAMED_UNIT ( * ) SI_UNIT ( .MILLI., .METRE. ) );
#60295=EDGE_LOOP ( 'NONE', ( #6702, #59775, #68366 ) ) ;
#60309=VECTOR ( 'NONE', #17668, 1000.000000000000000 ) ;
#60311=CARTESIAN_POINT ( 'NONE',  ( 35.99999999999999289, 5.000000000000000000, -29.00402776293825724 ) ) ;
#60318=DIRECTION ( 'NONE',  ( 0.000000000000000000, 1.000000000000000000, 0.000000000000000000 ) ) ;
#60334=CARTESIAN_POINT ( 'NONE',  ( 20.00000000000001776, 15.00000000000000000, -29.68999999999999417 ) ) ;
#60335=EDGE_CURVE ( 'NONE', #16364, #17287, #10604, .T. ) ;
#60342=ORIENTED_EDGE ( 'NONE', *, *, #5911, .F. ) ;
#60344=CARTESIAN_POINT ( 'NONE',  ( 57.00000000000000000, 14.00000000000000000, 72.50402776293826435 ) ) ;
#60351=ADVANCED_FACE ( 'NONE', ( #49626 ), #33097, .T. ) ;
#60358=PRESENTATION_STYLE_ASSIGNMENT (( #38957 ) ) ;
#60365=( NAMED_UNIT ( * ) SI_UNIT ( $, .STERADIAN. ) SOLID_ANGLE_UNIT ( ) );
#60366=VERTEX_POINT ( 'NONE', #27089 ) ;
#60373=CARTESIAN_POINT ( 'NONE',  ( 16.00000000000001776, 15.00000000000000000, -34.68999999999999773 ) ) ;
#60378=CARTESIAN_POINT ( 'NONE',  ( 0.9999999999999991118, 50.00000000000000000, -60.00000000000000000 ) ) ;
#60398=PRESENTATION_STYLE_ASSIGNMENT (( #1942 ) ) ;
#60399=CARTESIAN_POINT ( 'NONE',  ( 0.9999999999999991118, 50.00000000000000000, 60.00000000000000000 ) ) ;
#60409=ORIENTED_EDGE ( 'NONE', *, *, #15964, .F. ) ;
#60415=( LENGTH_UNIT ( ) NAMED_UNIT ( * ) SI_UNIT ( .MILLI., .METRE. ) );
#60423=CARTESIAN_POINT ( 'NONE',  ( 31.00000000000001421, 14.00000000000000000, 34.49999999999998579 ) ) ;
#60429=ORIENTED_EDGE ( 'NONE', *, *, #42548, .F. ) ;
#60430=VERTEX_POINT ( 'NONE', #61202 ) ;
#60431=( NAMED_UNIT ( * ) PLANE_ANGLE_UNIT ( ) SI_UNIT ( $, .RADIAN. ) );
#60444=EDGE_LOOP ( 'NONE', ( #29565, #33409, #42364, #67048, #41662, #64080, #22365, #4080 ) ) ;
#60450=CARTESIAN_POINT ( 'NONE',  ( 10.00000000000001954, 42.00000000000000000, -28.38386403503541899 ) ) ;
#60461=ORIENTED_EDGE ( 'NONE', *, *, #57769, .F. ) ;
#60467=( LENGTH_UNIT ( ) NAMED_UNIT ( * ) SI_UNIT ( .MILLI., .METRE. ) );
#60468=( NAMED_UNIT ( * ) SI_UNIT ( $, .STERADIAN. ) SOLID_ANGLE_UNIT ( ) );
#60472=CARTESIAN_POINT ( 'NONE',  ( 22.99999999999995026, 0.000000000000000000, 77.00402776293825013 ) ) ;
#60484=FACE_OUTER_BOUND ( 'NONE', #25706, .T. ) ;
#60496=AXIS2_PLACEMENT_3D ( 'NONE', #11511, #11160, #5514 ) ;
#60501=ORIENTED_EDGE ( 'NONE', *, *, #24686, .T. ) ;
#60532=COLOUR_RGB ( '', 0.40784314, 0.44705882, 0.49803922) ;
#60539=VERTEX_POINT ( 'NONE', #36241 ) ;
#60548=SURFACE_STYLE_FILL_AREA ( #28887 ) ;
#60560=EDGE_CURVE ( 'NONE', #52516, #17554, #8056, .T. ) ;
#60562=VECTOR ( 'NONE', #65147, 1000.000000000000000 ) ;
#60571=AXIS2_PLACEMENT_3D ( 'NONE', #38553, #11762, #51844 ) ;
#60576=LINE ( 'NONE', #44130, #21431 ) ;
#60577=FILL_AREA_STYLE_COLOUR ( '', #27016 ) ;
#60579=ADVANCED_FACE ( 'NONE', ( #8781 ), #30208, .T. ) ;
#60586=( GEOMETRIC_REPRESENTATION_CONTEXT ( 3 ) GLOBAL_UNCERTAINTY_ASSIGNED_CONTEXT ( ( #59405 ) ) GLOBAL_UNIT_ASSIGNED_CONTEXT ( ( #15878, #27070, #32035 ) ) REPRESENTATION_CONTEXT ( 'NONE', 'WORKASPACE' ) );
#60601=ORIENTED_EDGE ( 'NONE', *, *, #58867, .F. ) ;
#60604=AXIS2_PLACEMENT_3D ( 'NONE', #36803, #52951, #46679 ) ;
#60615=VERTEX_POINT ( 'NONE', #53754 ) ;
#60619=ORIENTED_EDGE ( 'NONE', *, *, #39255, .F. ) ;
#60620=PLANE ( 'NONE',  #1293 ) ;
#60621=CARTESIAN_POINT ( 'NONE',  ( 32.00000000000000711, 42.00000000000000000, -45.00000000000000000 ) ) ;
#60634=DIRECTION ( 'NONE',  ( 0.000000000000000000, 0.9396926207859104263, -0.3420201433256632173 ) ) ;
#60664=DIRECTION ( 'NONE',  ( 0.000000000000000000, 0.000000000000000000, 1.000000000000000000 ) ) ;
#60668=FACE_OUTER_BOUND ( 'NONE', #13352, .T. ) ;
#60670=DIRECTION ( 'NONE',  ( -1.000000000000000000, -0.000000000000000000, -0.000000000000000000 ) ) ;
#60673=AXIS2_PLACEMENT_3D ( 'NONE', #13671, #35488, #67848 ) ;
#60677=DIRECTION ( 'NONE',  ( 0.000000000000000000, 1.000000000000000000, 0.000000000000000000 ) ) ;
#60678=AXIS2_PLACEMENT_3D ( 'NONE', #43182, #6502, #136 ) ;
#60682=DIRECTION ( 'NONE',  ( 0.000000000000000000, -1.000000000000000000, 0.000000000000000000 ) ) ;
#60691=ORIENTED_EDGE ( 'NONE', *, *, #64740, .F. ) ;
#60699=( LENGTH_UNIT ( ) NAMED_UNIT ( * ) SI_UNIT ( .MILLI., .METRE. ) );
#60701=FILL_AREA_STYLE ('',( #39295 ) ) ;
#60702=ORIENTED_EDGE ( 'NONE', *, *, #52333, .T. ) ;
#60705=DIRECTION ( 'NONE',  ( -0.000000000000000000, -1.000000000000000000, 0.000000000000000000 ) ) ;
#60709=CIRCLE ( 'NONE', #56186, 0.9999999999999995559 ) ;
#60711=FACE_BOUND ( 'NONE', #39299, .T. ) ;
#60715=VERTEX_POINT ( 'NONE', #53434 ) ;
#60729=CARTESIAN_POINT ( 'NONE',  ( 35.99999999999999289, 0.000000000000000000, -37.00402776293825724 ) ) ;
#60730=VECTOR ( 'NONE', #34551, 1000.000000000000000 ) ;
#60741=FILL_AREA_STYLE_COLOUR ( '', #14678 ) ;
#60761=DIRECTION ( 'NONE',  ( 0.000000000000000000, 0.000000000000000000, 1.000000000000000000 ) ) ;
#60762=ORIENTED_EDGE ( 'NONE', *, *, #27537, .F. ) ;
#60763=CARTESIAN_POINT ( 'NONE',  ( 31.00000000000001066, 42.00000000000000000, -4.033029030585349936E-15 ) ) ;
#60765=ORIENTED_EDGE ( 'NONE', *, *, #3838, .F. ) ;
#60767=CARTESIAN_POINT ( 'NONE',  ( 75.83633811589984930, 13.00000000000000178, 66.72655454856716517 ) ) ;
#60770=FILL_AREA_STYLE ('',( #50252 ) ) ;
#60777=DIRECTION ( 'NONE',  ( 1.000000000000000000, 0.000000000000000000, 0.000000000000000000 ) ) ;
#60780=VERTEX_POINT ( 'NONE', #34035 ) ;
#60781=STYLED_ITEM ( 'NONE', ( #29028 ), #18149 ) ;
#60782=DIRECTION ( 'NONE',  ( 0.000000000000000000, -0.7431448254773930229, 0.6691306063588596809 ) ) ;
#60790=VERTEX_POINT ( 'NONE', #33686 ) ;
#60792=CARTESIAN_POINT ( 'NONE',  ( 30.99999999999998579, 5.000000000000000000, -72.00402776293822171 ) ) ;
#60794=( NAMED_UNIT ( * ) SI_UNIT ( $, .STERADIAN. ) SOLID_ANGLE_UNIT ( ) );
#60801=ORIENTED_EDGE ( 'NONE', *, *, #45856, .F. ) ;
#60805=ADVANCED_FACE ( 'NONE', ( #40047 ), #44641, .T. ) ;
#60806=AXIS2_PLACEMENT_3D ( 'NONE', #4238, #26068, #57046 ) ;
#60809=EDGE_CURVE ( 'NONE', #20391, #18094, #62833, .T. ) ;
#60811=EDGE_CURVE ( 'NONE', #48506, #29677, #25214, .T. ) ;
#60817=( NAMED_UNIT ( * ) SI_UNIT ( $, .STERADIAN. ) SOLID_ANGLE_UNIT ( ) );
#60827=FACE_OUTER_BOUND ( 'NONE', #57776, .T. ) ;
#60839=VECTOR ( 'NONE', #37475, 1000.000000000000114 ) ;
#60841=VECTOR ( 'NONE', #68355, 1000.000000000000000 ) ;
#60844=ORIENTED_EDGE ( 'NONE', *, *, #65445, .T. ) ;
#60848=AXIS2_PLACEMENT_3D ( 'NONE', #10563, #50269, #60122 ) ;
#60856=ORIENTED_EDGE ( 'NONE', *, *, #59726, .F. ) ;
#60858=SURFACE_STYLE_USAGE ( .BOTH. , #32067 ) ;
#60867=FILL_AREA_STYLE ('',( #44419 ) ) ;
#60871=ORIENTED_EDGE ( 'NONE', *, *, #60025, .F. ) ;
#60876=DIRECTION ( 'NONE',  ( -0.000000000000000000, 1.000000000000000000, -0.000000000000000000 ) ) ;
#60877=SURFACE_STYLE_FILL_AREA ( #19711 ) ;
#60879=VERTEX_POINT ( 'NONE', #13968 ) ;
#60891=DIRECTION ( 'NONE',  ( 0.000000000000000000, 0.000000000000000000, -1.000000000000000000 ) ) ;
#60922=SURFACE_STYLE_FILL_AREA ( #7807 ) ;
#60929=( LENGTH_UNIT ( ) NAMED_UNIT ( * ) SI_UNIT ( .MILLI., .METRE. ) );
#60934=( GEOMETRIC_REPRESENTATION_CONTEXT ( 3 ) GLOBAL_UNCERTAINTY_ASSIGNED_CONTEXT ( ( #62358 ) ) GLOBAL_UNIT_ASSIGNED_CONTEXT ( ( #25013, #57375, #16230 ) ) REPRESENTATION_CONTEXT ( 'NONE', 'WORKASPACE' ) );
#60940=EDGE_CURVE ( 'NONE', #17236, #69376, #4783, .T. ) ;
#60947=EDGE_CURVE ( 'NONE', #62177, #51568, #20984, .T. ) ;
#60949=UNCERTAINTY_MEASURE_WITH_UNIT (LENGTH_MEASURE( 1.000000000000000082E-05 ), #6648, 'distance_accuracy_value', 'NONE');
#60951=( NAMED_UNIT ( * ) PLANE_ANGLE_UNIT ( ) SI_UNIT ( $, .RADIAN. ) );
#60955=SURFACE_STYLE_FILL_AREA ( #17734 ) ;
#60959=DIRECTION ( 'NONE',  ( 0.000000000000000000, 0.000000000000000000, 1.000000000000000000 ) ) ;
#60961=ORIENTED_EDGE ( 'NONE', *, *, #60054, .T. ) ;
#60971=EDGE_CURVE ( 'NONE', #36334, #8511, #26250, .T. ) ;
#60975=EDGE_CURVE ( 'NONE', #18052, #57872, #42833, .T. ) ;
#60978=CARTESIAN_POINT ( 'NONE',  ( 32.00000000000001421, 15.00000000000000000, -35.50000000000000000 ) ) ;
#60993=DIRECTION ( 'NONE',  ( -1.300977106640434891E-16, 0.000000000000000000, -1.000000000000000000 ) ) ;
#61001=EDGE_LOOP ( 'NONE', ( #63402, #39666, #55781, #38269 ) ) ;
#61008=( LENGTH_UNIT ( ) NAMED_UNIT ( * ) SI_UNIT ( .MILLI., .METRE. ) );
#61010=DIRECTION ( 'NONE',  ( 0.000000000000000000, 1.000000000000000000, 0.000000000000000000 ) ) ;
#61020=STYLED_ITEM ( 'NONE', ( #24714 ), #46922 ) ;
#61024=DIRECTION ( 'NONE',  ( 1.000000000000000000, 0.000000000000000000, -1.300977106640434891E-16 ) ) ;
#61034=ORIENTED_EDGE ( 'NONE', *, *, #20827, .F. ) ;
#61036=AXIS2_PLACEMENT_3D ( 'NONE', #40046, #61110, #12212 ) ;
#61038=CARTESIAN_POINT ( 'NONE',  ( 10.00000000000000711, 50.00000000000000000, -59.99999999999999289 ) ) ;
#61044=CARTESIAN_POINT ( 'NONE',  ( 31.00000000000000355, 42.00000000000000000, -75.00000000000001421 ) ) ;
#61046=DIRECTION ( 'NONE',  ( -0.000000000000000000, 0.000000000000000000, 1.000000000000000000 ) ) ;
#61055=DIRECTION ( 'NONE',  ( -0.000000000000000000, -1.000000000000000000, 0.000000000000000000 ) ) ;
#61056=ORIENTED_EDGE ( 'NONE', *, *, #20150, .F. ) ;
#61060=CARTESIAN_POINT ( 'NONE',  ( 1.000000000000000000, 42.00000000000000000, 79.00402776293826435 ) ) ;
#61078=ORIENTED_EDGE ( 'NONE', *, *, #2059, .F. ) ;
#61096=VECTOR ( 'NONE', #5241, 1000.000000000000000 ) ;
#61102=VECTOR ( 'NONE', #46845, 1000.000000000000000 ) ;
#61105=( LENGTH_UNIT ( ) NAMED_UNIT ( * ) SI_UNIT ( .MILLI., .METRE. ) );
#61106=VECTOR ( 'NONE', #43482, 1000.000000000000000 ) ;
#61110=DIRECTION ( 'NONE',  ( 0.000000000000000000, 1.000000000000000000, 0.000000000000000000 ) ) ;
#61111=( NAMED_UNIT ( * ) SI_UNIT ( $, .STERADIAN. ) SOLID_ANGLE_UNIT ( ) );
#61113=VERTEX_POINT ( 'NONE', #49806 ) ;
#61114=AXIS2_PLACEMENT_3D ( 'NONE', #8706, #30127, #3370 ) ;
#61115=SURFACE_SIDE_STYLE ('',( #66386 ) ) ;
#61118=SURFACE_STYLE_USAGE ( .BOTH. , #18214 ) ;
#61120=ORIENTED_EDGE ( 'NONE', *, *, #38326, .F. ) ;
#61123=COLOUR_RGB ( '', 0.09019608, 0.27058824, 0.51372549) ;
#61127=ORIENTED_EDGE ( 'NONE', *, *, #9064, .T. ) ;
#61135=MECHANICAL_DESIGN_GEOMETRIC_PRESENTATION_REPRESENTATION('',(#25195),#51309);
#61136=SURFACE_STYLE_FILL_AREA ( #60770 ) ;
#61142=ORIENTED_EDGE ( 'NONE', *, *, #10386, .F. ) ;
#61148=ORIENTED_EDGE ( 'NONE', *, *, #43039, .T. ) ;
#61149=SURFACE_STYLE_USAGE ( .BOTH. , #44338 ) ;
#61150=ORIENTED_EDGE ( 'NONE', *, *, #49053, .T. ) ;
#61160=CARTESIAN_POINT ( 'NONE',  ( 0.4142135623730929250, 14.00000000000000355, 35.49999999999999289 ) ) ;
#61161=DIRECTION ( 'NONE',  ( -2.168404344971007882E-16, 0.000000000000000000, -1.000000000000000000 ) ) ;
#61169=DIRECTION ( 'NONE',  ( 1.000000000000000000, -0.000000000000000000, -0.000000000000000000 ) ) ;
#61177=SURFACE_SIDE_STYLE ('',( #7378 ) ) ;
#61179=CARTESIAN_POINT ( 'NONE',  ( 7.000000000000017764, 17.78868675966041835, -9.106839746483067901E-16 ) ) ;
#61182=PRESENTATION_STYLE_ASSIGNMENT (( #33749 ) ) ;
#61189=FILL_AREA_STYLE_COLOUR ( '', #25199 ) ;
#61191=CARTESIAN_POINT ( 'NONE',  ( 0.000000000000000000, 13.00000000000000178, 36.50000000000000000 ) ) ;
#61194=CARTESIAN_POINT ( 'NONE',  ( 29.00000000000002842, 0.000000000000000000, 89.00000000000000000 ) ) ;
#61202=CARTESIAN_POINT ( 'NONE',  ( 16.00000000000001776, 15.00000000000000000, 34.68999999999999062 ) ) ;
#61207=AXIS2_PLACEMENT_3D ( 'NONE', #65775, #3073, #34788 ) ;
#61219=LINE ( 'NONE', #17645, #64657 ) ;
#61223=COLOUR_RGB ( '', 0.40784314, 0.44705882, 0.49803922) ;
#61229=DIRECTION ( 'NONE',  ( 0.000000000000000000, 0.000000000000000000, -1.000000000000000000 ) ) ;
#61235=DIRECTION ( 'NONE',  ( 0.000000000000000000, 0.000000000000000000, -1.000000000000000000 ) ) ;
#61237=EDGE_CURVE ( 'NONE', #46312, #42163, #24771, .T. ) ;
#61240=AXIS2_PLACEMENT_3D ( 'NONE', #36371, #15254, #20491 ) ;
#61242=ORIENTED_EDGE ( 'NONE', *, *, #2760, .F. ) ;
#61243=SURFACE_STYLE_FILL_AREA ( #66161 ) ;
#61245=DIRECTION ( 'NONE',  ( 1.000000000000000000, 0.000000000000000000, 0.000000000000000000 ) ) ;
#61250=EDGE_CURVE ( 'NONE', #13259, #66860, #12716, .T. ) ;
#61256=DIRECTION ( 'NONE',  ( -1.000000000000000000, 0.000000000000000000, 0.000000000000000000 ) ) ;
#61260=CARTESIAN_POINT ( 'NONE',  ( 0.000000000000000000, 13.00000000000000178, 80.00402776293826435 ) ) ;
#61269=AXIS2_PLACEMENT_3D ( 'NONE', #20208, #69117, #25833 ) ;
#61272=DIRECTION ( 'NONE',  ( -0.000000000000000000, 0.000000000000000000, 1.000000000000000000 ) ) ;
#61284=( GEOMETRIC_REPRESENTATION_CONTEXT ( 3 ) GLOBAL_UNCERTAINTY_ASSIGNED_CONTEXT ( ( #60157 ) ) GLOBAL_UNIT_ASSIGNED_CONTEXT ( ( #39117, #34488, #29188 ) ) REPRESENTATION_CONTEXT ( 'NONE', 'WORKASPACE' ) );
#61287=FILL_AREA_STYLE ('',( #60577 ) ) ;
#61295=CYLINDRICAL_SURFACE ( 'NONE', #43947, 5.000000000000000888 ) ;
#61299=AXIS2_PLACEMENT_3D ( 'NONE', #15009, #30434, #24470 ) ;
#61301=CARTESIAN_POINT ( 'NONE',  ( 73.01088739851488185, 5.000000000000000000, -65.71817553072278884 ) ) ;
#61306=FILL_AREA_STYLE_COLOUR ( '', #16327 ) ;
#61316=( LENGTH_UNIT ( ) NAMED_UNIT ( * ) SI_UNIT ( .MILLI., .METRE. ) );
#61317=LINE ( 'NONE', #2157, #16215 ) ;
#61318=EDGE_CURVE ( 'NONE', #17308, #57515, #11619, .T. ) ;
#61337=CARTESIAN_POINT ( 'NONE',  ( 27.99999999999998934, 5.000000000000000000, -37.00402776293828566 ) ) ;
#61341=CARTESIAN_POINT ( 'NONE',  ( 24.70577775730027881, 26.00000000000004619, -27.50000000000000711 ) ) ;
#61351=LINE ( 'NONE', #61679, #36216 ) ;
#61356=VECTOR ( 'NONE', #34332, 1000.000000000000000 ) ;
#61360=CARTESIAN_POINT ( 'NONE',  ( 29.00000000000002842, 42.00000000000000000, 80.00402776293826435 ) ) ;
#61363=SURFACE_STYLE_FILL_AREA ( #1537 ) ;
#61369=EDGE_CURVE ( 'NONE', #8081, #35716, #58775, .T. ) ;
#61380=ORIENTED_EDGE ( 'NONE', *, *, #48246, .T. ) ;
#61382=DIRECTION ( 'NONE',  ( 0.000000000000000000, 1.000000000000000000, 0.000000000000000000 ) ) ;
#61389=( NAMED_UNIT ( * ) SI_UNIT ( $, .STERADIAN. ) SOLID_ANGLE_UNIT ( ) );
#61391=UNCERTAINTY_MEASURE_WITH_UNIT (LENGTH_MEASURE( 1.000000000000000082E-05 ), #60699, 'distance_accuracy_value', 'NONE');
#61410=AXIS2_PLACEMENT_3D ( 'NONE', #12005, #29200, #66152 ) ;
#61419=STYLED_ITEM ( 'NONE', ( #46749 ), #87 ) ;
#61423=CARTESIAN_POINT ( 'NONE',  ( 23.50000000000001776, -3.148064030671221758, -29.68999999999999417 ) ) ;
#61427=PRESENTATION_STYLE_ASSIGNMENT (( #67080 ) ) ;
#61434=DIRECTION ( 'NONE',  ( 1.000000000000000000, 0.000000000000000000, 0.000000000000000000 ) ) ;
#61446=FACE_OUTER_BOUND ( 'NONE', #24715, .T. ) ;
#61460=VERTEX_POINT ( 'NONE', #40830 ) ;
#61463=CARTESIAN_POINT ( 'NONE',  ( 24.68215867018893306, 26.35226335530614961, -27.48643897612095088 ) ) ;
#61471=ORIENTED_EDGE ( 'NONE', *, *, #1201, .T. ) ;
#61477=( NAMED_UNIT ( * ) SI_UNIT ( $, .STERADIAN. ) SOLID_ANGLE_UNIT ( ) );
#61494=LINE ( 'NONE', #55898, #40804 ) ;
#61508=DIRECTION ( 'NONE',  ( 0.000000000000000000, 1.000000000000000000, 0.000000000000000000 ) ) ;
#61509=FILL_AREA_STYLE_COLOUR ( '', #22591 ) ;
#61517=CARTESIAN_POINT ( 'NONE',  ( 29.00000000000002842, 38.70020753820971748, 89.00000000000000000 ) ) ;
#61529=COLOUR_RGB ( '', 0.31764706, 0.68627451, 0.89019608) ;
#61541=CARTESIAN_POINT ( 'NONE',  ( 86.21825843581756033, 5.000000000000000000, 39.83014742847163348 ) ) ;
#61546=( NAMED_UNIT ( * ) SI_UNIT ( $, .STERADIAN. ) SOLID_ANGLE_UNIT ( ) );
#61554=( GEOMETRIC_REPRESENTATION_CONTEXT ( 3 ) GLOBAL_UNCERTAINTY_ASSIGNED_CONTEXT ( ( #52320 ) ) GLOBAL_UNIT_ASSIGNED_CONTEXT ( ( #40269, #28979, #56789 ) ) REPRESENTATION_CONTEXT ( 'NONE', 'WORKASPACE' ) );
#61557=EDGE_LOOP ( 'NONE', ( #10607, #23573, #28766, #41607 ) ) ;
#61566=UNCERTAINTY_MEASURE_WITH_UNIT (LENGTH_MEASURE( 1.000000000000000082E-05 ), #18940, 'distance_accuracy_value', 'NONE');
#61581=ORIENTED_EDGE ( 'NONE', *, *, #42389, .T. ) ;
#61585=( LENGTH_UNIT ( ) NAMED_UNIT ( * ) SI_UNIT ( .MILLI., .METRE. ) );
#61592=FILL_AREA_STYLE ('',( #44113 ) ) ;
#61602=PRESENTATION_STYLE_ASSIGNMENT (( #45148 ) ) ;
#61603=EDGE_LOOP ( 'NONE', ( #4186, #54867, #38355, #55886 ) ) ;
#61607=UNCERTAINTY_MEASURE_WITH_UNIT (LENGTH_MEASURE( 1.000000000000000082E-05 ), #37077, 'distance_accuracy_value', 'NONE');
#61609=COLOUR_RGB ( '', 0.40784314, 0.44705882, 0.49803922) ;
#61610=CARTESIAN_POINT ( 'NONE',  ( 30.99999999999998579, 0.000000000000000000, 72.00402776293822171 ) ) ;
#61611=DIRECTION ( 'NONE',  ( 0.000000000000000000, 0.000000000000000000, -1.000000000000000000 ) ) ;
#61622=( GEOMETRIC_REPRESENTATION_CONTEXT ( 3 ) GLOBAL_UNCERTAINTY_ASSIGNED_CONTEXT ( ( #32194 ) ) GLOBAL_UNIT_ASSIGNED_CONTEXT ( ( #45735, #50977, #14368 ) ) REPRESENTATION_CONTEXT ( 'NONE', 'WORKASPACE' ) );
#61624=SURFACE_SIDE_STYLE ('',( #40220 ) ) ;
#61628=EDGE_LOOP ( 'NONE', ( #19161, #67733 ) ) ;
#61637=MECHANICAL_DESIGN_GEOMETRIC_PRESENTATION_REPRESENTATION('',(#51515),#69537);
#61642=STYLED_ITEM ( 'NONE', ( #24733 ), #19692 ) ;
#61643=FILL_AREA_STYLE_COLOUR ( '', #44786 ) ;
#61646=ORIENTED_EDGE ( 'NONE', *, *, #14449, .F. ) ;
#61650=DIRECTION ( 'NONE',  ( 0.000000000000000000, 0.9396926207859082059, 0.3420201433256693790 ) ) ;
#61658=COLOUR_RGB ( '', 0.66274510, 0.83137255, 0.94901961) ;
#61664=CARTESIAN_POINT ( 'NONE',  ( 23.67676504785522340, 24.55989583710076474, -27.19000000000005102 ) ) ;
#61667=EDGE_CURVE ( 'NONE', #50347, #46312, #66703, .T. ) ;
#61673=ORIENTED_EDGE ( 'NONE', *, *, #12206, .T. ) ;
#61675=ADVANCED_FACE ( 'NONE', ( #9152 ), #30568, .T. ) ;
#61677=COLOUR_RGB ( '', 0.31764706, 0.68627451, 0.89019608) ;
#61678=ADVANCED_FACE ( 'NONE', ( #47161 ), #5559, .T. ) ;
#61679=CARTESIAN_POINT ( 'NONE',  ( 22.99999999999995026, 0.000000000000000000, -32.00402776293824303 ) ) ;
#61681=CARTESIAN_POINT ( 'NONE',  ( 29.00000000000000000, 35.42594141563417054, -80.00402776293826435 ) ) ;
#61689=LINE ( 'NONE', #35343, #60839 ) ;
#61692=( GEOMETRIC_REPRESENTATION_CONTEXT ( 3 ) GLOBAL_UNCERTAINTY_ASSIGNED_CONTEXT ( ( #15857 ) ) GLOBAL_UNIT_ASSIGNED_CONTEXT ( ( #2658, #34371, #35422 ) ) REPRESENTATION_CONTEXT ( 'NONE', 'WORKASPACE' ) );
#61700=( NAMED_UNIT ( * ) SI_UNIT ( $, .STERADIAN. ) SOLID_ANGLE_UNIT ( ) );
#61707=PRESENTATION_STYLE_ASSIGNMENT (( #19861 ) ) ;
#61710=MECHANICAL_DESIGN_GEOMETRIC_PRESENTATION_REPRESENTATION('',(#48271),#57213);
#61712=PRESENTATION_STYLE_ASSIGNMENT (( #62436 ) ) ;
#61717=AXIS2_PLACEMENT_3D ( 'NONE', #48626, #38423, #28478 ) ;
#61724=CARTESIAN_POINT ( 'NONE',  ( 28.00000000000000000, 5.569094604152798667, 2.026984667724099243 ) ) ;
#61729=STYLED_ITEM ( 'NONE', ( #53746 ), #51534 ) ;
#61739=DIRECTION ( 'NONE',  ( 1.000000000000000000, -0.000000000000000000, -1.300977106640434891E-16 ) ) ;
#61752=EDGE_CURVE ( 'NONE', #67697, #26455, #10866, .T. ) ;
#61763=( LENGTH_UNIT ( ) NAMED_UNIT ( * ) SI_UNIT ( .MILLI., .METRE. ) );
#61768=CIRCLE ( 'NONE', #69677, 16.00000000000000711 ) ;
#61771=DIRECTION ( 'NONE',  ( -1.000000000000000000, -0.000000000000000000, -0.000000000000000000 ) ) ;
#61776=EDGE_CURVE ( 'NONE', #52976, #28531, #67096, .T. ) ;
#61779=MECHANICAL_DESIGN_GEOMETRIC_PRESENTATION_REPRESENTATION('',(#29202),#58448);
#61793=DIRECTION ( 'NONE',  ( 1.000000000000000000, 0.000000000000000000, -0.000000000000000000 ) ) ;
#61803=ADVANCED_FACE ( 'NONE', ( #61446 ), #8001, .T. ) ;
#61812=FILL_AREA_STYLE_COLOUR ( '', #22303 ) ;
#61816=CARTESIAN_POINT ( 'NONE',  ( 57.00000000000000000, 16.00000000000000000, -60.00402776293825724 ) ) ;
#61817=EDGE_LOOP ( 'NONE', ( #43806, #3555, #3954, #34313 ) ) ;
#61819=DIRECTION ( 'NONE',  ( 0.000000000000000000, 0.000000000000000000, 1.000000000000000000 ) ) ;
#61824=STYLED_ITEM ( 'NONE', ( #58353 ), #34550 ) ;
#61825=( NAMED_UNIT ( * ) PLANE_ANGLE_UNIT ( ) SI_UNIT ( $, .RADIAN. ) );
#61830=DIRECTION ( 'NONE',  ( 1.000000000000000000, -0.000000000000000000, -0.000000000000000000 ) ) ;
#61835=CIRCLE ( 'NONE', #43927, 5.000000000000000888 ) ;
#61839=CARTESIAN_POINT ( 'NONE',  ( 27.00000000000001776, 15.00000000000000000, 35.50000000000000000 ) ) ;
#61857=CARTESIAN_POINT ( 'NONE',  ( 31.00000000000001421, 15.00000000000000000, 36.49999999999999289 ) ) ;
#61861=( NAMED_UNIT ( * ) PLANE_ANGLE_UNIT ( ) SI_UNIT ( $, .RADIAN. ) );
#61862=( LENGTH_UNIT ( ) NAMED_UNIT ( * ) SI_UNIT ( .MILLI., .METRE. ) );
#61869=DIRECTION ( 'NONE',  ( 0.000000000000000000, 0.000000000000000000, 1.000000000000000000 ) ) ;
#61873=AXIS2_PLACEMENT_3D ( 'NONE', #64068, #4983, #36707 ) ;
#61877=ADVANCED_FACE ( 'NONE', ( #20286 ), #56891, .T. ) ;
#61888=EDGE_LOOP ( 'NONE', ( #69256, #18768, #16612, #20649, #9522, #56445 ) ) ;
#61899=DIRECTION ( 'NONE',  ( 0.000000000000000000, 0.000000000000000000, -1.000000000000000000 ) ) ;
#61901=VERTEX_POINT ( 'NONE', #21321 ) ;
#61909=( NAMED_UNIT ( * ) SI_UNIT ( $, .STERADIAN. ) SOLID_ANGLE_UNIT ( ) );
#61932=EDGE_CURVE ( 'NONE', #55787, #32128, #54380, .T. ) ;
#61933=ORIENTED_EDGE ( 'NONE', *, *, #41103, .F. ) ;
#61934=SURFACE_SIDE_STYLE ('',( #67225 ) ) ;
#61943=STYLED_ITEM ( 'NONE', ( #65549 ), #35265 ) ;
#61947=EDGE_LOOP ( 'NONE', ( #51638, #38709, #20082, #12167 ) ) ;
#61948=CARTESIAN_POINT ( 'NONE',  ( 22.29422224269975672, 26.00000000000000355, -27.50000000000000711 ) ) ;
#61950=CARTESIAN_POINT ( 'NONE',  ( 31.00000000000000355, 43.00000000000000000, -36.50000000000000000 ) ) ;
#61957=DIRECTION ( 'NONE',  ( 1.734723475976805517E-15, 0.000000000000000000, -1.000000000000000000 ) ) ;
#61970=STYLED_ITEM ( 'NONE', ( #21490 ), #60351 ) ;
#61972=DIRECTION ( 'NONE',  ( 0.000000000000000000, 1.000000000000000000, 0.000000000000000000 ) ) ;
#61983=VERTEX_POINT ( 'NONE', #65631 ) ;
#61987=( NAMED_UNIT ( * ) SI_UNIT ( $, .STERADIAN. ) SOLID_ANGLE_UNIT ( ) );
#62007=COLOUR_RGB ( '', 0.09019608, 0.27058824, 0.51372549) ;
#62011=SURFACE_STYLE_FILL_AREA ( #7855 ) ;
#62018=CARTESIAN_POINT ( 'NONE',  ( 8.000000000000030198, 0.000000000000000000, -29.00402776293826079 ) ) ;
#62039=AXIS2_PLACEMENT_3D ( 'NONE', #48049, #53617, #37844 ) ;
#62047=PRODUCT_DEFINITION_CONTEXT ( 'detailed design', #45596, 'design' ) ;
#62052=AXIS2_PLACEMENT_3D ( 'NONE', #30618, #57727, #52122 ) ;
#62065=AXIS2_PLACEMENT_3D ( 'NONE', #48449, #15723, #21669 ) ;
#62068=( GEOMETRIC_REPRESENTATION_CONTEXT ( 3 ) GLOBAL_UNCERTAINTY_ASSIGNED_CONTEXT ( ( #14296 ) ) GLOBAL_UNIT_ASSIGNED_CONTEXT ( ( #11571, #27723, #23856 ) ) REPRESENTATION_CONTEXT ( 'NONE', 'WORKASPACE' ) );
#62075=DIRECTION ( 'NONE',  ( -0.000000000000000000, 1.000000000000000000, -0.000000000000000000 ) ) ;
#62083=( NAMED_UNIT ( * ) PLANE_ANGLE_UNIT ( ) SI_UNIT ( $, .RADIAN. ) );
#62124=FILL_AREA_STYLE_COLOUR ( '', #38000 ) ;
#62128=SURFACE_STYLE_FILL_AREA ( #7625 ) ;
#62131=CIRCLE ( 'NONE', #3546, 110.0000000000000142 ) ;
#62133=LINE ( 'NONE', #34377, #42483 ) ;
#62134=UNCERTAINTY_MEASURE_WITH_UNIT (LENGTH_MEASURE( 1.000000000000000082E-05 ), #66825, 'distance_accuracy_value', 'NONE');
#62151=( NAMED_UNIT ( * ) SI_UNIT ( $, .STERADIAN. ) SOLID_ANGLE_UNIT ( ) );
#62152=MECHANICAL_DESIGN_GEOMETRIC_PRESENTATION_REPRESENTATION('',(#7144),#7304);
#62155=CARTESIAN_POINT ( 'NONE',  ( 23.50000000000001776, 43.00000000000000000, -29.68999999999999417 ) ) ;
#62157=ADVANCED_FACE ( 'NONE', ( #35006 ), #62434, .F. ) ;
#62159=VECTOR ( 'NONE', #37301, 1000.000000000000000 ) ;
#62165=APPLICATION_CONTEXT ( 'automotive_design' ) ;
#62166=MECHANICAL_DESIGN_GEOMETRIC_PRESENTATION_REPRESENTATION('',(#61020),#26227);
#62171=VERTEX_POINT ( 'NONE', #67721 ) ;
#62177=VERTEX_POINT ( 'NONE', #68773 ) ;
#62182=CARTESIAN_POINT ( 'NONE',  ( 57.00000000000000000, 5.000000000000000000, 65.00402776293825013 ) ) ;
#62189=DIRECTION ( 'NONE',  ( -1.000000000000000000, 0.000000000000000000, 1.300977106640434891E-16 ) ) ;
#62190=MECHANICAL_DESIGN_GEOMETRIC_PRESENTATION_REPRESENTATION('',(#48742),#8288);
#62195=ORIENTED_EDGE ( 'NONE', *, *, #9390, .F. ) ;
#62201=CIRCLE ( 'NONE', #31866, 110.0000000000000142 ) ;
#62204=LINE ( 'NONE', #14028, #69679 ) ;
#62219=MECHANICAL_DESIGN_GEOMETRIC_PRESENTATION_REPRESENTATION('',(#27346),#40920);
#62225=DIRECTION ( 'NONE',  ( 1.000000000000000000, 0.000000000000000000, 0.000000000000000000 ) ) ;
#62226=DIRECTION ( 'NONE',  ( 1.000000000000000000, -0.000000000000000000, 1.982541115402068561E-16 ) ) ;
#62234=CYLINDRICAL_SURFACE ( 'NONE', #52801, 2.499999999999998668 ) ;
#62238=CARTESIAN_POINT ( 'NONE',  ( 98.00000000000000000, 14.00000000000000000, 12.50000000000000178 ) ) ;
#62240=ORIENTED_EDGE ( 'NONE', *, *, #20519, .F. ) ;
#62244=CARTESIAN_POINT ( 'NONE',  ( 28.00000000000000000, 38.70020753820971748, -89.00000000000000000 ) ) ;
#62252=SURFACE_STYLE_FILL_AREA ( #65893 ) ;
#62254=EDGE_CURVE ( 'NONE', #31566, #23198, #26312, .T. ) ;
#62256=DIRECTION ( 'NONE',  ( -0.000000000000000000, 1.000000000000000000, -0.000000000000000000 ) ) ;
#62265=CARTESIAN_POINT ( 'NONE',  ( 32.00000000000002132, 43.00000000000000000, 79.00402776293823592 ) ) ;
#62269=ORIENTED_EDGE ( 'NONE', *, *, #28386, .F. ) ;
#62271=UNCERTAINTY_MEASURE_WITH_UNIT (LENGTH_MEASURE( 1.000000000000000082E-05 ), #38594, 'distance_accuracy_value', 'NONE');
#62276=DIRECTION ( 'NONE',  ( 0.000000000000000000, 1.000000000000000000, 0.000000000000000000 ) ) ;
#62279=ADVANCED_FACE ( 'NONE', ( #41707 ), #63130, .T. ) ;
#62287=VERTEX_POINT ( 'NONE', #6116 ) ;
#62289=UNCERTAINTY_MEASURE_WITH_UNIT (LENGTH_MEASURE( 1.000000000000000082E-05 ), #44266, 'distance_accuracy_value', 'NONE');
#62291=EDGE_CURVE ( 'NONE', #51395, #51817, #53611, .T. ) ;
#62298=( LENGTH_UNIT ( ) NAMED_UNIT ( * ) SI_UNIT ( .MILLI., .METRE. ) );
#62306=ORIENTED_EDGE ( 'NONE', *, *, #42396, .F. ) ;
#62308=( NAMED_UNIT ( * ) SI_UNIT ( $, .STERADIAN. ) SOLID_ANGLE_UNIT ( ) );
#62309=FACE_OUTER_BOUND ( 'NONE', #3756, .T. ) ;
#62310=( BOUNDED_CURVE ( )  B_SPLINE_CURVE ( 3, ( #50368, #24317, #12718, #23622 ),
 .UNSPECIFIED., .F., .T. ) 
 B_SPLINE_CURVE_WITH_KNOTS ( ( 4, 4 ),
 ( 4.712388980384691450, 5.550147021341966358 ),
 .UNSPECIFIED. ) 
 CURVE ( )  GEOMETRIC_REPRESENTATION_ITEM ( )  RATIONAL_B_SPLINE_CURVE ( ( 1.000000000000000000, 0.9423636384284010958, 0.9423636384284010958, 1.000000000000000000 ) ) 
 REPRESENTATION_ITEM ( '' )  );
#62312=CARTESIAN_POINT ( 'NONE',  ( 22.99999999999996092, 5.000000000000000000, -77.00402776293825013 ) ) ;
#62319=( GEOMETRIC_REPRESENTATION_CONTEXT ( 3 ) GLOBAL_UNCERTAINTY_ASSIGNED_CONTEXT ( ( #39835 ) ) GLOBAL_UNIT_ASSIGNED_CONTEXT ( ( #69086, #9993, #25802 ) ) REPRESENTATION_CONTEXT ( 'NONE', 'WORKASPACE' ) );
#62322=LINE ( 'NONE', #49788, #32104 ) ;
#62325=AXIS2_PLACEMENT_3D ( 'NONE', #43784, #425, #17039 ) ;
#62329=ORIENTED_EDGE ( 'NONE', *, *, #50376, .F. ) ;
#62333=EDGE_CURVE ( 'NONE', #45721, #16530, #1564, .T. ) ;
#62339=EDGE_CURVE ( 'NONE', #30128, #38068, #11034, .T. ) ;
#62349=AXIS2_PLACEMENT_3D ( 'NONE', #25400, #31020, #51447 ) ;
#62358=UNCERTAINTY_MEASURE_WITH_UNIT (LENGTH_MEASURE( 1.000000000000000082E-05 ), #25013, 'distance_accuracy_value', 'NONE');
#62359=DIRECTION ( 'NONE',  ( 0.000000000000000000, 0.000000000000000000, 1.000000000000000000 ) ) ;
#62378=EDGE_LOOP ( 'NONE', ( #61581, #21036, #9238, #35263 ) ) ;
#62379=EDGE_CURVE ( 'NONE', #23681, #56835, #12862, .T. ) ;
#62380=SURFACE_STYLE_FILL_AREA ( #52547 ) ;
#62408=SURFACE_SIDE_STYLE ('',( #45907 ) ) ;
#62412=ORIENTED_EDGE ( 'NONE', *, *, #29359, .T. ) ;
#62415=SHAPE_DEFINITION_REPRESENTATION ( #15361, #40670 ) ;
#62419=CARTESIAN_POINT ( 'NONE',  ( 32.00000000000002132, 50.00000000000000000, 59.99999999999999289 ) ) ;
#62434=SPHERICAL_SURFACE ( 'NONE', #38773, 1.000000000000000000 ) ;
#62436=SURFACE_STYLE_USAGE ( .BOTH. , #2946 ) ;
#62446=VECTOR ( 'NONE', #50247, 1000.000000000000000 ) ;
#62457=ADVANCED_FACE ( 'NONE', ( #39545 ), #7502, .F. ) ;
#62463=ORIENTED_EDGE ( 'NONE', *, *, #42389, .F. ) ;
#62474=CARTESIAN_POINT ( 'NONE',  ( 98.00000000000000000, 5.000000000000000000, 5.000000000000004441 ) ) ;
#62475=CARTESIAN_POINT ( 'NONE',  ( 22.00000000000002132, 50.00000000000000000, 59.99999999999999289 ) ) ;
#62478=SURFACE_STYLE_USAGE ( .BOTH. , #57923 ) ;
#62484=ADVANCED_FACE ( 'NONE', ( #23674 ), #66597, .F. ) ;
#62489=PLANE ( 'NONE',  #69686 ) ;
#62496=EDGE_LOOP ( 'NONE', ( #53625, #9769, #6026, #47162 ) ) ;
#62505=EDGE_CURVE ( 'NONE', #60539, #17255, #2025, .T. ) ;
#62509=DIRECTION ( 'NONE',  ( 0.000000000000000000, -1.000000000000000000, 3.469446951953611033E-15 ) ) ;
#62516=CARTESIAN_POINT ( 'NONE',  ( 0.000000000000000000, 43.00000000000000000, 0.000000000000000000 ) ) ;
#62523=CIRCLE ( 'NONE', #34414, 3.499999999999999556 ) ;
#62529=DIRECTION ( 'NONE',  ( -0.000000000000000000, -0.000000000000000000, -1.000000000000000000 ) ) ;
#62535=CIRCLE ( 'NONE', #41246, 4.999999999999997335 ) ;
#62543=CARTESIAN_POINT ( 'NONE',  ( 1.000000000000000000, 42.00000000000000000, -80.00402776293826435 ) ) ;
#62548=SURFACE_SIDE_STYLE ('',( #64563 ) ) ;
#62550=DIRECTION ( 'NONE',  ( 0.000000000000000000, 1.000000000000000000, 0.000000000000000000 ) ) ;
#62555=DIRECTION ( 'NONE',  ( 0.000000000000000000, 0.000000000000000000, -1.000000000000000000 ) ) ;
#62556=COLOUR_RGB ( '', 0.09019608, 0.27058824, 0.51372549) ;
#62559=CIRCLE ( 'NONE', #13099, 1.000000000000002442 ) ;
#62563=( GEOMETRIC_REPRESENTATION_CONTEXT ( 3 ) GLOBAL_UNCERTAINTY_ASSIGNED_CONTEXT ( ( #36320 ) ) GLOBAL_UNIT_ASSIGNED_CONTEXT ( ( #14261, #35725, #61389 ) ) REPRESENTATION_CONTEXT ( 'NONE', 'WORKASPACE' ) );
#62565=FILL_AREA_STYLE ('',( #29874 ) ) ;
#62568=ORIENTED_EDGE ( 'NONE', *, *, #6195, .F. ) ;
#62574=( NAMED_UNIT ( * ) PLANE_ANGLE_UNIT ( ) SI_UNIT ( $, .RADIAN. ) );
#62578=SURFACE_STYLE_FILL_AREA ( #3449 ) ;
#62580=VERTEX_POINT ( 'NONE', #18643 ) ;
#62603=EDGE_LOOP ( 'NONE', ( #17819, #3468, #41107, #28544, #65964 ) ) ;
#62605=STYLED_ITEM ( 'NONE', ( #31900 ), #58619 ) ;
#62607=CARTESIAN_POINT ( 'NONE',  ( 10.00000000000002132, 50.00000000000000000, 60.00000000000000000 ) ) ;
#62620=DIRECTION ( 'NONE',  ( -0.000000000000000000, 0.000000000000000000, -1.000000000000000000 ) ) ;
#62624=ORIENTED_EDGE ( 'NONE', *, *, #64472, .F. ) ;
#62632=VERTEX_POINT ( 'NONE', #40456 ) ;
#62635=FACE_OUTER_BOUND ( 'NONE', #61603, .T. ) ;
#62642=EDGE_CURVE ( 'NONE', #13573, #57372, #36889, .T. ) ;
#62643=CARTESIAN_POINT ( 'NONE',  ( 32.00000000000000711, 43.00000000000000000, -75.00000000000001421 ) ) ;
#62647=( GEOMETRIC_REPRESENTATION_CONTEXT ( 3 ) GLOBAL_UNCERTAINTY_ASSIGNED_CONTEXT ( ( #8855 ) ) GLOBAL_UNIT_ASSIGNED_CONTEXT ( ( #29747, #62083, #5411 ) ) REPRESENTATION_CONTEXT ( 'NONE', 'WORKASPACE' ) );
#62651=DIRECTION ( 'NONE',  ( 0.000000000000000000, 0.000000000000000000, -1.000000000000000000 ) ) ;
#62662=VECTOR ( 'NONE', #28895, 1000.000000000000000 ) ;
#62682=CARTESIAN_POINT ( 'NONE',  ( 31.00000000000002132, 42.00000000000000000, 79.00402776293823592 ) ) ;
#62692=CARTESIAN_POINT ( 'NONE',  ( 22.99999999999999645, 0.000000000000000000, -72.00402776293825013 ) ) ;
#62695=DIRECTION ( 'NONE',  ( 1.000000000000000000, 0.000000000000000000, 0.000000000000000000 ) ) ;
#62699=( NAMED_UNIT ( * ) SI_UNIT ( $, .STERADIAN. ) SOLID_ANGLE_UNIT ( ) );
#62710=( LENGTH_UNIT ( ) NAMED_UNIT ( * ) SI_UNIT ( .MILLI., .METRE. ) );
#62719=EDGE_CURVE ( 'NONE', #37912, #4579, #45406, .T. ) ;
#62720=CARTESIAN_POINT ( 'NONE',  ( 24.29733203266260944, 24.87668888026472658, -27.31792417249472749 ) ) ;
#62723=LINE ( 'NONE', #31069, #25783 ) ;
#62724=EDGE_LOOP ( 'NONE', ( #14268, #41224, #2814, #30929 ) ) ;
#62726=ADVANCED_FACE ( 'NONE', ( #58648 ), #4464, .F. ) ;
#62734=VECTOR ( 'NONE', #45477, 1000.000000000000000 ) ;
#62748=DIRECTION ( 'NONE',  ( -0.000000000000000000, -0.000000000000000000, 1.000000000000000000 ) ) ;
#62749=ORIENTED_EDGE ( 'NONE', *, *, #16706, .F. ) ;
#62752=VERTEX_POINT ( 'NONE', #42192 ) ;
#62755=DIRECTION ( 'NONE',  ( 0.000000000000000000, 0.000000000000000000, -1.000000000000000000 ) ) ;
#62759=CARTESIAN_POINT ( 'NONE',  ( 36.00000000000002842, 5.000000000000000000, 29.00402776293825724 ) ) ;
#62761=( GEOMETRIC_REPRESENTATION_CONTEXT ( 3 ) GLOBAL_UNCERTAINTY_ASSIGNED_CONTEXT ( ( #66375 ) ) GLOBAL_UNIT_ASSIGNED_CONTEXT ( ( #52714, #19282, #51664 ) ) REPRESENTATION_CONTEXT ( 'NONE', 'WORKASPACE' ) );
#62763=VERTEX_POINT ( 'NONE', #60373 ) ;
#62767=CARTESIAN_POINT ( 'NONE',  ( 27.99999999999999289, 34.36176364315826248, -80.00402776293826435 ) ) ;
#62772=DIRECTION ( 'NONE',  ( 0.000000000000000000, -1.000000000000000000, 0.000000000000000000 ) ) ;
#62775=STYLED_ITEM ( 'NONE', ( #37622 ), #43661 ) ;
#62781=DIRECTION ( 'NONE',  ( -0.000000000000000000, 1.000000000000000000, -0.000000000000000000 ) ) ;
#62783=ORIENTED_EDGE ( 'NONE', *, *, #16151, .T. ) ;
#62789=AXIS2_PLACEMENT_3D ( 'NONE', #39364, #49209, #27013 ) ;
#62796=EDGE_LOOP ( 'NONE', ( #21237, #20008, #62568, #56815 ) ) ;
#62801=DIRECTION ( 'NONE',  ( -0.000000000000000000, -1.000000000000000000, 0.000000000000000000 ) ) ;
#62802=EDGE_CURVE ( 'NONE', #55787, #45031, #34161, .T. ) ;
#62813=FACE_OUTER_BOUND ( 'NONE', #47229, .T. ) ;
#62816=ADVANCED_FACE ( 'NONE', ( #60711, #49498 ), #22402, .T. ) ;
#62821=MECHANICAL_DESIGN_GEOMETRIC_PRESENTATION_REPRESENTATION('',(#31391),#58366);
#62822=UNCERTAINTY_MEASURE_WITH_UNIT (LENGTH_MEASURE( 1.000000000000000082E-05 ), #12110, 'distance_accuracy_value', 'NONE');
#62827=( LENGTH_UNIT ( ) NAMED_UNIT ( * ) SI_UNIT ( .MILLI., .METRE. ) );
#62828=MECHANICAL_DESIGN_GEOMETRIC_PRESENTATION_REPRESENTATION('',(#31401),#44909);
#62833=LINE ( 'NONE', #35440, #45250 ) ;
#62837=AXIS2_PLACEMENT_3D ( 'NONE', #37121, #43774, #6095 ) ;
#62842=MECHANICAL_DESIGN_GEOMETRIC_PRESENTATION_REPRESENTATION('',(#61729),#21271);
#62852=DIRECTION ( 'NONE',  ( 0.000000000000000000, 1.000000000000000000, -0.000000000000000000 ) ) ;
#62855=DIRECTION ( 'NONE',  ( 0.000000000000000000, 1.000000000000000000, -0.000000000000000000 ) ) ;
#62856=( NAMED_UNIT ( * ) PLANE_ANGLE_UNIT ( ) SI_UNIT ( $, .RADIAN. ) );
#62860=CARTESIAN_POINT ( 'NONE',  ( 10.00000000000001954, 50.00000000000000000, 60.00000000000000000 ) ) ;
#62861=ORIENTED_EDGE ( 'NONE', *, *, #30307, .F. ) ;
#62875=CARTESIAN_POINT ( 'NONE',  ( 10.00000000000000178, 43.00000000000000000, -90.00000000000000000 ) ) ;
#62876=DIRECTION ( 'NONE',  ( 0.000000000000000000, 0.000000000000000000, -1.000000000000000000 ) ) ;
#62883=ORIENTED_EDGE ( 'NONE', *, *, #44446, .T. ) ;
#62893=FILL_AREA_STYLE_COLOUR ( '', #27505 ) ;
#62899=SURFACE_STYLE_USAGE ( .BOTH. , #14042 ) ;
#62907=AXIS2_PLACEMENT_3D ( 'NONE', #35526, #41868, #46457 ) ;
#62908=PRESENTATION_STYLE_ASSIGNMENT (( #4148 ) ) ;
#62909=UNCERTAINTY_MEASURE_WITH_UNIT (LENGTH_MEASURE( 1.000000000000000082E-05 ), #53041, 'distance_accuracy_value', 'NONE');
#62916=CARTESIAN_POINT ( 'NONE',  ( 27.00000000000001776, 15.00000000000000000, 29.68999999999999417 ) ) ;
#62919=ORIENTED_EDGE ( 'NONE', *, *, #53728, .F. ) ;
#62924=DIRECTION ( 'NONE',  ( 0.000000000000000000, -0.8823529411764736707, -0.4705882352941119229 ) ) ;
#62935=DIRECTION ( 'NONE',  ( 1.000000000000000000, -0.000000000000000000, -1.300977106640434891E-16 ) ) ;
#62937=ORIENTED_EDGE ( 'NONE', *, *, #67338, .T. ) ;
#62939=CIRCLE ( 'NONE', #48384, 4.999999999999990230 ) ;
#62941=AXIS2_PLACEMENT_3D ( 'NONE', #234, #43283, #55844 ) ;
#62943=DIRECTION ( 'NONE',  ( 0.000000000000000000, 0.000000000000000000, -1.000000000000000000 ) ) ;
#62948=( GEOMETRIC_REPRESENTATION_CONTEXT ( 3 ) GLOBAL_UNCERTAINTY_ASSIGNED_CONTEXT ( ( #62271 ) ) GLOBAL_UNIT_ASSIGNED_CONTEXT ( ( #38594, #31864, #32549 ) ) REPRESENTATION_CONTEXT ( 'NONE', 'WORKASPACE' ) );
#62949=VERTEX_POINT ( 'NONE', #44256 ) ;
#62955=DIRECTION ( 'NONE',  ( 0.000000000000000000, 0.000000000000000000, 1.000000000000000000 ) ) ;
#62957=AXIS2_PLACEMENT_3D ( 'NONE', #64358, #38012, #27727 ) ;
#62960=ORIENTED_EDGE ( 'NONE', *, *, #53231, .F. ) ;
#62976=MECHANICAL_DESIGN_GEOMETRIC_PRESENTATION_REPRESENTATION('',(#32635),#19172);
#62978=CARTESIAN_POINT ( 'NONE',  ( 22.41794263251858155, 25.31045447836329743, 27.43560882268856815 ) ) ;
#62981=EDGE_LOOP ( 'NONE', ( #62783, #35497, #33562, #5067 ) ) ;
#62990=VERTEX_POINT ( 'NONE', #25099 ) ;
#62993=VECTOR ( 'NONE', #68204, 1000.000000000000000 ) ;
#62995=CARTESIAN_POINT ( 'NONE',  ( 22.70255002340108774, 27.12311843165924330, -27.31797491105104569 ) ) ;
#62996=PLANE ( 'NONE',  #65120 ) ;
#63001=UNCERTAINTY_MEASURE_WITH_UNIT (LENGTH_MEASURE( 1.000000000000000082E-05 ), #38503, 'distance_accuracy_value', 'NONE');
#63009=STYLED_ITEM ( 'NONE', ( #6008 ), #52676 ) ;
#63027=ORIENTED_EDGE ( 'NONE', *, *, #54007, .F. ) ;
#63029=DIRECTION ( 'NONE',  ( 0.000000000000000000, 0.000000000000000000, -1.000000000000000000 ) ) ;
#63045=VECTOR ( 'NONE', #63618, 1000.000000000000000 ) ;
#63048=CIRCLE ( 'NONE', #20364, 17.00000000000000000 ) ;
#63056=ORIENTED_EDGE ( 'NONE', *, *, #2299, .F. ) ;
#63073=SURFACE_STYLE_FILL_AREA ( #69065 ) ;
#63074=MECHANICAL_DESIGN_GEOMETRIC_PRESENTATION_REPRESENTATION('',(#4616),#27093);
#63082=VECTOR ( 'NONE', #57362, 1000.000000000000000 ) ;
#63083=CARTESIAN_POINT ( 'NONE',  ( 98.00000000000000000, 16.00000000000000000, 0.000000000000000000 ) ) ;
#63097=AXIS2_PLACEMENT_3D ( 'NONE', #41663, #14543, #8246 ) ;
#63098=DIRECTION ( 'NONE',  ( -0.3361263392814427542, 0.000000000000000000, 0.9418169057949938860 ) ) ;
#63107=SURFACE_STYLE_USAGE ( .BOTH. , #19845 ) ;
#63111=CARTESIAN_POINT ( 'NONE',  ( 0.000000000000000000, 43.00000000000000000, 0.000000000000000000 ) ) ;
#63113=EDGE_CURVE ( 'NONE', #63408, #17554, #44448, .T. ) ;
#63114=AXIS2_PLACEMENT_3D ( 'NONE', #12048, #67256, #46552 ) ;
#63115=DIRECTION ( 'NONE',  ( 0.000000000000000000, 0.000000000000000000, 1.000000000000000000 ) ) ;
#63124=MECHANICAL_DESIGN_GEOMETRIC_PRESENTATION_REPRESENTATION('',(#44042),#13659);
#63128=UNCERTAINTY_MEASURE_WITH_UNIT (LENGTH_MEASURE( 1.000000000000000082E-05 ), #5209, 'distance_accuracy_value', 'NONE');
#63130=CYLINDRICAL_SURFACE ( 'NONE', #53315, 0.9999999999999993339 ) ;
#63143=STYLED_ITEM ( 'NONE', ( #54221 ), #46200 ) ;
#63159=EDGE_CURVE ( 'NONE', #20856, #22897, #3154, .T. ) ;
#63163=( GEOMETRIC_REPRESENTATION_CONTEXT ( 3 ) GLOBAL_UNCERTAINTY_ASSIGNED_CONTEXT ( ( #64443 ) ) GLOBAL_UNIT_ASSIGNED_CONTEXT ( ( #46756, #62856, #63569 ) ) REPRESENTATION_CONTEXT ( 'NONE', 'WORKASPACE' ) );
#63172=DIRECTION ( 'NONE',  ( 0.000000000000000000, 0.000000000000000000, -1.000000000000000000 ) ) ;
#63204=DIRECTION ( 'NONE',  ( 8.705236002253083981E-17, -0.7431448254773934670, 0.6691306063588592368 ) ) ;
#63206=SURFACE_SIDE_STYLE ('',( #13614 ) ) ;
#63210=SURFACE_SIDE_STYLE ('',( #41792 ) ) ;
#63223=DIRECTION ( 'NONE',  ( 0.000000000000000000, 0.000000000000000000, -1.000000000000000000 ) ) ;
#63231=DIRECTION ( 'NONE',  ( 0.000000000000000000, 0.000000000000000000, 1.000000000000000000 ) ) ;
#63233=EDGE_CURVE ( 'NONE', #18424, #62171, #67586, .T. ) ;
#63235=ORIENTED_EDGE ( 'NONE', *, *, #69485, .T. ) ;
#63242=( NAMED_UNIT ( * ) PLANE_ANGLE_UNIT ( ) SI_UNIT ( $, .RADIAN. ) );
#63246=DIRECTION ( 'NONE',  ( 0.000000000000000000, 0.000000000000000000, -1.000000000000000000 ) ) ;
#63252=ORIENTED_EDGE ( 'NONE', *, *, #3354, .F. ) ;
#63261=EDGE_CURVE ( 'NONE', #360, #44696, #14126, .T. ) ;
#63262=ORIENTED_EDGE ( 'NONE', *, *, #45899, .T. ) ;
#63263=AXIS2_PLACEMENT_3D ( 'NONE', #53466, #48218, #21096 ) ;
#63264=SURFACE_STYLE_FILL_AREA ( #57642 ) ;
#63269=SURFACE_STYLE_FILL_AREA ( #29864 ) ;
#63270=VECTOR ( 'NONE', #4266, 1000.000000000000000 ) ;
#63294=CYLINDRICAL_SURFACE ( 'NONE', #58585, 3.499999999999999556 ) ;
#63299=ORIENTED_EDGE ( 'NONE', *, *, #243, .T. ) ;
#63304=SURFACE_STYLE_FILL_AREA ( #9850 ) ;
#63316=DIRECTION ( 'NONE',  ( 0.000000000000000000, 1.000000000000000000, 0.000000000000000000 ) ) ;
#63325=DIRECTION ( 'NONE',  ( 0.000000000000000000, -0.000000000000000000, 1.000000000000000000 ) ) ;
#63329=MECHANICAL_DESIGN_GEOMETRIC_PRESENTATION_REPRESENTATION('',(#21750),#10515);
#63342=( GEOMETRIC_REPRESENTATION_CONTEXT ( 3 ) GLOBAL_UNCERTAINTY_ASSIGNED_CONTEXT ( ( #120 ) ) GLOBAL_UNIT_ASSIGNED_CONTEXT ( ( #23829, #34715, #24172 ) ) REPRESENTATION_CONTEXT ( 'NONE', 'WORKASPACE' ) );
#63343=( GEOMETRIC_REPRESENTATION_CONTEXT ( 3 ) GLOBAL_UNCERTAINTY_ASSIGNED_CONTEXT ( ( #38310 ) ) GLOBAL_UNIT_ASSIGNED_CONTEXT ( ( #36946, #68236, #31620 ) ) REPRESENTATION_CONTEXT ( 'NONE', 'WORKASPACE' ) );
#63344=CARTESIAN_POINT ( 'NONE',  ( 35.99999999999999289, 5.000000000000000000, -24.00402776293825369 ) ) ;
#63356=DIRECTION ( 'NONE',  ( 1.000000000000000000, -0.000000000000000000, 2.592503555346955593E-15 ) ) ;
#63365=CYLINDRICAL_SURFACE ( 'NONE', #17833, 14.00000000000001243 ) ;
#63376=FACE_OUTER_BOUND ( 'NONE', #17651, .T. ) ;
#63380=VERTEX_POINT ( 'NONE', #67952 ) ;
#63393=( LENGTH_UNIT ( ) NAMED_UNIT ( * ) SI_UNIT ( .MILLI., .METRE. ) );
#63402=ORIENTED_EDGE ( 'NONE', *, *, #16332, .T. ) ;
#63406=VECTOR ( 'NONE', #13354, 1000.000000000000000 ) ;
#63408=VERTEX_POINT ( 'NONE', #58411 ) ;
#63409=SURFACE_STYLE_USAGE ( .BOTH. , #15256 ) ;
#63414=ORIENTED_EDGE ( 'NONE', *, *, #485, .T. ) ;
#63423=SURFACE_SIDE_STYLE ('',( #15601 ) ) ;
#63451=FACE_BOUND ( 'NONE', #45292, .T. ) ;
#63460=VECTOR ( 'NONE', #31715, 1000.000000000000000 ) ;
#63464=CARTESIAN_POINT ( 'NONE',  ( 1.000000000000000000, 43.00000000000000000, -79.00402776293826435 ) ) ;
#63468=( LENGTH_UNIT ( ) NAMED_UNIT ( * ) SI_UNIT ( .MILLI., .METRE. ) );
#63477=AXIS2_PLACEMENT_3D ( 'NONE', #47484, #58008, #67864 ) ;
#63478=ORIENTED_EDGE ( 'NONE', *, *, #43018, .T. ) ;
#63488=MECHANICAL_DESIGN_GEOMETRIC_PRESENTATION_REPRESENTATION('',(#28620),#17427);
#63501=ORIENTED_EDGE ( 'NONE', *, *, #52479, .F. ) ;
#63502=FILL_AREA_STYLE_COLOUR ( '', #60532 ) ;
#63507=STYLED_ITEM ( 'NONE', ( #5234 ), #57035 ) ;
#63516=ORIENTED_EDGE ( 'NONE', *, *, #68416, .T. ) ;
#63525=( LENGTH_UNIT ( ) NAMED_UNIT ( * ) SI_UNIT ( .MILLI., .METRE. ) );
#63548=SURFACE_SIDE_STYLE ('',( #47782 ) ) ;
#63555=PRESENTATION_STYLE_ASSIGNMENT (( #19595 ) ) ;
#63558=( NAMED_UNIT ( * ) SI_UNIT ( $, .STERADIAN. ) SOLID_ANGLE_UNIT ( ) );
#63568=( NAMED_UNIT ( * ) SI_UNIT ( $, .STERADIAN. ) SOLID_ANGLE_UNIT ( ) );
#63569=( NAMED_UNIT ( * ) SI_UNIT ( $, .STERADIAN. ) SOLID_ANGLE_UNIT ( ) );
#63573=PRESENTATION_STYLE_ASSIGNMENT (( #43215 ) ) ;
#63575=DIRECTION ( 'NONE',  ( -1.982541115402068561E-16, 0.000000000000000000, 1.000000000000000000 ) ) ;
#63578=COLOUR_RGB ( '', 0.66274510, 0.83137255, 0.94901961) ;
#63584=SURFACE_STYLE_FILL_AREA ( #5497 ) ;
#63610=FILL_AREA_STYLE_COLOUR ( '', #16857 ) ;
#63618=DIRECTION ( 'NONE',  ( 0.000000000000000000, 0.000000000000000000, -1.000000000000000000 ) ) ;
#63620=VERTEX_POINT ( 'NONE', #5974 ) ;
#63630=DIRECTION ( 'NONE',  ( 0.000000000000000000, 0.000000000000000000, -1.000000000000000000 ) ) ;
#63636=FILL_AREA_STYLE ('',( #64322 ) ) ;
#63638=PRESENTATION_STYLE_ASSIGNMENT (( #20739 ) ) ;
#63642=SURFACE_SIDE_STYLE ('',( #52426 ) ) ;
#63651=FILL_AREA_STYLE ('',( #42262 ) ) ;
#63670=UNCERTAINTY_MEASURE_WITH_UNIT (LENGTH_MEASURE( 1.000000000000000082E-05 ), #57685, 'distance_accuracy_value', 'NONE');
#63677=CARTESIAN_POINT ( 'NONE',  ( 22.54460582735575969, 26.91484815598150604, 27.37908301411970768 ) ) ;
#63682=FILL_AREA_STYLE_COLOUR ( '', #4484 ) ;
#63683=FILL_AREA_STYLE_COLOUR ( '', #29208 ) ;
#63685=PRESENTATION_STYLE_ASSIGNMENT (( #67585 ) ) ;
#63698=DIRECTION ( 'NONE',  ( 0.000000000000000000, 0.000000000000000000, 1.000000000000000000 ) ) ;
#63701=CARTESIAN_POINT ( 'NONE',  ( 108.3664351561509420, 1.000000000000000000, -18.43563588791578667 ) ) ;
#63715=EDGE_LOOP ( 'NONE', ( #59102, #64441, #13400, #6506 ) ) ;
#63720=VERTEX_POINT ( 'NONE', #12984 ) ;
#63732=UNCERTAINTY_MEASURE_WITH_UNIT (LENGTH_MEASURE( 1.000000000000000082E-05 ), #15304, 'distance_accuracy_value', 'NONE');
#63735=CIRCLE ( 'NONE', #17713, 4.999999999999990230 ) ;
#63766=( NAMED_UNIT ( * ) PLANE_ANGLE_UNIT ( ) SI_UNIT ( $, .RADIAN. ) );
#63768=DIRECTION ( 'NONE',  ( -0.000000000000000000, 0.6691306063588581265, 0.7431448254773944662 ) ) ;
#63789=DIRECTION ( 'NONE',  ( 1.000000000000000000, -0.000000000000000000, -1.300977106640434891E-16 ) ) ;
#63796=CARTESIAN_POINT ( 'NONE',  ( 57.00000000000000000, 13.00000000000000178, -79.00402776293826435 ) ) ;
#63799=SURFACE_STYLE_FILL_AREA ( #47700 ) ;
#63829=CARTESIAN_POINT ( 'NONE',  ( 57.00000000000000000, 16.00000000000000000, -72.50402776293826435 ) ) ;
#63830=EDGE_CURVE ( 'NONE', #20856, #13735, #3904, .T. ) ;
#63839=AXIS2_PLACEMENT_3D ( 'NONE', #18709, #22950, #66548 ) ;
#63840=DIRECTION ( 'NONE',  ( 0.000000000000000000, -1.000000000000000000, 0.000000000000000000 ) ) ;
#63845=CIRCLE ( 'NONE', #33526, 5.000000000000004441 ) ;
#63848=FILL_AREA_STYLE_COLOUR ( '', #57764 ) ;
#63849=CARTESIAN_POINT ( 'NONE',  ( 0.000000000000000000, 42.00000000000000711, 44.99999999999999289 ) ) ;
#63851=ADVANCED_FACE ( 'NONE', ( #14737 ), #38768, .T. ) ;
#63864=AXIS2_PLACEMENT_3D ( 'NONE', #31754, #63768, #36021 ) ;
#63866=CARTESIAN_POINT ( 'NONE',  ( 4.000000000000029310, 34.36176364315826248, 80.00402776293826435 ) ) ;
#63870=SURFACE_SIDE_STYLE ('',( #3720 ) ) ;
#63875=CARTESIAN_POINT ( 'NONE',  ( 27.99999999999999645, 5.000000000000000000, 24.00402776293821816 ) ) ;
#63878=ADVANCED_FACE ( 'NONE', ( #33580 ), #17770, .T. ) ;
#63886=CARTESIAN_POINT ( 'NONE',  ( 3.000000000000002665, 34.36176364315826248, -80.00402776293826435 ) ) ;
#63897=DIRECTION ( 'NONE',  ( 0.000000000000000000, -0.000000000000000000, 1.000000000000000000 ) ) ;
#63904=DIRECTION ( 'NONE',  ( -1.000000000000000000, 0.000000000000000000, -0.000000000000000000 ) ) ;
#63908=CYLINDRICAL_SURFACE ( 'NONE', #51843, 1.000000000000000000 ) ;
#63915=EDGE_CURVE ( 'NONE', #34757, #32368, #48771, .T. ) ;
#63924=DIRECTION ( 'NONE',  ( 0.000000000000000000, -0.000000000000000000, 1.000000000000000000 ) ) ;
#63935=SURFACE_STYLE_USAGE ( .BOTH. , #16142 ) ;
#63937=FACE_BOUND ( 'NONE', #41542, .T. ) ;
#63948=VECTOR ( 'NONE', #51169, 1000.000000000000000 ) ;
#63957=DIRECTION ( 'NONE',  ( 0.000000000000000000, 1.000000000000000000, 0.000000000000000000 ) ) ;
#63959=DIRECTION ( 'NONE',  ( 0.000000000000000000, -1.000000000000000000, 0.000000000000000000 ) ) ;
#63963=ORIENTED_EDGE ( 'NONE', *, *, #6195, .T. ) ;
#63968=PRESENTATION_STYLE_ASSIGNMENT (( #16176 ) ) ;
#63977=ORIENTED_EDGE ( 'NONE', *, *, #9307, .T. ) ;
#63982=STYLED_ITEM ( 'NONE', ( #27981 ), #58704 ) ;
#64009=CIRCLE ( 'NONE', #43866, 1.000000000000001998 ) ;
#64021=CARTESIAN_POINT ( 'NONE',  ( 27.00000000000001776, 15.00000000000000000, -34.49999999999999289 ) ) ;
#64022=SURFACE_SIDE_STYLE ('',( #42616 ) ) ;
#64032=CARTESIAN_POINT ( 'NONE',  ( 31.00000000000000000, 14.00000000000000000, -80.00402776293826435 ) ) ;
#64041=MECHANICAL_DESIGN_GEOMETRIC_PRESENTATION_REPRESENTATION('',(#23564),#29171);
#64043=VECTOR ( 'NONE', #37631, 1000.000000000000000 ) ;
#64060=( NAMED_UNIT ( * ) PLANE_ANGLE_UNIT ( ) SI_UNIT ( $, .RADIAN. ) );
#64068=CARTESIAN_POINT ( 'NONE',  ( 1.000000000000000000, 42.00000000000000000, 0.000000000000000000 ) ) ;
#64075=PLANE ( 'NONE',  #2611 ) ;
#64080=ORIENTED_EDGE ( 'NONE', *, *, #18960, .T. ) ;
#64082=( GEOMETRIC_REPRESENTATION_CONTEXT ( 3 ) GLOBAL_UNCERTAINTY_ASSIGNED_CONTEXT ( ( #47405 ) ) GLOBAL_UNIT_ASSIGNED_CONTEXT ( ( #61763, #24479, #40716 ) ) REPRESENTATION_CONTEXT ( 'NONE', 'WORKASPACE' ) );
#64097=VECTOR ( 'NONE', #50044, 1000.000000000000000 ) ;
#64100=DIRECTION ( 'NONE',  ( -1.000000000000000000, -0.000000000000000000, -0.000000000000000000 ) ) ;
#64118=DIRECTION ( 'NONE',  ( -0.000000000000000000, -1.000000000000000000, -0.000000000000000000 ) ) ;
#64119=DIRECTION ( 'NONE',  ( 0.000000000000000000, 1.000000000000000000, 0.000000000000000000 ) ) ;
#64129=DIRECTION ( 'NONE',  ( -0.000000000000000000, -1.000000000000000000, -0.000000000000000000 ) ) ;
#64147=DIRECTION ( 'NONE',  ( 0.000000000000000000, -1.000000000000000000, 0.000000000000000000 ) ) ;
#64155=EDGE_CURVE ( 'NONE', #14824, #21109, #62322, .T. ) ;
#64164=DIRECTION ( 'NONE',  ( -8.673617379884015751E-17, 0.000000000000000000, -1.000000000000000000 ) ) ;
#64170=( BOUNDED_CURVE ( )  B_SPLINE_CURVE ( 3, ( #62767, #58549, #52265, #3657 ),
 .UNSPECIFIED., .F., .F. ) 
 B_SPLINE_CURVE_WITH_KNOTS ( ( 4, 4 ),
 ( -7.105427357601001859E-15, 1.570796326794896558 ),
 .UNSPECIFIED. ) 
 CURVE ( )  GEOMETRIC_REPRESENTATION_ITEM ( )  RATIONAL_B_SPLINE_CURVE ( ( 1.000000000000000000, 0.8047378541243632721, 0.8047378541243632721, 1.000000000000000000 ) ) 
 REPRESENTATION_ITEM ( '' )  );
#64172=CARTESIAN_POINT ( 'NONE',  ( 7.000000000000017764, 17.78868675966041835, -9.106839746483067901E-16 ) ) ;
#64173=CARTESIAN_POINT ( 'NONE',  ( 2.000000000000015543, 26.00000000000000355, 23.99999999999999645 ) ) ;
#64178=EDGE_CURVE ( 'NONE', #46991, #3091, #46181, .T. ) ;
#64190=STYLED_ITEM ( 'NONE', ( #48379 ), #45798 ) ;
#64191=DIRECTION ( 'NONE',  ( 0.000000000000000000, -0.000000000000000000, 1.000000000000000000 ) ) ;
#64194=FILL_AREA_STYLE ('',( #64559 ) ) ;
#64198=( LENGTH_UNIT ( ) NAMED_UNIT ( * ) SI_UNIT ( .MILLI., .METRE. ) );
#64200=DIRECTION ( 'NONE',  ( 0.000000000000000000, 0.000000000000000000, 1.000000000000000000 ) ) ;
#64223=DIRECTION ( 'NONE',  ( -1.239088197126290324E-16, 0.000000000000000000, -1.000000000000000000 ) ) ;
#64224=EDGE_CURVE ( 'NONE', #62949, #65192, #52795, .T. ) ;
#64227=SURFACE_STYLE_USAGE ( .BOTH. , #63548 ) ;
#64230=AXIS2_PLACEMENT_3D ( 'NONE', #33252, #60318, #54686 ) ;
#64240=CARTESIAN_POINT ( 'NONE',  ( 6.000000000000017764, -60.04052944165106709, -35.50000000000000000 ) ) ;
#64258=DIRECTION ( 'NONE',  ( 1.000000000000000000, 0.000000000000000000, 4.516179008354028246E-16 ) ) ;
#64261=ORIENTED_EDGE ( 'NONE', *, *, #48879, .F. ) ;
#64262=PRESENTATION_STYLE_ASSIGNMENT (( #17154 ) ) ;
#64266=( LENGTH_UNIT ( ) NAMED_UNIT ( * ) SI_UNIT ( .MILLI., .METRE. ) );
#64276=EDGE_LOOP ( 'NONE', ( #54877, #36778, #21938, #47688 ) ) ;
#64277=DIRECTION ( 'NONE',  ( 0.000000000000000000, 0.000000000000000000, -1.000000000000000000 ) ) ;
#64278=DIRECTION ( 'NONE',  ( 0.000000000000000000, 1.000000000000000000, -0.000000000000000000 ) ) ;
#64282=CARTESIAN_POINT ( 'NONE',  ( 4.000000000000029310, 43.00000000000000000, 90.00000000000000000 ) ) ;
#64288=ORIENTED_EDGE ( 'NONE', *, *, #20335, .F. ) ;
#64295=CARTESIAN_POINT ( 'NONE',  ( 24.16127419156986278, 27.24068003726083376, 27.27382999534755115 ) ) ;
#64299=VECTOR ( 'NONE', #22917, 1000.000000000000000 ) ;
#64300=FACE_BOUND ( 'NONE', #18885, .T. ) ;
#64312=EDGE_CURVE ( 'NONE', #33379, #30008, #4607, .T. ) ;
#64321=SURFACE_STYLE_FILL_AREA ( #36941 ) ;
#64322=FILL_AREA_STYLE_COLOUR ( '', #15782 ) ;
#64326=ORIENTED_EDGE ( 'NONE', *, *, #14798, .F. ) ;
#64329=CARTESIAN_POINT ( 'NONE',  ( 179.4361977533518484, 5.000000000000000000, 103.7004518695275550 ) ) ;
#64332=PRESENTATION_STYLE_ASSIGNMENT (( #58363 ) ) ;
#64334=ORIENTED_EDGE ( 'NONE', *, *, #16706, .T. ) ;
#64338=( NAMED_UNIT ( * ) SI_UNIT ( $, .STERADIAN. ) SOLID_ANGLE_UNIT ( ) );
#64344=SURFACE_STYLE_FILL_AREA ( #54473 ) ;
#64351=MECHANICAL_DESIGN_GEOMETRIC_PRESENTATION_REPRESENTATION('',(#41903),#29497);
#64356=CARTESIAN_POINT ( 'NONE',  ( 179.4361977533490631, 5.000000000000000000, -103.7004518695262192 ) ) ;
#64358=CARTESIAN_POINT ( 'NONE',  ( 4.000000000000030198, 43.00000000000000000, 89.00000000000000000 ) ) ;
#64364=FILL_AREA_STYLE_COLOUR ( '', #45188 ) ;
#64371=ORIENTED_EDGE ( 'NONE', *, *, #47319, .F. ) ;
#64375=STYLED_ITEM ( 'NONE', ( #63685 ), #29078 ) ;
#64378=SPHERICAL_SURFACE ( 'NONE', #45020, 1.000000000000000000 ) ;
#64379=DIRECTION ( 'NONE',  ( 0.000000000000000000, 0.000000000000000000, -1.000000000000000000 ) ) ;
#64384=ORIENTED_EDGE ( 'NONE', *, *, #30550, .T. ) ;
#64386=AXIS2_PLACEMENT_3D ( 'NONE', #57373, #3151, #14124 ) ;
#64389=SURFACE_SIDE_STYLE ('',( #16582 ) ) ;
#64393=CARTESIAN_POINT ( 'NONE',  ( 22.00000000000001066, 43.00000000000000000, -45.61250543006184444 ) ) ;
#64401=ORIENTED_EDGE ( 'NONE', *, *, #31477, .F. ) ;
#64404=LINE ( 'NONE', #21487, #54954 ) ;
#64406=( GEOMETRIC_REPRESENTATION_CONTEXT ( 3 ) GLOBAL_UNCERTAINTY_ASSIGNED_CONTEXT ( ( #44758 ) ) GLOBAL_UNIT_ASSIGNED_CONTEXT ( ( #30737, #14233, #9673 ) ) REPRESENTATION_CONTEXT ( 'NONE', 'WORKASPACE' ) );
#64409=DIRECTION ( 'NONE',  ( 0.000000000000000000, 0.000000000000000000, -1.000000000000000000 ) ) ;
#64411=ORIENTED_EDGE ( 'NONE', *, *, #40160, .F. ) ;
#64421=ORIENTED_EDGE ( 'NONE', *, *, #45481, .F. ) ;
#64431=CARTESIAN_POINT ( 'NONE',  ( -2.012550282676216817E-15, 42.24279663153547659, -74.85430519625602130 ) ) ;
#64434=AXIS2_PLACEMENT_3D ( 'NONE', #12141, #55408, #50160 ) ;
#64435=PRESENTATION_STYLE_ASSIGNMENT (( #43709 ) ) ;
#64441=ORIENTED_EDGE ( 'NONE', *, *, #29946, .F. ) ;
#64443=UNCERTAINTY_MEASURE_WITH_UNIT (LENGTH_MEASURE( 1.000000000000000082E-05 ), #46756, 'distance_accuracy_value', 'NONE');
#64456=AXIS2_PLACEMENT_3D ( 'NONE', #62692, #35650, #19089 ) ;
#64460=CARTESIAN_POINT ( 'NONE',  ( 57.00000000000000000, 0.000000000000000000, 77.00402776293825013 ) ) ;
#64461=SURFACE_STYLE_USAGE ( .BOTH. , #43057 ) ;
#64466=SURFACE_STYLE_USAGE ( .BOTH. , #68717 ) ;
#64472=EDGE_CURVE ( 'NONE', #34731, #37678, #51305, .T. ) ;
#64488=( GEOMETRIC_REPRESENTATION_CONTEXT ( 3 ) GLOBAL_UNCERTAINTY_ASSIGNED_CONTEXT ( ( #55268 ) ) GLOBAL_UNIT_ASSIGNED_CONTEXT ( ( #16031, #32175, #42431 ) ) REPRESENTATION_CONTEXT ( 'NONE', 'WORKASPACE' ) );
#64509=SURFACE_SIDE_STYLE ('',( #10366 ) ) ;
#64512=DIRECTION ( 'NONE',  ( 0.000000000000000000, 0.000000000000000000, -1.000000000000000000 ) ) ;
#64516=ORIENTED_EDGE ( 'NONE', *, *, #21368, .F. ) ;
#64521=CARTESIAN_POINT ( 'NONE',  ( 10.00000000000000711, 50.00000000000000000, -59.99999999999999289 ) ) ;
#64528=CARTESIAN_POINT ( 'NONE',  ( 4.000000000000001776, 43.00000000000000000, -90.00000000000000000 ) ) ;
#64531=CARTESIAN_POINT ( 'NONE',  ( 21.00000000000001776, 15.00000000000000000, 29.68999999999999417 ) ) ;
#64534=ORIENTED_EDGE ( 'NONE', *, *, #50669, .F. ) ;
#64536=AXIS2_PLACEMENT_3D ( 'NONE', #6658, #27417, #16235 ) ;
#64538=CARTESIAN_POINT ( 'NONE',  ( 6.000000000000017764, 16.44305403005404287, -2.635024667321593109E-15 ) ) ;
#64540=PRESENTATION_STYLE_ASSIGNMENT (( #21980 ) ) ;
#64558=FACE_OUTER_BOUND ( 'NONE', #34436, .T. ) ;
#64559=FILL_AREA_STYLE_COLOUR ( '', #13351 ) ;
#64560=DIRECTION ( 'NONE',  ( 1.000000000000000000, 0.000000000000000000, -1.300977106640434644E-16 ) ) ;
#64563=SURFACE_STYLE_FILL_AREA ( #37536 ) ;
#64589=AXIS2_PLACEMENT_3D ( 'NONE', #47316, #58514, #52905 ) ;
#64593=LINE ( 'NONE', #69177, #56320 ) ;
#64596=CIRCLE ( 'NONE', #35428, 12.50000000000000178 ) ;
#64606=COLOUR_RGB ( '', 0.31764706, 0.68627451, 0.89019608) ;
#64607=PRESENTATION_STYLE_ASSIGNMENT (( #42846 ) ) ;
#64611=( NAMED_UNIT ( * ) PLANE_ANGLE_UNIT ( ) SI_UNIT ( $, .RADIAN. ) );
#64618=COLOUR_RGB ( '', 0.40784314, 0.44705882, 0.49803922) ;
#64620=( LENGTH_UNIT ( ) NAMED_UNIT ( * ) SI_UNIT ( .MILLI., .METRE. ) );
#64630=MECHANICAL_DESIGN_GEOMETRIC_PRESENTATION_REPRESENTATION('',(#32043),#47873);
#64635=ORIENTED_EDGE ( 'NONE', *, *, #50645, .F. ) ;
#64654=DIRECTION ( 'NONE',  ( 0.000000000000000000, 0.000000000000000000, -1.000000000000000000 ) ) ;
#64657=VECTOR ( 'NONE', #33785, 1000.000000000000000 ) ;
#64684=ORIENTED_EDGE ( 'NONE', *, *, #9944, .F. ) ;
#64691=DIRECTION ( 'NONE',  ( 0.000000000000000000, 1.000000000000000000, -0.000000000000000000 ) ) ;
#64700=ORIENTED_EDGE ( 'NONE', *, *, #44364, .F. ) ;
#64708=SURFACE_SIDE_STYLE ('',( #262 ) ) ;
#64725=CYLINDRICAL_SURFACE ( 'NONE', #60673, 1.000000000000000888 ) ;
#64737=FACE_OUTER_BOUND ( 'NONE', #58626, .T. ) ;
#64738=CARTESIAN_POINT ( 'NONE',  ( 23.50000000000001776, -3.148064030671221758, 29.68999999999999417 ) ) ;
#64740=EDGE_CURVE ( 'NONE', #66764, #28375, #18701, .T. ) ;
#64757=FILL_AREA_STYLE_COLOUR ( '', #12554 ) ;
#64764=CARTESIAN_POINT ( 'NONE',  ( 22.99999999999996447, 5.000000000000000000, -29.00402776293825369 ) ) ;
#64768=ORIENTED_EDGE ( 'NONE', *, *, #67909, .F. ) ;
#64769=ORIENTED_EDGE ( 'NONE', *, *, #56534, .T. ) ;
#64770=( LENGTH_UNIT ( ) NAMED_UNIT ( * ) SI_UNIT ( .MILLI., .METRE. ) );
#64783=CARTESIAN_POINT ( 'NONE',  ( 2.000000000000008438, 50.00000000000000000, -65.00000000000000000 ) ) ;
#64795=ORIENTED_EDGE ( 'NONE', *, *, #381, .T. ) ;
#64810=( GEOMETRIC_REPRESENTATION_CONTEXT ( 3 ) GLOBAL_UNCERTAINTY_ASSIGNED_CONTEXT ( ( #6530 ) ) GLOBAL_UNIT_ASSIGNED_CONTEXT ( ( #156, #64611, #11475 ) ) REPRESENTATION_CONTEXT ( 'NONE', 'WORKASPACE' ) );
#64838=AXIS2_PLACEMENT_3D ( 'NONE', #33802, #28145, #11661 ) ;
#64850=FACE_BOUND ( 'NONE', #32515, .T. ) ;
#64865=CARTESIAN_POINT ( 'NONE',  ( 31.00000000000002132, 42.00000000000000000, 80.00402776293826435 ) ) ;
#64867=MECHANICAL_DESIGN_GEOMETRIC_PRESENTATION_REPRESENTATION('',(#62605),#34539);
#64873=DIRECTION ( 'NONE',  ( 1.000000000000000000, 0.000000000000000000, 0.000000000000000000 ) ) ;
#64894=EDGE_CURVE ( 'NONE', #67044, #52223, #37879, .T. ) ;
#64899=( NAMED_UNIT ( * ) PLANE_ANGLE_UNIT ( ) SI_UNIT ( $, .RADIAN. ) );
#64913=( NAMED_UNIT ( * ) SI_UNIT ( $, .STERADIAN. ) SOLID_ANGLE_UNIT ( ) );
#64918=DIRECTION ( 'NONE',  ( 0.000000000000000000, 0.000000000000000000, -1.000000000000000000 ) ) ;
#64919=MECHANICAL_DESIGN_GEOMETRIC_PRESENTATION_REPRESENTATION('',(#49233),#58171);
#64926=( NAMED_UNIT ( * ) PLANE_ANGLE_UNIT ( ) SI_UNIT ( $, .RADIAN. ) );
#64930=ORIENTED_EDGE ( 'NONE', *, *, #31696, .T. ) ;
#64931=CARTESIAN_POINT ( 'NONE',  ( 29.00000000000000000, 42.00000000000000000, -80.00402776293826435 ) ) ;
#64935=ORIENTED_EDGE ( 'NONE', *, *, #38499, .T. ) ;
#64937=EDGE_CURVE ( 'NONE', #52223, #1044, #28339, .T. ) ;
#64940=EDGE_LOOP ( 'NONE', ( #57469, #54131, #31103, #18829 ) ) ;
#64942=CARTESIAN_POINT ( 'NONE',  ( 16.00000000000001776, 15.00000000000000000, -29.68999999999999417 ) ) ;
#64944=CARTESIAN_POINT ( 'NONE',  ( 57.00000000000000000, 14.00000000000000000, 60.00402776293825724 ) ) ;
#64946=ADVANCED_FACE ( 'NONE', ( #37939 ), #8607, .T. ) ;
#64949=ORIENTED_EDGE ( 'NONE', *, *, #65212, .T. ) ;
#64952=FILL_AREA_STYLE ('',( #59313 ) ) ;
#64965=ORIENTED_EDGE ( 'NONE', *, *, #871, .F. ) ;
#64988=AXIS2_PLACEMENT_3D ( 'NONE', #2011, #18276, #12277 ) ;
#65015=CARTESIAN_POINT ( 'NONE',  ( 0.000000000000000000, 42.00000000000000000, -79.00402776293826435 ) ) ;
#65028=SURFACE_STYLE_USAGE ( .BOTH. , #49578 ) ;
#65033=FILL_AREA_STYLE ('',( #64364 ) ) ;
#65034=UNCERTAINTY_MEASURE_WITH_UNIT (LENGTH_MEASURE( 1.000000000000000082E-05 ), #58517, 'distance_accuracy_value', 'NONE');
#65035=VERTEX_POINT ( 'NONE', #55793 ) ;
#65037=DIRECTION ( 'NONE',  ( 1.982541115402069054E-16, 0.000000000000000000, 1.000000000000000000 ) ) ;
#65041=ORIENTED_EDGE ( 'NONE', *, *, #26089, .T. ) ;
#65056=VERTEX_POINT ( 'NONE', #34671 ) ;
#65058=FACE_OUTER_BOUND ( 'NONE', #55884, .T. ) ;
#65059=( NAMED_UNIT ( * ) PLANE_ANGLE_UNIT ( ) SI_UNIT ( $, .RADIAN. ) );
#65066=VECTOR ( 'NONE', #13858, 1000.000000000000000 ) ;
#65070=AXIS2_PLACEMENT_3D ( 'NONE', #4229, #67600, #46894 ) ;
#65084=SURFACE_SIDE_STYLE ('',( #59123 ) ) ;
#65085=VECTOR ( 'NONE', #4676, 1000.000000000000000 ) ;
#65086=DIRECTION ( 'NONE',  ( -0.000000000000000000, -1.000000000000000000, -0.000000000000000000 ) ) ;
#65097=CARTESIAN_POINT ( 'NONE',  ( 3.000000000000030198, 38.70020753820971748, 90.00000000000000000 ) ) ;
#65098=MECHANICAL_DESIGN_GEOMETRIC_PRESENTATION_REPRESENTATION('',(#29077),#15681);
#65103=EDGE_CURVE ( 'NONE', #408, #40021, #36810, .T. ) ;
#65112=UNCERTAINTY_MEASURE_WITH_UNIT (LENGTH_MEASURE( 1.000000000000000082E-05 ), #59386, 'distance_accuracy_value', 'NONE');
#65120=AXIS2_PLACEMENT_3D ( 'NONE', #8514, #19742, #34879 ) ;
#65127=UNCERTAINTY_MEASURE_WITH_UNIT (LENGTH_MEASURE( 1.000000000000000082E-05 ), #45550, 'distance_accuracy_value', 'NONE');
#65135=COLOUR_RGB ( '', 0.31764706, 0.68627451, 0.89019608) ;
#65140=FILL_AREA_STYLE ('',( #49686 ) ) ;
#65147=DIRECTION ( 'NONE',  ( -1.000000000000000000, 0.000000000000000000, 1.300977106640434891E-16 ) ) ;
#65156=CARTESIAN_POINT ( 'NONE',  ( 31.00000000000000355, 43.00000000000000000, -45.61250543006184444 ) ) ;
#65163=STYLED_ITEM ( 'NONE', ( #38233 ), #52134 ) ;
#65165=( GEOMETRIC_REPRESENTATION_CONTEXT ( 3 ) GLOBAL_UNCERTAINTY_ASSIGNED_CONTEXT ( ( #26330 ) ) GLOBAL_UNIT_ASSIGNED_CONTEXT ( ( #32350, #32020, #42297 ) ) REPRESENTATION_CONTEXT ( 'NONE', 'WORKASPACE' ) );
#65172=COLOUR_RGB ( '', 0.66274510, 0.83137255, 0.94901961) ;
#65176=CARTESIAN_POINT ( 'NONE',  ( 35.99999999999999289, 5.000000000000000000, 32.00402776293825724 ) ) ;
#65179=MECHANICAL_DESIGN_GEOMETRIC_PRESENTATION_REPRESENTATION('',(#15805),#64082);
#65180=FILL_AREA_STYLE_COLOUR ( '', #55525 ) ;
#65192=VERTEX_POINT ( 'NONE', #57171 ) ;
#65205=FILL_AREA_STYLE ('',( #5751 ) ) ;
#65207=MECHANICAL_DESIGN_GEOMETRIC_PRESENTATION_REPRESENTATION('',(#61824),#57328);
#65210=LINE ( 'NONE', #33886, #50322 ) ;
#65212=EDGE_CURVE ( 'NONE', #65703, #50928, #53313, .T. ) ;
#65215=FILL_AREA_STYLE_COLOUR ( '', #11214 ) ;
#65227=PRESENTATION_STYLE_ASSIGNMENT (( #6826 ) ) ;
#65249=( NAMED_UNIT ( * ) SI_UNIT ( $, .STERADIAN. ) SOLID_ANGLE_UNIT ( ) );
#65263=CIRCLE ( 'NONE', #37194, 3.499999999999996003 ) ;
#65270=COLOUR_RGB ( '', 0.66274510, 0.83137255, 0.94901961) ;
#65278=PLANE ( 'NONE',  #24827 ) ;
#65285=SURFACE_STYLE_FILL_AREA ( #33287 ) ;
#65286=EDGE_LOOP ( 'NONE', ( #59858, #17882, #44238, #44764, #52530, #43020 ) ) ;
#65287=SURFACE_STYLE_USAGE ( .BOTH. , #21687 ) ;
#65296=COLOUR_RGB ( '', 0.40784314, 0.44705882, 0.49803922) ;
#65311=CARTESIAN_POINT ( 'NONE',  ( 27.00000000000001776, 15.00000000000000000, -34.49999999999999289 ) ) ;
#65315=PRESENTATION_STYLE_ASSIGNMENT (( #66002 ) ) ;
#65319=VECTOR ( 'NONE', #41336, 1000.000000000000000 ) ;
#65331=COLOUR_RGB ( '', 0.40784314, 0.44705882, 0.49803922) ;
#65333=ADVANCED_FACE ( 'NONE', ( #54322 ), #65575, .T. ) ;
#65338=CARTESIAN_POINT ( 'NONE',  ( 24.29522375537286649, 27.12549504607582662, 27.31719062346842364 ) ) ;
#65349=VECTOR ( 'NONE', #34288, 1000.000000000000000 ) ;
#65367=FILL_AREA_STYLE_COLOUR ( '', #40543 ) ;
#65381=LINE ( 'NONE', #55513, #41959 ) ;
#65384=( GEOMETRIC_REPRESENTATION_CONTEXT ( 3 ) GLOBAL_UNCERTAINTY_ASSIGNED_CONTEXT ( ( #32853 ) ) GLOBAL_UNIT_ASSIGNED_CONTEXT ( ( #15428, #5767, #43489 ) ) REPRESENTATION_CONTEXT ( 'NONE', 'WORKASPACE' ) );
#65386=DIRECTION ( 'NONE',  ( 0.000000000000000000, 0.000000000000000000, 1.000000000000000000 ) ) ;
#65391=DIRECTION ( 'NONE',  ( 0.000000000000000000, 0.000000000000000000, -1.000000000000000000 ) ) ;
#65410=FACE_OUTER_BOUND ( 'NONE', #28706, .T. ) ;
#65418=LINE ( 'NONE', #48938, #3349 ) ;
#65426=PRESENTATION_STYLE_ASSIGNMENT (( #27752 ) ) ;
#65427=CARTESIAN_POINT ( 'NONE',  ( 1.000000000000000000, -60.04052944165106709, 35.50000000000000000 ) ) ;
#65433=VECTOR ( 'NONE', #19188, 1000.000000000000000 ) ;
#65443=PRESENTATION_STYLE_ASSIGNMENT (( #39785 ) ) ;
#65445=EDGE_CURVE ( 'NONE', #57229, #54767, #4577, .T. ) ;
#65452=AXIS2_PLACEMENT_3D ( 'NONE', #31284, #58734, #53461 ) ;
#65467=VERTEX_POINT ( 'NONE', #16222 ) ;
#65475=SURFACE_STYLE_FILL_AREA ( #44072 ) ;
#65485=CARTESIAN_POINT ( 'NONE',  ( 22.99999999999998224, 5.000000000000000000, 72.00402776293825013 ) ) ;
#65489=DIRECTION ( 'NONE',  ( 0.000000000000000000, 0.000000000000000000, -1.000000000000000000 ) ) ;
#65494=ORIENTED_EDGE ( 'NONE', *, *, #44390, .T. ) ;
#65501=( GEOMETRIC_REPRESENTATION_CONTEXT ( 3 ) GLOBAL_UNCERTAINTY_ASSIGNED_CONTEXT ( ( #32533 ) ) GLOBAL_UNIT_ASSIGNED_CONTEXT ( ( #2335, #66067, #44673 ) ) REPRESENTATION_CONTEXT ( 'NONE', 'WORKASPACE' ) );
#65503=VERTEX_POINT ( 'NONE', #54150 ) ;
#65507=MECHANICAL_DESIGN_GEOMETRIC_PRESENTATION_REPRESENTATION('',(#55365),#58738);
#65509=ADVANCED_FACE ( 'NONE', ( #10911 ), #27407, .T. ) ;
#65513=LINE ( 'NONE', #28188, #59282 ) ;
#65534=DIRECTION ( 'NONE',  ( 0.000000000000000000, 0.000000000000000000, 1.000000000000000000 ) ) ;
#65548=ORIENTED_EDGE ( 'NONE', *, *, #24553, .F. ) ;
#65549=PRESENTATION_STYLE_ASSIGNMENT (( #50084 ) ) ;
#65552=FILL_AREA_STYLE_COLOUR ( '', #51864 ) ;
#65553=DIRECTION ( 'NONE',  ( 0.000000000000000000, 0.000000000000000000, -1.000000000000000000 ) ) ;
#65555=ORIENTED_EDGE ( 'NONE', *, *, #52420, .F. ) ;
#65559=VERTEX_POINT ( 'NONE', #28081 ) ;
#65571=DIRECTION ( 'NONE',  ( 1.000000000000000000, 0.000000000000000000, -1.300977106640435137E-16 ) ) ;
#65575=CYLINDRICAL_SURFACE ( 'NONE', #10909, 1.000000000000000888 ) ;
#65581=COLOUR_RGB ( '', 0.08235294, 0.09019608, 0.10196078) ;
#65583=FACE_OUTER_BOUND ( 'NONE', #38676, .T. ) ;
#65585=DIRECTION ( 'NONE',  ( 0.000000000000000000, 0.000000000000000000, -1.000000000000000000 ) ) ;
#65589=SURFACE_STYLE_USAGE ( .BOTH. , #44191 ) ;
#65594=ORIENTED_EDGE ( 'NONE', *, *, #20580, .T. ) ;
#65596=ADVANCED_FACE ( 'NONE', ( #11945 ), #7368, .T. ) ;
#65600=UNCERTAINTY_MEASURE_WITH_UNIT (LENGTH_MEASURE( 1.000000000000000082E-05 ), #69195, 'distance_accuracy_value', 'NONE');
#65605=( LENGTH_UNIT ( ) NAMED_UNIT ( * ) SI_UNIT ( .MILLI., .METRE. ) );
#65607=EDGE_CURVE ( 'NONE', #11349, #60715, #36846, .T. ) ;
#65622=ORIENTED_EDGE ( 'NONE', *, *, #2328, .T. ) ;
#65623=FILL_AREA_STYLE ('',( #1546 ) ) ;
#65631=CARTESIAN_POINT ( 'NONE',  ( 22.99999999999996447, 5.000000000000000000, 29.00402776293825369 ) ) ;
#65636=DIRECTION ( 'NONE',  ( 0.000000000000000000, -0.000000000000000000, 1.000000000000000000 ) ) ;
#65639=STYLED_ITEM ( 'NONE', ( #31102 ), #62157 ) ;
#65646=UNCERTAINTY_MEASURE_WITH_UNIT (LENGTH_MEASURE( 1.000000000000000082E-05 ), #64620, 'distance_accuracy_value', 'NONE');
#65652=B_SPLINE_CURVE_WITH_KNOTS ( 'NONE', 3,
 ( #53418, #26640, #48165, #64295, #65338, #43926, #561, #22086, #43586, #16832, #11520, #32993, #54426, #27673, #883, #17183, #60057, #17849, #49870, #50215 ),
 .UNSPECIFIED., .F., .F.,
 ( 4, 2, 2, 2, 2, 2, 2, 2, 2, 4 ),
 ( 0.004227980867416260453, 0.004756478475843291601, 0.005284976084270322748, 0.005813473692697353895, 0.006341971301124385042, 0.006870468909551416190, 0.007398966517978447337, 0.007663215322191966813, 0.007927464126405487158, 0.008455961734832519172 ),
 .UNSPECIFIED. ) ;
#65653=FILL_AREA_STYLE_COLOUR ( '', #35240 ) ;
#65660=( GEOMETRIC_REPRESENTATION_CONTEXT ( 3 ) GLOBAL_UNCERTAINTY_ASSIGNED_CONTEXT ( ( #57429 ) ) GLOBAL_UNIT_ASSIGNED_CONTEXT ( ( #66831, #39424, #67503 ) ) REPRESENTATION_CONTEXT ( 'NONE', 'WORKASPACE' ) );
#65670=SURFACE_STYLE_USAGE ( .BOTH. , #49513 ) ;
#65673=ORIENTED_EDGE ( 'NONE', *, *, #52226, .T. ) ;
#65680=CARTESIAN_POINT ( 'NONE',  ( 27.00000000000001776, 14.00000000000000000, 34.49999999999998579 ) ) ;
#65681=SURFACE_STYLE_USAGE ( .BOTH. , #34016 ) ;
#65685=LINE ( 'NONE', #34375, #53377 ) ;
#65687=VECTOR ( 'NONE', #59053, 1000.000000000000000 ) ;
#65691=( NAMED_UNIT ( * ) SI_UNIT ( $, .STERADIAN. ) SOLID_ANGLE_UNIT ( ) );
#65699=SPHERICAL_SURFACE ( 'NONE', #11338, 1.000000000000000000 ) ;
#65703=VERTEX_POINT ( 'NONE', #61839 ) ;
#65711=FILL_AREA_STYLE ('',( #27358 ) ) ;
#65716=EDGE_LOOP ( 'NONE', ( #9270, #52738, #15249, #2249 ) ) ;
#65722=DIRECTION ( 'NONE',  ( 0.000000000000000000, 0.000000000000000000, -1.000000000000000000 ) ) ;
#65725=ORIENTED_EDGE ( 'NONE', *, *, #40277, .T. ) ;
#65731=( LENGTH_UNIT ( ) NAMED_UNIT ( * ) SI_UNIT ( .MILLI., .METRE. ) );
#65733=DIRECTION ( 'NONE',  ( -0.000000000000000000, 1.000000000000000000, -0.000000000000000000 ) ) ;
#65736=( LENGTH_UNIT ( ) NAMED_UNIT ( * ) SI_UNIT ( .MILLI., .METRE. ) );
#65738=SURFACE_STYLE_FILL_AREA ( #11930 ) ;
#65743=( GEOMETRIC_REPRESENTATION_CONTEXT ( 3 ) GLOBAL_UNCERTAINTY_ASSIGNED_CONTEXT ( ( #41031 ) ) GLOBAL_UNIT_ASSIGNED_CONTEXT ( ( #4126, #3412, #53050 ) ) REPRESENTATION_CONTEXT ( 'NONE', 'WORKASPACE' ) );
#65746=FACE_OUTER_BOUND ( 'NONE', #28519, .T. ) ;
#65757=FILL_AREA_STYLE_COLOUR ( '', #58165 ) ;
#65761=VERTEX_POINT ( 'NONE', #45725 ) ;
#65764=EDGE_CURVE ( 'NONE', #5489, #62632, #8746, .T. ) ;
#65771=DIRECTION ( 'NONE',  ( 0.000000000000000000, 0.6691306063588591257, 0.7431448254773933559 ) ) ;
#65774=DIRECTION ( 'NONE',  ( -1.000000000000000000, 0.000000000000000000, 1.300977106640434891E-16 ) ) ;
#65775=CARTESIAN_POINT ( 'NONE',  ( 2.999999999999998668, 5.000000000000000000, 72.00402776293822171 ) ) ;
#65786=FILL_AREA_STYLE_COLOUR ( '', #5612 ) ;
#65787=MECHANICAL_DESIGN_GEOMETRIC_PRESENTATION_REPRESENTATION('',(#2825),#5156);
#65792=VECTOR ( 'NONE', #65952, 1000.000000000000000 ) ;
#65793=DIRECTION ( 'NONE',  ( -0.000000000000000000, -1.000000000000000000, 0.000000000000000000 ) ) ;
#65810=DIRECTION ( 'NONE',  ( 0.000000000000000000, -0.9984713486292863260, 0.05527174654752588928 ) ) ;
#65814=VECTOR ( 'NONE', #5013, 1000.000000000000000 ) ;
#65818=( GEOMETRIC_REPRESENTATION_CONTEXT ( 3 ) GLOBAL_UNCERTAINTY_ASSIGNED_CONTEXT ( ( #49616 ) ) GLOBAL_UNIT_ASSIGNED_CONTEXT ( ( #37311, #16186, #64338 ) ) REPRESENTATION_CONTEXT ( 'NONE', 'WORKASPACE' ) );
#65823=COLOUR_RGB ( '', 0.31764706, 0.68627451, 0.89019608) ;
#65830=FILL_AREA_STYLE ('',( #44428 ) ) ;
#65835=CARTESIAN_POINT ( 'NONE',  ( 2.000000000000015987, 26.00000000000000355, 27.49999999999999645 ) ) ;
#65840=COLOUR_RGB ( '', 0.31764706, 0.68627451, 0.89019608) ;
#65846=ORIENTED_EDGE ( 'NONE', *, *, #69500, .F. ) ;
#65856=( GEOMETRIC_REPRESENTATION_CONTEXT ( 3 ) GLOBAL_UNCERTAINTY_ASSIGNED_CONTEXT ( ( #34659 ) ) GLOBAL_UNIT_ASSIGNED_CONTEXT ( ( #17556, #17878, #62151 ) ) REPRESENTATION_CONTEXT ( 'NONE', 'WORKASPACE' ) );
#65893=FILL_AREA_STYLE ('',( #52074 ) ) ;
#65899=UNCERTAINTY_MEASURE_WITH_UNIT (LENGTH_MEASURE( 1.000000000000000082E-05 ), #45792, 'distance_accuracy_value', 'NONE');
#65908=SURFACE_STYLE_FILL_AREA ( #65205 ) ;
#65910=ORIENTED_EDGE ( 'NONE', *, *, #13363, .T. ) ;
#65911=SURFACE_STYLE_USAGE ( .BOTH. , #13835 ) ;
#65917=DIRECTION ( 'NONE',  ( 1.000000000000000000, -0.000000000000000000, -0.000000000000000000 ) ) ;
#65923=SURFACE_SIDE_STYLE ('',( #32881 ) ) ;
#65925=CARTESIAN_POINT ( 'NONE',  ( 26.00000000000001776, 42.00000000000000000, -34.49999999999999289 ) ) ;
#65933=ORIENTED_EDGE ( 'NONE', *, *, #69514, .T. ) ;
#65941=FILL_AREA_STYLE_COLOUR ( '', #19690 ) ;
#65943=AXIS2_PLACEMENT_3D ( 'NONE', #36971, #46854, #30948 ) ;
#65952=DIRECTION ( 'NONE',  ( 1.000000000000000000, -0.000000000000000000, 0.000000000000000000 ) ) ;
#65962=PRESENTATION_STYLE_ASSIGNMENT (( #12488 ) ) ;
#65964=ORIENTED_EDGE ( 'NONE', *, *, #50524, .T. ) ;
#65973=( NAMED_UNIT ( * ) SI_UNIT ( $, .STERADIAN. ) SOLID_ANGLE_UNIT ( ) );
#65977=DIRECTION ( 'NONE',  ( 0.000000000000000000, 0.6449798928094538919, 0.7641995406119433953 ) ) ;
#65978=EDGE_CURVE ( 'NONE', #30128, #11361, #32285, .T. ) ;
#65994=CARTESIAN_POINT ( 'NONE',  ( 35.99999999999999289, 0.000000000000000000, 72.00402776293825013 ) ) ;
#65995=EDGE_CURVE ( 'NONE', #14584, #7763, #41051, .T. ) ;
#66002=SURFACE_STYLE_USAGE ( .BOTH. , #55452 ) ;
#66011=ORIENTED_EDGE ( 'NONE', *, *, #5371, .F. ) ;
#66031=DIRECTION ( 'NONE',  ( 0.000000000000000000, 0.000000000000000000, -1.000000000000000000 ) ) ;
#66036=DIRECTION ( 'NONE',  ( -1.000000000000000000, 0.000000000000000000, 0.000000000000000000 ) ) ;
#66037=DIRECTION ( 'NONE',  ( 0.000000000000000000, 0.000000000000000000, 1.000000000000000000 ) ) ;
#66040=SURFACE_STYLE_FILL_AREA ( #59121 ) ;
#66042=CARTESIAN_POINT ( 'NONE',  ( 57.00000000000000000, 14.00000000000000000, 60.00402776293825724 ) ) ;
#66047=FILL_AREA_STYLE ('',( #33021 ) ) ;
#66049=ORIENTED_EDGE ( 'NONE', *, *, #34227, .F. ) ;
#66055=EDGE_CURVE ( 'NONE', #25561, #11136, #9917, .T. ) ;
#66056=ORIENTED_EDGE ( 'NONE', *, *, #25271, .T. ) ;
#66057=FACE_OUTER_BOUND ( 'NONE', #26839, .T. ) ;
#66060=DIRECTION ( 'NONE',  ( 0.000000000000000000, -0.000000000000000000, -1.000000000000000000 ) ) ;
#66061=ORIENTED_EDGE ( 'NONE', *, *, #47807, .F. ) ;
#66064=PRESENTATION_STYLE_ASSIGNMENT (( #1977 ) ) ;
#66066=VECTOR ( 'NONE', #35670, 1000.000000000000000 ) ;
#66067=( NAMED_UNIT ( * ) PLANE_ANGLE_UNIT ( ) SI_UNIT ( $, .RADIAN. ) );
#66070=( NAMED_UNIT ( * ) PLANE_ANGLE_UNIT ( ) SI_UNIT ( $, .RADIAN. ) );
#66073=CARTESIAN_POINT ( 'NONE',  ( 31.00000000000001421, 43.00000000000000000, 36.49999999999999289 ) ) ;
#66078=CARTESIAN_POINT ( 'NONE',  ( 25.00000000000001421, 43.00000000000000000, -34.49999999999999289 ) ) ;
#66080=( GEOMETRIC_REPRESENTATION_CONTEXT ( 3 ) GLOBAL_UNCERTAINTY_ASSIGNED_CONTEXT ( ( #49484 ) ) GLOBAL_UNIT_ASSIGNED_CONTEXT ( ( #14337, #2333, #47811 ) ) REPRESENTATION_CONTEXT ( 'NONE', 'WORKASPACE' ) );
#66084=CARTESIAN_POINT ( 'NONE',  ( 31.00000000000001421, 43.00000000000000000, 36.50000000000000000 ) ) ;
#66085=ORIENTED_EDGE ( 'NONE', *, *, #9003, .F. ) ;
#66086=VECTOR ( 'NONE', #15529, 1000.000000000000000 ) ;
#66096=SURFACE_SIDE_STYLE ('',( #69406 ) ) ;
#66098=MECHANICAL_DESIGN_GEOMETRIC_PRESENTATION_REPRESENTATION('',(#14434),#24500);
#66100=SURFACE_SIDE_STYLE ('',( #17611 ) ) ;
#66105=DIRECTION ( 'NONE',  ( -1.000000000000000000, 0.000000000000000000, 1.300977106640434891E-16 ) ) ;
#66109=CIRCLE ( 'NONE', #54853, 1.000000000000000888 ) ;
#66118=CARTESIAN_POINT ( 'NONE',  ( 23.50000000000001776, 42.00000000000000000, 29.68999999999999417 ) ) ;
#66128=DIRECTION ( 'NONE',  ( 1.000000000000000000, 0.000000000000000000, 0.000000000000000000 ) ) ;
#66130=CARTESIAN_POINT ( 'NONE',  ( 23.50000000000001776, 15.00000000000000000, -29.68999999999999417 ) ) ;
#66133=VERTEX_POINT ( 'NONE', #18532 ) ;
#66140=LINE ( 'NONE', #61541, #19228 ) ;
#66141=FILL_AREA_STYLE ('',( #22555 ) ) ;
#66152=DIRECTION ( 'NONE',  ( 0.000000000000000000, 0.000000000000000000, 1.000000000000000000 ) ) ;
#66161=FILL_AREA_STYLE ('',( #2076 ) ) ;
#66173=COLOUR_RGB ( '', 0.72549020, 0.75294118, 0.79215686) ;
#66176=CARTESIAN_POINT ( 'NONE',  ( 27.00000000000001776, 15.00000000000000000, 29.68999999999999417 ) ) ;
#66198=SURFACE_SIDE_STYLE ('',( #60922 ) ) ;
#66207=DIRECTION ( 'NONE',  ( -0.000000000000000000, -1.000000000000000000, -0.000000000000000000 ) ) ;
#66214=DIRECTION ( 'NONE',  ( 0.000000000000000000, 0.000000000000000000, 1.000000000000000000 ) ) ;
#66223=CARTESIAN_POINT ( 'NONE',  ( 31.00000000000001421, 42.00000000000000000, 36.50000000000000000 ) ) ;
#66224=STYLED_ITEM ( 'NONE', ( #5618 ), #15305 ) ;
#66226=STYLED_ITEM ( 'NONE', ( #6079 ), #15907 ) ;
#66227=EDGE_LOOP ( 'NONE', ( #22861, #49928, #66747, #39834 ) ) ;
#66228=DIRECTION ( 'NONE',  ( 0.000000000000000000, 0.000000000000000000, -1.000000000000000000 ) ) ;
#66233=( GEOMETRIC_REPRESENTATION_CONTEXT ( 3 ) GLOBAL_UNCERTAINTY_ASSIGNED_CONTEXT ( ( #2286 ) ) GLOBAL_UNIT_ASSIGNED_CONTEXT ( ( #47305, #9651, #17275 ) ) REPRESENTATION_CONTEXT ( 'NONE', 'WORKASPACE' ) );
#66237=( NAMED_UNIT ( * ) PLANE_ANGLE_UNIT ( ) SI_UNIT ( $, .RADIAN. ) );
#66246=FILL_AREA_STYLE ('',( #12781 ) ) ;
#66252=ORIENTED_EDGE ( 'NONE', *, *, #49255, .F. ) ;
#66270=CARTESIAN_POINT ( 'NONE',  ( 28.00000000000002842, 5.569094604152798667, -2.026984667724098355 ) ) ;
#66272=( LENGTH_UNIT ( ) NAMED_UNIT ( * ) SI_UNIT ( .MILLI., .METRE. ) );
#66288=DIRECTION ( 'NONE',  ( 0.000000000000000000, 0.000000000000000000, -1.000000000000000000 ) ) ;
#66289=CARTESIAN_POINT ( 'NONE',  ( 10.00000000000001776, 17.78868675966041835, -1.300977106640437060E-15 ) ) ;
#66307=CYLINDRICAL_SURFACE ( 'NONE', #45400, 5.000000000000004441 ) ;
#66318=CARTESIAN_POINT ( 'NONE',  ( 10.00000000000001954, 50.00000000000000000, 46.00000000000000000 ) ) ;
#66320=( NAMED_UNIT ( * ) PLANE_ANGLE_UNIT ( ) SI_UNIT ( $, .RADIAN. ) );
#66324=( GEOMETRIC_REPRESENTATION_CONTEXT ( 3 ) GLOBAL_UNCERTAINTY_ASSIGNED_CONTEXT ( ( #60123 ) ) GLOBAL_UNIT_ASSIGNED_CONTEXT ( ( #50216, #54427, #5891 ) ) REPRESENTATION_CONTEXT ( 'NONE', 'WORKASPACE' ) );
#66350=CARTESIAN_POINT ( 'NONE',  ( 0.9999999999999991118, 43.00000000000000000, 45.61250543006183733 ) ) ;
#66357=TOROIDAL_SURFACE ( 'NONE', #14709, 6.000000000000000000, 1.000000000000000000 ) ;
#66361=VECTOR ( 'NONE', #44637, 1000.000000000000000 ) ;
#66363=DIRECTION ( 'NONE',  ( 1.300977106640434891E-16, -0.000000000000000000, 1.000000000000000000 ) ) ;
#66366=CARTESIAN_POINT ( 'NONE',  ( 2.527095087882868789E-16, 42.58578643762690774, 35.91421356237309226 ) ) ;
#66375=UNCERTAINTY_MEASURE_WITH_UNIT (LENGTH_MEASURE( 1.000000000000000082E-05 ), #52714, 'distance_accuracy_value', 'NONE');
#66376=STYLED_ITEM ( 'NONE', ( #31862 ), #16864 ) ;
#66377=CARTESIAN_POINT ( 'NONE',  ( 11.00000000000001776, -3.148064030671221758, -29.68999999999999417 ) ) ;
#66380=CARTESIAN_POINT ( 'NONE',  ( 28.00000000000002842, 38.70020753820971748, 89.00000000000000000 ) ) ;
#66381=ADVANCED_FACE ( 'NONE', ( #59606, #64558 ), #1509, .F. ) ;
#66385=ORIENTED_EDGE ( 'NONE', *, *, #52653, .F. ) ;
#66386=SURFACE_STYLE_FILL_AREA ( #44976 ) ;
#66387=CIRCLE ( 'NONE', #45057, 5.000000000000004441 ) ;
#66389=PLANE ( 'NONE',  #51837 ) ;
#66390=MECHANICAL_DESIGN_GEOMETRIC_PRESENTATION_REPRESENTATION('',(#15875),#68681);
#66404=DIRECTION ( 'NONE',  ( 0.000000000000000000, 0.000000000000000000, -1.000000000000000000 ) ) ;
#66413=ORIENTED_EDGE ( 'NONE', *, *, #822, .F. ) ;
#66416=CARTESIAN_POINT ( 'NONE',  ( 24.35019923159519450, 27.05390878412926270, -27.33833584792231974 ) ) ;
#66424=CARTESIAN_POINT ( 'NONE',  ( 7.000000000000017764, 17.04554193418302788, 0.6691306063588586817 ) ) ;
#66425=VERTEX_POINT ( 'NONE', #27584 ) ;
#66439=EDGE_LOOP ( 'NONE', ( #51517, #12944 ) ) ;
#66446=( NAMED_UNIT ( * ) SI_UNIT ( $, .STERADIAN. ) SOLID_ANGLE_UNIT ( ) );
#66453=CIRCLE ( 'NONE', #38443, 0.9999999999999984457 ) ;
#66459=DIRECTION ( 'NONE',  ( 0.000000000000000000, 0.000000000000000000, -1.000000000000000000 ) ) ;
#66481=DIRECTION ( 'NONE',  ( 0.000000000000000000, 0.000000000000000000, -1.000000000000000000 ) ) ;
#66491=LINE ( 'NONE', #46463, #19599 ) ;
#66492=AXIS2_PLACEMENT_3D ( 'NONE', #46776, #67834, #3044 ) ;
#66498=ORIENTED_EDGE ( 'NONE', *, *, #2571, .T. ) ;
#66506=CARTESIAN_POINT ( 'NONE',  ( 0.9999999999999991118, 43.00000000000000000, 45.61250543006183733 ) ) ;
#66510=SURFACE_STYLE_FILL_AREA ( #60867 ) ;
#66542=EDGE_LOOP ( 'NONE', ( #31289, #50315, #54247, #5480, #30170, #55957, #12594, #33783, #46585, #34401 ) ) ;
#66543=( NAMED_UNIT ( * ) PLANE_ANGLE_UNIT ( ) SI_UNIT ( $, .RADIAN. ) );
#66548=DIRECTION ( 'NONE',  ( 0.000000000000000000, 0.000000000000000000, -1.000000000000000000 ) ) ;
#66552=EDGE_CURVE ( 'NONE', #22382, #67437, #39585, .T. ) ;
#66558=LINE ( 'NONE', #67247, #28962 ) ;
#66567=EDGE_CURVE ( 'NONE', #59091, #22594, #18904, .T. ) ;
#66573=LINE ( 'NONE', #50068, #38642 ) ;
#66580=( GEOMETRIC_REPRESENTATION_CONTEXT ( 3 ) GLOBAL_UNCERTAINTY_ASSIGNED_CONTEXT ( ( #67934 ) ) GLOBAL_UNIT_ASSIGNED_CONTEXT ( ( #1570, #33975, #67042 ) ) REPRESENTATION_CONTEXT ( 'NONE', 'WORKASPACE' ) );
#66584=VERTEX_POINT ( 'NONE', #13857 ) ;
#66591=ORIENTED_EDGE ( 'NONE', *, *, #67861, .T. ) ;
#66597=PLANE ( 'NONE',  #46517 ) ;
#66602=ORIENTED_EDGE ( 'NONE', *, *, #24301, .F. ) ;
#66606=CARTESIAN_POINT ( 'NONE',  ( 36.00000000000002842, 0.000000000000000000, 77.00402776293825013 ) ) ;
#66621=ORIENTED_EDGE ( 'NONE', *, *, #69502, .F. ) ;
#66636=EDGE_CURVE ( 'NONE', #4733, #17912, #15600, .T. ) ;
#66640=ADVANCED_FACE ( 'NONE', ( #9288 ), #58852, .T. ) ;
#66641=DIRECTION ( 'NONE',  ( 0.000000000000000000, 0.000000000000000000, -1.000000000000000000 ) ) ;
#66648=AXIS2_PLACEMENT_3D ( 'NONE', #42618, #48236, #58759 ) ;
#66649=SURFACE_STYLE_FILL_AREA ( #19833 ) ;
#66669=LINE ( 'NONE', #17122, #4874 ) ;
#66688=EDGE_LOOP ( 'NONE', ( #64700, #47314, #14251, #31217 ) ) ;
#66691=CARTESIAN_POINT ( 'NONE',  ( 7.999999999999998224, 5.000000000000000000, -37.00402776293825724 ) ) ;
#66692=ORIENTED_EDGE ( 'NONE', *, *, #65764, .F. ) ;
#66695=AXIS2_PLACEMENT_3D ( 'NONE', #38283, #33647, #55085 ) ;
#66698=ADVANCED_FACE ( 'NONE', ( #21197 ), #43427, .T. ) ;
#66703=CIRCLE ( 'NONE', #40884, 5.000000000000004441 ) ;
#66713=DIRECTION ( 'NONE',  ( -0.000000000000000000, -1.000000000000000000, -0.000000000000000000 ) ) ;
#66715=SURFACE_STYLE_FILL_AREA ( #29773 ) ;
#66734=VECTOR ( 'NONE', #37201, 1000.000000000000000 ) ;
#66747=ORIENTED_EDGE ( 'NONE', *, *, #20567, .F. ) ;
#66748=COLOUR_RGB ( '', 0.09019608, 0.27058824, 0.51372549) ;
#66763=CARTESIAN_POINT ( 'NONE',  ( 8.000000000000030198, 5.000000000000000000, 29.00402776293826079 ) ) ;
#66764=VERTEX_POINT ( 'NONE', #55293 ) ;
#66767=CARTESIAN_POINT ( 'NONE',  ( 30.99999999999998579, 0.000000000000000000, -72.00402776293822171 ) ) ;
#66788=SURFACE_STYLE_USAGE ( .BOTH. , #45368 ) ;
#66790=DIRECTION ( 'NONE',  ( 1.000000000000000000, -0.000000000000000000, -1.300977106640434891E-16 ) ) ;
#66791=DIRECTION ( 'NONE',  ( 0.000000000000000000, 0.000000000000000000, -1.000000000000000000 ) ) ;
#66822=( LENGTH_UNIT ( ) NAMED_UNIT ( * ) SI_UNIT ( .MILLI., .METRE. ) );
#66825=( LENGTH_UNIT ( ) NAMED_UNIT ( * ) SI_UNIT ( .MILLI., .METRE. ) );
#66826=CIRCLE ( 'NONE', #69087, 1.000000000000000888 ) ;
#66827=EDGE_CURVE ( 'NONE', #26732, #27703, #51571, .T. ) ;
#66831=( LENGTH_UNIT ( ) NAMED_UNIT ( * ) SI_UNIT ( .MILLI., .METRE. ) );
#66833=VECTOR ( 'NONE', #55668, 1000.000000000000000 ) ;
#66850=COLOUR_RGB ( '', 0.40784314, 0.44705882, 0.49803922) ;
#66851=COLOUR_RGB ( '', 0.72549020, 0.75294118, 0.79215686) ;
#66854=DIRECTION ( 'NONE',  ( 0.000000000000000000, 1.000000000000000000, -0.000000000000000000 ) ) ;
#66856=ORIENTED_EDGE ( 'NONE', *, *, #41585, .F. ) ;
#66860=VERTEX_POINT ( 'NONE', #61950 ) ;
#66867=( NAMED_UNIT ( * ) SI_UNIT ( $, .STERADIAN. ) SOLID_ANGLE_UNIT ( ) );
#66880=ORIENTED_EDGE ( 'NONE', *, *, #7013, .T. ) ;
#66884=( NAMED_UNIT ( * ) SI_UNIT ( $, .STERADIAN. ) SOLID_ANGLE_UNIT ( ) );
#66908=( NAMED_UNIT ( * ) SI_UNIT ( $, .STERADIAN. ) SOLID_ANGLE_UNIT ( ) );
#66918=DIRECTION ( 'NONE',  ( -0.000000000000000000, -0.000000000000000000, -1.000000000000000000 ) ) ;
#66926=DIRECTION ( 'NONE',  ( 0.000000000000000000, 0.000000000000000000, -1.000000000000000000 ) ) ;
#66927=ORIENTED_EDGE ( 'NONE', *, *, #42064, .F. ) ;
#66931=( NAMED_UNIT ( * ) PLANE_ANGLE_UNIT ( ) SI_UNIT ( $, .RADIAN. ) );
#66932=EDGE_CURVE ( 'NONE', #22147, #30954, #46995, .T. ) ;
#66940=ORIENTED_EDGE ( 'NONE', *, *, #9944, .T. ) ;
#66963=SURFACE_STYLE_FILL_AREA ( #66246 ) ;
#66965=( BOUNDED_CURVE ( )  B_SPLINE_CURVE ( 3, ( #34038, #21763, #44644, #54450 ),
 .UNSPECIFIED., .F., .F. ) 
 B_SPLINE_CURVE_WITH_KNOTS ( ( 4, 4 ),
 ( 4.712388980384689674, 6.283185307179586232 ),
 .UNSPECIFIED. ) 
 CURVE ( )  GEOMETRIC_REPRESENTATION_ITEM ( )  RATIONAL_B_SPLINE_CURVE ( ( 1.000000000000000000, 0.8047378541243649375, 0.8047378541243649375, 1.000000000000000000 ) ) 
 REPRESENTATION_ITEM ( '' )  );
#66968=DIRECTION ( 'NONE',  ( 1.000000000000000000, 0.000000000000000000, 0.000000000000000000 ) ) ;
#66972=ORIENTED_EDGE ( 'NONE', *, *, #58867, .T. ) ;
#66988=SURFACE_STYLE_USAGE ( .BOTH. , #45567 ) ;
#66989=FILL_AREA_STYLE ('',( #28965 ) ) ;
#66991=CARTESIAN_POINT ( 'NONE',  ( 23.50000000000041211, 24.55989583709592949, -27.18999999999997286 ) ) ;
#66997=DIRECTION ( 'NONE',  ( 0.000000000000000000, 0.000000000000000000, -1.000000000000000000 ) ) ;
#66998=( NAMED_UNIT ( * ) SI_UNIT ( $, .STERADIAN. ) SOLID_ANGLE_UNIT ( ) );
#67012=FILL_AREA_STYLE ('',( #67700 ) ) ;
#67030=EDGE_LOOP ( 'NONE', ( #13386, #24648, #41687, #27440 ) ) ;
#67042=( NAMED_UNIT ( * ) SI_UNIT ( $, .STERADIAN. ) SOLID_ANGLE_UNIT ( ) );
#67044=VERTEX_POINT ( 'NONE', #35938 ) ;
#67048=ORIENTED_EDGE ( 'NONE', *, *, #61237, .T. ) ;
#67076=DIRECTION ( 'NONE',  ( -1.300977106640434891E-16, 0.000000000000000000, -1.000000000000000000 ) ) ;
#67080=SURFACE_STYLE_USAGE ( .BOTH. , #2996 ) ;
#67084=( LENGTH_UNIT ( ) NAMED_UNIT ( * ) SI_UNIT ( .MILLI., .METRE. ) );
#67086=AXIS2_PLACEMENT_3D ( 'NONE', #43558, #20674, #64258 ) ;
#67087=VECTOR ( 'NONE', #32014, 1000.000000000000000 ) ;
#67088=CARTESIAN_POINT ( 'NONE',  ( 23.50000000000001776, 14.00000000000000000, -29.68999999999999417 ) ) ;
#67096=LINE ( 'NONE', #45341, #17283 ) ;
#67099=VERTEX_POINT ( 'NONE', #38995 ) ;
#67105=DIRECTION ( 'NONE',  ( 0.000000000000000000, 0.000000000000000000, 1.000000000000000000 ) ) ;
#67112=DIRECTION ( 'NONE',  ( 0.000000000000000000, 0.000000000000000000, 1.000000000000000000 ) ) ;
#67119=EDGE_CURVE ( 'NONE', #22594, #8864, #28722, .T. ) ;
#67121=DIRECTION ( 'NONE',  ( -0.000000000000000000, -1.000000000000000000, -0.000000000000000000 ) ) ;
#67127=CARTESIAN_POINT ( 'NONE',  ( 25.00000000000001421, 42.00000000000000000, 0.000000000000000000 ) ) ;
#67138=CARTESIAN_POINT ( 'NONE',  ( 29.00000000000000000, 43.00000000000000000, -79.00402776293826435 ) ) ;
#67139=DIRECTION ( 'NONE',  ( -0.000000000000000000, -0.000000000000000000, -1.000000000000000000 ) ) ;
#67144=DIRECTION ( 'NONE',  ( 0.000000000000000000, 0.000000000000000000, -1.000000000000000000 ) ) ;
#67146=( NAMED_UNIT ( * ) PLANE_ANGLE_UNIT ( ) SI_UNIT ( $, .RADIAN. ) );
#67152=CARTESIAN_POINT ( 'NONE',  ( 31.00000000000000000, 43.00000000000000000, -80.00402776293826435 ) ) ;
#67155=CYLINDRICAL_SURFACE ( 'NONE', #46095, 1.000000000000000888 ) ;
#67156=TOROIDAL_SURFACE ( 'NONE', #3013, 111.0000000000000142, 1.000000000000000000 ) ;
#67157=LINE ( 'NONE', #35844, #44974 ) ;
#67162=DIRECTION ( 'NONE',  ( 0.000000000000000000, -1.000000000000000000, 0.000000000000000000 ) ) ;
#67163=( NAMED_UNIT ( * ) PLANE_ANGLE_UNIT ( ) SI_UNIT ( $, .RADIAN. ) );
#67164=UNCERTAINTY_MEASURE_WITH_UNIT (LENGTH_MEASURE( 1.000000000000000082E-05 ), #35708, 'distance_accuracy_value', 'NONE');
#67170=CARTESIAN_POINT ( 'NONE',  ( 86.21825843581756033, 5.000000000000000000, 39.83014742847163348 ) ) ;
#67190=VECTOR ( 'NONE', #24412, 1000.000000000000000 ) ;
#67194=FILL_AREA_STYLE_COLOUR ( '', #3605 ) ;
#67196=FILL_AREA_STYLE ('',( #45777 ) ) ;
#67224=VERTEX_POINT ( 'NONE', #2988 ) ;
#67225=SURFACE_STYLE_FILL_AREA ( #45803 ) ;
#67226=DIRECTION ( 'NONE',  ( 0.000000000000000000, 0.000000000000000000, -1.000000000000000000 ) ) ;
#67236=CARTESIAN_POINT ( 'NONE',  ( 22.41829134511430155, 26.69040202514700866, -27.43543867392220648 ) ) ;
#67245=UNCERTAINTY_MEASURE_WITH_UNIT (LENGTH_MEASURE( 1.000000000000000082E-05 ), #26996, 'distance_accuracy_value', 'NONE');
#67247=CARTESIAN_POINT ( 'NONE',  ( 1.000000000000000000, 43.00000000000000000, 80.00402776293826435 ) ) ;
#67251=COLOUR_RGB ( '', 0.09019608, 0.27058824, 0.51372549) ;
#67256=DIRECTION ( 'NONE',  ( -0.000000000000000000, -1.000000000000000000, 0.000000000000000000 ) ) ;
#67259=UNCERTAINTY_MEASURE_WITH_UNIT (LENGTH_MEASURE( 1.000000000000000082E-05 ), #62298, 'distance_accuracy_value', 'NONE');
#67261=ADVANCED_FACE ( 'NONE', ( #40712 ), #67768, .F. ) ;
#67263=( GEOMETRIC_REPRESENTATION_CONTEXT ( 3 ) GLOBAL_UNCERTAINTY_ASSIGNED_CONTEXT ( ( #47540 ) ) GLOBAL_UNIT_ASSIGNED_CONTEXT ( ( #52883, #11680, #44443 ) ) REPRESENTATION_CONTEXT ( 'NONE', 'WORKASPACE' ) );
#67266=EDGE_CURVE ( 'NONE', #52535, #29977, #7977, .T. ) ;
#67275=( NAMED_UNIT ( * ) PLANE_ANGLE_UNIT ( ) SI_UNIT ( $, .RADIAN. ) );
#67279=CARTESIAN_POINT ( 'NONE',  ( 35.99999999999999289, 0.000000000000000000, -24.00402776293825369 ) ) ;
#67288=STYLED_ITEM ( 'NONE', ( #20813 ), #51194 ) ;
#67291=SURFACE_STYLE_USAGE ( .BOTH. , #2872 ) ;
#67293=CARTESIAN_POINT ( 'NONE',  ( 3.000000000000003109, 42.58578643762690774, -80.00402776293826435 ) ) ;
#67302=CARTESIAN_POINT ( 'NONE',  ( 31.00000000000000000, 42.00000000000000000, -75.00000000000001421 ) ) ;
#67307=VECTOR ( 'NONE', #7614, 1000.000000000000000 ) ;
#67327=MECHANICAL_DESIGN_GEOMETRIC_PRESENTATION_REPRESENTATION('',(#51605),#2119);
#67328=ORIENTED_EDGE ( 'NONE', *, *, #6279, .T. ) ;
#67330=LINE ( 'NONE', #39248, #2073 ) ;
#67331=MECHANICAL_DESIGN_GEOMETRIC_PRESENTATION_REPRESENTATION('',(#69585),#35911);
#67337=AXIS2_PLACEMENT_3D ( 'NONE', #2030, #33769, #66481 ) ;
#67338=EDGE_CURVE ( 'NONE', #4398, #41529, #24409, .T. ) ;
#67344=COLOUR_RGB ( '', 0.09019608, 0.27058824, 0.51372549) ;
#67357=TOROIDAL_SURFACE ( 'NONE', #10078, 6.000000000000000000, 1.000000000000000000 ) ;
#67373=VECTOR ( 'NONE', #37035, 1000.000000000000000 ) ;
#67397=( GEOMETRIC_REPRESENTATION_CONTEXT ( 3 ) GLOBAL_UNCERTAINTY_ASSIGNED_CONTEXT ( ( #5124 ) ) GLOBAL_UNIT_ASSIGNED_CONTEXT ( ( #49961, #50982, #60817 ) ) REPRESENTATION_CONTEXT ( 'NONE', 'WORKASPACE' ) );
#67405=COLOUR_RGB ( '', 0.66274510, 0.83137255, 0.94901961) ;
#67420=ADVANCED_FACE ( 'NONE', ( #15700 ), #67156, .T. ) ;
#67429=ORIENTED_EDGE ( 'NONE', *, *, #15745, .T. ) ;
#67432=SURFACE_SIDE_STYLE ('',( #35782 ) ) ;
#67435=AXIS2_PLACEMENT_3D ( 'NONE', #60729, #34014, #33334 ) ;
#67437=VERTEX_POINT ( 'NONE', #22346 ) ;
#67438=DIRECTION ( 'NONE',  ( 0.000000000000000000, 0.000000000000000000, 1.000000000000000000 ) ) ;
#67440=CARTESIAN_POINT ( 'NONE',  ( 22.00000000000002132, 42.00000000000000000, 75.00000000000000000 ) ) ;
#67449=( NAMED_UNIT ( * ) SI_UNIT ( $, .STERADIAN. ) SOLID_ANGLE_UNIT ( ) );
#67450=( GEOMETRIC_REPRESENTATION_CONTEXT ( 3 ) GLOBAL_UNCERTAINTY_ASSIGNED_CONTEXT ( ( #22698 ) ) GLOBAL_UNIT_ASSIGNED_CONTEXT ( ( #16278, #44414, #6023 ) ) REPRESENTATION_CONTEXT ( 'NONE', 'WORKASPACE' ) );
#67451=COLOUR_RGB ( '', 0.40784314, 0.44705882, 0.49803922) ;
#67458=( LENGTH_UNIT ( ) NAMED_UNIT ( * ) SI_UNIT ( .MILLI., .METRE. ) );
#67460=VECTOR ( 'NONE', #8187, 1000.000000000000227 ) ;
#67462=ORIENTED_EDGE ( 'NONE', *, *, #55276, .T. ) ;
#67473=STYLED_ITEM ( 'NONE', ( #47240 ), #53652 ) ;
#67497=CYLINDRICAL_SURFACE ( 'NONE', #49475, 1.000000000000000888 ) ;
#67503=( NAMED_UNIT ( * ) SI_UNIT ( $, .STERADIAN. ) SOLID_ANGLE_UNIT ( ) );
#67504=CARTESIAN_POINT ( 'NONE',  ( 25.00000000000001421, 42.00000000000000000, 29.68999999999999417 ) ) ;
#67505=STYLED_ITEM ( 'NONE', ( #54438 ), #59718 ) ;
#67506=CARTESIAN_POINT ( 'NONE',  ( 11.00000000000001776, 26.00000000000000355, -24.00000000000000355 ) ) ;
#67507=CARTESIAN_POINT ( 'NONE',  ( 10.00000000000000711, 50.00000000000000000, -65.00000000000000000 ) ) ;
#67508=( GEOMETRIC_REPRESENTATION_CONTEXT ( 3 ) GLOBAL_UNCERTAINTY_ASSIGNED_CONTEXT ( ( #65600 ) ) GLOBAL_UNIT_ASSIGNED_CONTEXT ( ( #69195, #69520, #54029 ) ) REPRESENTATION_CONTEXT ( 'NONE', 'WORKASPACE' ) );
#67510=ADVANCED_FACE ( 'NONE', ( #35334 ), #45901, .T. ) ;
#67535=ADVANCED_FACE ( 'NONE', ( #46263 ), #13158, .F. ) ;
#67537=CARTESIAN_POINT ( 'NONE',  ( 31.00000000000001421, 15.00000000000000000, 34.49999999999998579 ) ) ;
#67539=ORIENTED_EDGE ( 'NONE', *, *, #31527, .F. ) ;
#67561=PRESENTATION_STYLE_ASSIGNMENT (( #7444 ) ) ;
#67578=PRESENTATION_STYLE_ASSIGNMENT (( #23617 ) ) ;
#67585=SURFACE_STYLE_USAGE ( .BOTH. , #46160 ) ;
#67586=LINE ( 'NONE', #40886, #3849 ) ;
#67587=EDGE_CURVE ( 'NONE', #62632, #16376, #7377, .T. ) ;
#67588=SURFACE_SIDE_STYLE ('',( #8510 ) ) ;
#67589=DIRECTION ( 'NONE',  ( -1.000000000000000000, 0.000000000000000000, 0.000000000000000000 ) ) ;
#67591=CARTESIAN_POINT ( 'NONE',  ( 22.31835362224387964, 26.35424528420515955, -27.48617327699382074 ) ) ;
#67598=DIRECTION ( 'NONE',  ( -0.000000000000000000, -1.000000000000000000, -0.000000000000000000 ) ) ;
#67600=DIRECTION ( 'NONE',  ( 0.000000000000000000, -1.000000000000000000, 0.000000000000000000 ) ) ;
#67618=DIRECTION ( 'NONE',  ( -1.000000000000000000, 0.000000000000000000, 0.000000000000000000 ) ) ;
#67619=AXIS2_PLACEMENT_3D ( 'NONE', #16318, #37796, #59172 ) ;
#67631=ORIENTED_EDGE ( 'NONE', *, *, #68464, .T. ) ;
#67632=DIRECTION ( 'NONE',  ( 0.000000000000000000, 1.000000000000000000, 0.000000000000000000 ) ) ;
#67635=ORIENTED_EDGE ( 'NONE', *, *, #42396, .T. ) ;
#67652=( NAMED_UNIT ( * ) PLANE_ANGLE_UNIT ( ) SI_UNIT ( $, .RADIAN. ) );
#67655=ORIENTED_EDGE ( 'NONE', *, *, #39851, .F. ) ;
#67659=ORIENTED_EDGE ( 'NONE', *, *, #51249, .T. ) ;
#67667=VECTOR ( 'NONE', #35201, 1000.000000000000000 ) ;
#67677=COLOUR_RGB ( '', 0.31764706, 0.68627451, 0.89019608) ;
#67681=TOROIDAL_SURFACE ( 'NONE', #22737, 2.000000000000000000, 1.000000000000000000 ) ;
#67697=VERTEX_POINT ( 'NONE', #59530 ) ;
#67700=FILL_AREA_STYLE_COLOUR ( '', #23979 ) ;
#67704=( LENGTH_UNIT ( ) NAMED_UNIT ( * ) SI_UNIT ( .MILLI., .METRE. ) );
#67707=ORIENTED_EDGE ( 'NONE', *, *, #2497, .T. ) ;
#67708=LINE ( 'NONE', #8282, #50515 ) ;
#67714=VECTOR ( 'NONE', #53000, 1000.000000000000000 ) ;
#67719=EDGE_LOOP ( 'NONE', ( #9937, #2626, #4455 ) ) ;
#67721=CARTESIAN_POINT ( 'NONE',  ( 57.00000000000000000, 14.00000000000000000, -47.50402776293824303 ) ) ;
#67723=( NAMED_UNIT ( * ) SI_UNIT ( $, .STERADIAN. ) SOLID_ANGLE_UNIT ( ) );
#67733=ORIENTED_EDGE ( 'NONE', *, *, #40293, .T. ) ;
#67735=AXIS2_PLACEMENT_3D ( 'NONE', #63344, #35585, #8841 ) ;
#67741=EDGE_CURVE ( 'NONE', #26455, #8636, #65513, .T. ) ;
#67746=SURFACE_SIDE_STYLE ('',( #24807 ) ) ;
#67751=DIRECTION ( 'NONE',  ( 0.000000000000000000, 0.000000000000000000, 1.000000000000000000 ) ) ;
#67755=CARTESIAN_POINT ( 'NONE',  ( 31.00000000000000000, 43.00000000000000000, -79.00402776293826435 ) ) ;
#67768=CYLINDRICAL_SURFACE ( 'NONE', #51421, 16.00000000000000711 ) ;
#67778=UNCERTAINTY_MEASURE_WITH_UNIT (LENGTH_MEASURE( 1.000000000000000082E-05 ), #21918, 'distance_accuracy_value', 'NONE');
#67780=COLOUR_RGB ( '', 0.72549020, 0.75294118, 0.79215686) ;
#67783=CARTESIAN_POINT ( 'NONE',  ( 32.00000000000002132, 42.00000000000000000, 79.00402776293823592 ) ) ;
#67798=DIRECTION ( 'NONE',  ( 0.000000000000000000, 0.000000000000000000, -1.000000000000000000 ) ) ;
#67807=COLOUR_RGB ( '', 0.72549020, 0.75294118, 0.79215686) ;
#67819=FILL_AREA_STYLE ('',( #61812 ) ) ;
#67826=ORIENTED_EDGE ( 'NONE', *, *, #56285, .F. ) ;
#67827=CARTESIAN_POINT ( 'NONE',  ( 26.00000000000001776, -3.148064030671221758, -34.49999999999999289 ) ) ;
#67834=DIRECTION ( 'NONE',  ( -3.469446951953617344E-15, -0.000000000000000000, 1.000000000000000000 ) ) ;
#67848=DIRECTION ( 'NONE',  ( 0.000000000000000000, 0.000000000000000000, 1.000000000000000000 ) ) ;
#67850=DIRECTION ( 'NONE',  ( -3.469446951953611033E-15, 0.000000000000000000, -1.000000000000000000 ) ) ;
#67859=FACE_OUTER_BOUND ( 'NONE', #4816, .T. ) ;
#67861=EDGE_CURVE ( 'NONE', #2313, #69517, #40190, .T. ) ;
#67862=SURFACE_STYLE_USAGE ( .BOTH. , #46436 ) ;
#67864=DIRECTION ( 'NONE',  ( 0.000000000000000000, 0.000000000000000000, -1.000000000000000000 ) ) ;
#67873=( NAMED_UNIT ( * ) SI_UNIT ( $, .STERADIAN. ) SOLID_ANGLE_UNIT ( ) );
#67874=UNCERTAINTY_MEASURE_WITH_UNIT (LENGTH_MEASURE( 1.000000000000000082E-05 ), #53082, 'distance_accuracy_value', 'NONE');
#67885=ORIENTED_EDGE ( 'NONE', *, *, #54494, .T. ) ;
#67888=CARTESIAN_POINT ( 'NONE',  ( 107.0858988931383493, 5.000000000000000000, 16.89933289725615850 ) ) ;
#67897=ORIENTED_EDGE ( 'NONE', *, *, #57909, .F. ) ;
#67903=ORIENTED_EDGE ( 'NONE', *, *, #29743, .T. ) ;
#67909=EDGE_CURVE ( 'NONE', #56593, #55122, #66558, .T. ) ;
#67910=CARTESIAN_POINT ( 'NONE',  ( 1.000000000000000000, 42.00000000000000000, 0.000000000000000000 ) ) ;
#67915=ORIENTED_EDGE ( 'NONE', *, *, #47065, .T. ) ;
#67918=UNCERTAINTY_MEASURE_WITH_UNIT (LENGTH_MEASURE( 1.000000000000000082E-05 ), #11817, 'distance_accuracy_value', 'NONE');
#67923=EDGE_CURVE ( 'NONE', #49856, #31350, #10578, .T. ) ;
#67928=MECHANICAL_DESIGN_GEOMETRIC_PRESENTATION_REPRESENTATION('',(#55551),#36518);
#67934=UNCERTAINTY_MEASURE_WITH_UNIT (LENGTH_MEASURE( 1.000000000000000082E-05 ), #1570, 'distance_accuracy_value', 'NONE');
#67951=VECTOR ( 'NONE', #65086, 1000.000000000000000 ) ;
#67952=CARTESIAN_POINT ( 'NONE',  ( 98.00000000000000000, 16.00000000000000000, -12.50000000000000178 ) ) ;
#67953=CIRCLE ( 'NONE', #17393, 5.000000000000004441 ) ;
#67961=CARTESIAN_POINT ( 'NONE',  ( 73.01088739851485343, 0.000000000000000000, 65.71817553072288831 ) ) ;
#67982=CARTESIAN_POINT ( 'NONE',  ( 31.00000000000002132, 42.00000000000000000, 79.00402776293823592 ) ) ;
#67983=VECTOR ( 'NONE', #61739, 1000.000000000000000 ) ;
#67990=CARTESIAN_POINT ( 'NONE',  ( 32.00000000000001421, 42.00000000000000711, 44.99999999999998579 ) ) ;
#67992=SURFACE_SIDE_STYLE ('',( #3929 ) ) ;
#67998=CARTESIAN_POINT ( 'NONE',  ( 179.4361977533490347, 14.00000000000000000, 103.7004518695263044 ) ) ;
#68010=ORIENTED_EDGE ( 'NONE', *, *, #55610, .F. ) ;
#68014=CARTESIAN_POINT ( 'NONE',  ( 31.91038508792758677, 42.48853761352473413, 45.29557347147077451 ) ) ;
#68016=SURFACE_STYLE_USAGE ( .BOTH. , #57086 ) ;
#68020=EDGE_CURVE ( 'NONE', #30008, #20328, #4941, .T. ) ;
#68025=VERTEX_POINT ( 'NONE', #43659 ) ;
#68031=( NAMED_UNIT ( * ) PLANE_ANGLE_UNIT ( ) SI_UNIT ( $, .RADIAN. ) );
#68038=CARTESIAN_POINT ( 'NONE',  ( 1.709458476932651091E-14, 43.00000000000000000, -35.50000000000000000 ) ) ;
#68053=PRESENTATION_STYLE_ASSIGNMENT (( #46972 ) ) ;
#68056=LINE ( 'NONE', #3625, #65319 ) ;
#68064=FILL_AREA_STYLE_COLOUR ( '', #48283 ) ;
#68074=SURFACE_SIDE_STYLE ('',( #25142 ) ) ;
#68076=DIRECTION ( 'NONE',  ( -1.000000000000000000, 0.000000000000000000, 0.000000000000000000 ) ) ;
#68092=ORIENTED_EDGE ( 'NONE', *, *, #65978, .F. ) ;
#68095=CARTESIAN_POINT ( 'NONE',  ( 74.89452121010485541, 14.00000000000000000, -66.39042820928574429 ) ) ;
#68097=ORIENTED_EDGE ( 'NONE', *, *, #26693, .T. ) ;
#68116=FACE_OUTER_BOUND ( 'NONE', #30863, .T. ) ;
#68119=VECTOR ( 'NONE', #62855, 1000.000000000000000 ) ;
#68125=CARTESIAN_POINT ( 'NONE',  ( 98.00000000000000000, 0.000000000000000000, 0.000000000000000000 ) ) ;
#68130=FACE_OUTER_BOUND ( 'NONE', #35800, .T. ) ;
#68137=DIRECTION ( 'NONE',  ( 1.300977106640434891E-16, -0.000000000000000000, 1.000000000000000000 ) ) ;
#68141=LINE ( 'NONE', #19926, #7232 ) ;
#68143=ORIENTED_EDGE ( 'NONE', *, *, #40014, .F. ) ;
#68148=CARTESIAN_POINT ( 'NONE',  ( 22.31817967265634195, 25.64624525132450472, -27.48625952250267801 ) ) ;
#68160=SURFACE_STYLE_USAGE ( .BOTH. , #3738 ) ;
#68163=ADVANCED_FACE ( 'NONE', ( #14361 ), #9810, .T. ) ;
#68164=CARTESIAN_POINT ( 'NONE',  ( 0.000000000000000000, 43.00000000000000000, 0.000000000000000000 ) ) ;
#68171=EDGE_LOOP ( 'NONE', ( #38517, #56683, #56076, #34482, #35181, #58975, #25938, #61056 ) ) ;
#68173=SURFACE_STYLE_FILL_AREA ( #67819 ) ;
#68174=VECTOR ( 'NONE', #65636, 1000.000000000000000 ) ;
#68177=DIRECTION ( 'NONE',  ( 0.000000000000000000, 0.000000000000000000, 1.000000000000000000 ) ) ;
#68184=DIRECTION ( 'NONE',  ( 1.000000000000000000, 0.000000000000000000, 0.000000000000000000 ) ) ;
#68204=DIRECTION ( 'NONE',  ( -1.300977106640434891E-16, 0.000000000000000000, -1.000000000000000000 ) ) ;
#68216=DIRECTION ( 'NONE',  ( 0.000000000000000000, 0.000000000000000000, -1.000000000000000000 ) ) ;
#68217=SURFACE_STYLE_FILL_AREA ( #62565 ) ;
#68218=DIRECTION ( 'NONE',  ( 0.000000000000000000, -1.000000000000000000, 0.000000000000000000 ) ) ;
#68227=( NAMED_UNIT ( * ) SI_UNIT ( $, .STERADIAN. ) SOLID_ANGLE_UNIT ( ) );
#68233=CARTESIAN_POINT ( 'NONE',  ( 2.000000000000008882, 26.00000000000000355, -24.00000000000000355 ) ) ;
#68234=CARTESIAN_POINT ( 'NONE',  ( 10.00000000000001776, 42.00000000000000000, -28.38386403503541899 ) ) ;
#68236=( NAMED_UNIT ( * ) PLANE_ANGLE_UNIT ( ) SI_UNIT ( $, .RADIAN. ) );
#68252=ADVANCED_FACE ( 'NONE', ( #41141 ), #20338, .F. ) ;
#68263=CARTESIAN_POINT ( 'NONE',  ( 29.00000000000002842, 34.80256050929376954, 80.00402776293826435 ) ) ;
#68278=CIRCLE ( 'NONE', #12059, 1.000000000000000000 ) ;
#68280=EDGE_LOOP ( 'NONE', ( #51988, #27705, #29210, #36615 ) ) ;
#68286=DIRECTION ( 'NONE',  ( 0.000000000000000000, -0.6449798928094538919, 0.7641995406119433953 ) ) ;
#68294=CARTESIAN_POINT ( 'NONE',  ( 28.00000000000000000, 38.00000000000000711, -90.00000000000000000 ) ) ;
#68317=CARTESIAN_POINT ( 'NONE',  ( 22.00000000000000711, 50.00000000000000000, -60.00000000000000000 ) ) ;
#68334=CARTESIAN_POINT ( 'NONE',  ( 28.00000000000002842, 38.70020753820971748, 89.00000000000000000 ) ) ;
#68347=LINE ( 'NONE', #37067, #2467 ) ;
#68348=SURFACE_STYLE_FILL_AREA ( #40954 ) ;
#68351=CARTESIAN_POINT ( 'NONE',  ( 96.10348817448824832, 5.000000000000000000, -27.38099488609876531 ) ) ;
#68352=ORIENTED_EDGE ( 'NONE', *, *, #39976, .T. ) ;
#68354=AXIS2_PLACEMENT_3D ( 'NONE', #16736, #16403, #43151 ) ;
#68355=DIRECTION ( 'NONE',  ( 1.000000000000000000, -0.000000000000000000, -0.000000000000000000 ) ) ;
#68356=PRESENTATION_STYLE_ASSIGNMENT (( #9273 ) ) ;
#68359=PLANE ( 'NONE',  #29468 ) ;
#68360=TOROIDAL_SURFACE ( 'NONE', #45880, 1.499999999999998668, 1.000000000000000000 ) ;
#68365=FACE_OUTER_BOUND ( 'NONE', #32564, .T. ) ;
#68366=ORIENTED_EDGE ( 'NONE', *, *, #33071, .F. ) ;
#68374=CARTESIAN_POINT ( 'NONE',  ( 29.00000000000000355, 42.58578643762690774, -80.00402776293826435 ) ) ;
#68378=CIRCLE ( 'NONE', #64988, 1.000000000000000888 ) ;
#68382=STYLED_ITEM ( 'NONE', ( #32427 ), #41887 ) ;
#68383=EDGE_CURVE ( 'NONE', #29587, #60780, #10491, .T. ) ;
#68385=FILL_AREA_STYLE ('',( #29708 ) ) ;
#68390=AXIS2_PLACEMENT_3D ( 'NONE', #51220, #30417, #36090 ) ;
#68394=FACE_OUTER_BOUND ( 'NONE', #19714, .T. ) ;
#68403=VECTOR ( 'NONE', #21999, 1000.000000000000000 ) ;
#68404=DIRECTION ( 'NONE',  ( 0.000000000000000000, -1.000000000000000000, 0.000000000000000000 ) ) ;
#68406=SURFACE_STYLE_USAGE ( .BOTH. , #30390 ) ;
#68410=TOROIDAL_SURFACE ( 'NONE', #7737, 3.499999999999998668, 1.000000000000000000 ) ;
#68415=DIRECTION ( 'NONE',  ( 0.000000000000000000, 1.000000000000000000, -0.000000000000000000 ) ) ;
#68416=EDGE_CURVE ( 'NONE', #47418, #4847, #6928, .T. ) ;
#68438=CIRCLE ( 'NONE', #2114, 1.000000000000000888 ) ;
#68444=LINE ( 'NONE', #25515, #69516 ) ;
#68456=EDGE_LOOP ( 'NONE', ( #51874, #47204, #32829 ) ) ;
#68457=COLOUR_RGB ( '', 0.72549020, 0.75294118, 0.79215686) ;
#68464=EDGE_CURVE ( 'NONE', #6587, #36170, #29049, .T. ) ;
#68472=UNCERTAINTY_MEASURE_WITH_UNIT (LENGTH_MEASURE( 1.000000000000000082E-05 ), #20347, 'distance_accuracy_value', 'NONE');
#68485=( GEOMETRIC_REPRESENTATION_CONTEXT ( 3 ) GLOBAL_UNCERTAINTY_ASSIGNED_CONTEXT ( ( #47557 ) ) GLOBAL_UNIT_ASSIGNED_CONTEXT ( ( #60289, #33219, #43804 ) ) REPRESENTATION_CONTEXT ( 'NONE', 'WORKASPACE' ) );
#68488=LINE ( 'NONE', #36522, #34949 ) ;
#68489=( GEOMETRIC_REPRESENTATION_CONTEXT ( 3 ) GLOBAL_UNCERTAINTY_ASSIGNED_CONTEXT ( ( #21537 ) ) GLOBAL_UNIT_ASSIGNED_CONTEXT ( ( #31389, #37080, #69399 ) ) REPRESENTATION_CONTEXT ( 'NONE', 'WORKASPACE' ) );
#68493=FACE_OUTER_BOUND ( 'NONE', #36519, .T. ) ;
#68528=DIRECTION ( 'NONE',  ( 0.000000000000000000, -1.000000000000000000, 0.000000000000000000 ) ) ;
#68541=COLOUR_RGB ( '', 0.66274510, 0.83137255, 0.94901961) ;
#68543=VECTOR ( 'NONE', #14072, 1000.000000000000000 ) ;
#68551=ADVANCED_FACE ( 'NONE', ( #44616 ), #68410, .F. ) ;
#68557=STYLED_ITEM ( 'NONE', ( #38387 ), #17664 ) ;
#68572=EDGE_LOOP ( 'NONE', ( #51790, #45490, #65673, #16899, #59941, #7826 ) ) ;
#68577=UNCERTAINTY_MEASURE_WITH_UNIT (LENGTH_MEASURE( 1.000000000000000082E-05 ), #15638, 'distance_accuracy_value', 'NONE');
#68592=CIRCLE ( 'NONE', #52888, 12.50000000000001066 ) ;
#68594=VERTEX_POINT ( 'NONE', #26881 ) ;
#68595=DIRECTION ( 'NONE',  ( -1.000000000000000000, 0.000000000000000000, 0.000000000000000000 ) ) ;
#68600=ORIENTED_EDGE ( 'NONE', *, *, #22984, .F. ) ;
#68607=ORIENTED_EDGE ( 'NONE', *, *, #48879, .T. ) ;
#68616=UNCERTAINTY_MEASURE_WITH_UNIT (LENGTH_MEASURE( 1.000000000000000082E-05 ), #51543, 'distance_accuracy_value', 'NONE');
#68644=CARTESIAN_POINT ( 'NONE',  ( 10.00000000000001954, 42.00000000000000000, -28.38386403503541899 ) ) ;
#68646=UNCERTAINTY_MEASURE_WITH_UNIT (LENGTH_MEASURE( 1.000000000000000082E-05 ), #67084, 'distance_accuracy_value', 'NONE');
#68650=EDGE_CURVE ( 'NONE', #23421, #49208, #16842, .T. ) ;
#68656=FILL_AREA_STYLE_COLOUR ( '', #45970 ) ;
#68659=ORIENTED_EDGE ( 'NONE', *, *, #36100, .F. ) ;
#68676=LINE ( 'NONE', #20107, #14052 ) ;
#68678=CARTESIAN_POINT ( 'NONE',  ( 0.3542414993972742288, 42.77450856510288446, -74.52798351431924573 ) ) ;
#68681=( GEOMETRIC_REPRESENTATION_CONTEXT ( 3 ) GLOBAL_UNCERTAINTY_ASSIGNED_CONTEXT ( ( #22010 ) ) GLOBAL_UNIT_ASSIGNED_CONTEXT ( ( #38946, #66320, #49470 ) ) REPRESENTATION_CONTEXT ( 'NONE', 'WORKASPACE' ) );
#68689=UNCERTAINTY_MEASURE_WITH_UNIT (LENGTH_MEASURE( 1.000000000000000082E-05 ), #14834, 'distance_accuracy_value', 'NONE');
#68690=CARTESIAN_POINT ( 'NONE',  ( 98.00000000000000000, 16.00000000000000000, -5.000000000000004441 ) ) ;
#68708=VERTEX_POINT ( 'NONE', #63849 ) ;
#68715=DIRECTION ( 'NONE',  ( 1.000000000000000000, 0.000000000000000000, -0.000000000000000000 ) ) ;
#68716=CIRCLE ( 'NONE', #19257, 1.000000000000000888 ) ;
#68717=SURFACE_SIDE_STYLE ('',( #37789 ) ) ;
#68722=AXIS2_PLACEMENT_3D ( 'NONE', #60450, #34079, #18610 ) ;
#68739=ORIENTED_EDGE ( 'NONE', *, *, #67909, .T. ) ;
#68746=AXIS2_PLACEMENT_3D ( 'NONE', #4164, #25636, #21405 ) ;
#68748=DIRECTION ( 'NONE',  ( -7.816271194327172234E-17, 0.000000000000000000, -1.000000000000000000 ) ) ;
#68761=FILL_AREA_STYLE ('',( #21588 ) ) ;
#68763=CARTESIAN_POINT ( 'NONE',  ( 22.00000000000000711, 50.00000000000000000, -59.99999999999999289 ) ) ;
#68773=CARTESIAN_POINT ( 'NONE',  ( 31.00000000000001421, 42.00000000000000000, 35.50000000000000000 ) ) ;
#68784=( GEOMETRIC_REPRESENTATION_CONTEXT ( 3 ) GLOBAL_UNCERTAINTY_ASSIGNED_CONTEXT ( ( #30446 ) ) GLOBAL_UNIT_ASSIGNED_CONTEXT ( ( #6040, #16628, #55257 ) ) REPRESENTATION_CONTEXT ( 'NONE', 'WORKASPACE' ) );
#68791=DIRECTION ( 'NONE',  ( -1.665334536937733825E-15, 0.000000000000000000, -1.000000000000000000 ) ) ;
#68794=SURFACE_STYLE_USAGE ( .BOTH. , #42435 ) ;
#68801=CARTESIAN_POINT ( 'NONE',  ( 22.00000000000002132, 43.00000000000000000, 75.00000000000000000 ) ) ;
#68808=EDGE_CURVE ( 'NONE', #27703, #57733, #11427, .T. ) ;
#68821=CARTESIAN_POINT ( 'NONE',  ( 27.00000000000001776, 14.00000000000000000, -60.00402776293827145 ) ) ;
#68834=PRESENTATION_STYLE_ASSIGNMENT (( #3356 ) ) ;
#68839=CARTESIAN_POINT ( 'NONE',  ( 179.4361977533490347, 13.00000000000000178, 103.7004518695263044 ) ) ;
#68842=ORIENTED_EDGE ( 'NONE', *, *, #1693, .T. ) ;
#68852=FILL_AREA_STYLE ('',( #15403 ) ) ;
#68860=CARTESIAN_POINT ( 'NONE',  ( 32.00000000000000711, 15.00000000000000000, -36.50000000000000000 ) ) ;
#68871=CARTESIAN_POINT ( 'NONE',  ( 0.000000000000000000, 42.00000000000000000, 79.00402776293826435 ) ) ;
#68891=EDGE_CURVE ( 'NONE', #49984, #56901, #52217, .T. ) ;
#68916=LINE ( 'NONE', #42228, #63045 ) ;
#68924=ORIENTED_EDGE ( 'NONE', *, *, #44143, .F. ) ;
#68926=ORIENTED_EDGE ( 'NONE', *, *, #48692, .F. ) ;
#68927=COLOUR_RGB ( '', 0.08235294, 0.09019608, 0.10196078) ;
#68929=CARTESIAN_POINT ( 'NONE',  ( 31.00000000000002132, 15.00000000000000000, 80.00402776293826435 ) ) ;
#68930=COLOUR_RGB ( '', 0.08235294, 0.09019608, 0.10196078) ;
#68931=DIRECTION ( 'NONE',  ( -1.239088197126290817E-16, 0.000000000000000000, -1.000000000000000000 ) ) ;
#68934=ORIENTED_EDGE ( 'NONE', *, *, #26963, .F. ) ;
#68938=ORIENTED_EDGE ( 'NONE', *, *, #29440, .T. ) ;
#68939=ORIENTED_EDGE ( 'NONE', *, *, #69425, .T. ) ;
#68940=EDGE_CURVE ( 'NONE', #62763, #30128, #57199, .T. ) ;
#68942=CARTESIAN_POINT ( 'NONE',  ( 179.4361977533518484, 5.000000000000000000, 103.7004518695275550 ) ) ;
#68954=DIRECTION ( 'NONE',  ( 0.000000000000000000, 0.000000000000000000, 1.000000000000000000 ) ) ;
#68971=AXIS2_PLACEMENT_3D ( 'NONE', #15391, #58609, #27260 ) ;
#68978=CARTESIAN_POINT ( 'NONE',  ( 22.29424117603575084, 26.17668566172280009, 27.49998957561865964 ) ) ;
#68979=EDGE_CURVE ( 'NONE', #63620, #67437, #10365, .T. ) ;
#68991=CARTESIAN_POINT ( 'NONE',  ( 33.00000000000001421, 14.00000000000000000, 36.49999999999999289 ) ) ;
#69009=COLOUR_RGB ( '', 0.31764706, 0.68627451, 0.89019608) ;
#69025=CYLINDRICAL_SURFACE ( 'NONE', #61873, 1.000000000000000000 ) ;
#69039=MECHANICAL_DESIGN_GEOMETRIC_PRESENTATION_REPRESENTATION('',(#9492),#56682);
#69042=ADVANCED_FACE ( 'NONE', ( #64737 ), #11956, .F. ) ;
#69065=FILL_AREA_STYLE ('',( #15610 ) ) ;
#69073=SURFACE_STYLE_USAGE ( .BOTH. , #66096 ) ;
#69074=FILL_AREA_STYLE_COLOUR ( '', #33541 ) ;
#69075=( GEOMETRIC_REPRESENTATION_CONTEXT ( 3 ) GLOBAL_UNCERTAINTY_ASSIGNED_CONTEXT ( ( #25619 ) ) GLOBAL_UNIT_ASSIGNED_CONTEXT ( ( #36213, #58942, #30528 ) ) REPRESENTATION_CONTEXT ( 'NONE', 'WORKASPACE' ) );
#69084=ORIENTED_EDGE ( 'NONE', *, *, #21472, .F. ) ;
#69086=( LENGTH_UNIT ( ) NAMED_UNIT ( * ) SI_UNIT ( .MILLI., .METRE. ) );
#69087=AXIS2_PLACEMENT_3D ( 'NONE', #66223, #28213, #60265 ) ;
#69091=CARTESIAN_POINT ( 'NONE',  ( 10.00000000000000533, 43.00000000000000000, -45.61250543006183733 ) ) ;
#69095=CIRCLE ( 'NONE', #57850, 0.9999999999999986677 ) ;
#69097=SURFACE_STYLE_USAGE ( .BOTH. , #42746 ) ;
#69105=ORIENTED_EDGE ( 'NONE', *, *, #47959, .T. ) ;
#69108=FACE_OUTER_BOUND ( 'NONE', #66227, .T. ) ;
#69112=VERTEX_POINT ( 'NONE', #20527 ) ;
#69117=DIRECTION ( 'NONE',  ( 0.000000000000000000, -1.000000000000000000, 0.000000000000000000 ) ) ;
#69118=DIRECTION ( 'NONE',  ( -0.7681514953298218540, 0.000000000000000000, 0.6402681315062924705 ) ) ;
#69122=AXIS2_PLACEMENT_3D ( 'NONE', #51978, #56180, #67438 ) ;
#69123=ORIENTED_EDGE ( 'NONE', *, *, #55798, .F. ) ;
#69148=CARTESIAN_POINT ( 'NONE',  ( 31.00000000000001421, 42.00000000000000000, 36.50000000000000000 ) ) ;
#69150=CARTESIAN_POINT ( 'NONE',  ( 2.999999999999997335, 5.000000000000000000, 72.00402776293822171 ) ) ;
#69162=UNCERTAINTY_MEASURE_WITH_UNIT (LENGTH_MEASURE( 1.000000000000000082E-05 ), #47899, 'distance_accuracy_value', 'NONE');
#69164=( NAMED_UNIT ( * ) PLANE_ANGLE_UNIT ( ) SI_UNIT ( $, .RADIAN. ) );
#69169=MECHANICAL_DESIGN_GEOMETRIC_PRESENTATION_REPRESENTATION('',(#551),#38868);
#69177=CARTESIAN_POINT ( 'NONE',  ( 29.00000000000002842, 34.36176364315826248, 80.00402776293826435 ) ) ;
#69178=ADVANCED_FACE ( 'NONE', ( #29149 ), #14582, .T. ) ;
#69185=CIRCLE ( 'NONE', #11880, 12.50000000000001066 ) ;
#69187=ADVANCED_FACE ( 'NONE', ( #18280 ), #67155, .T. ) ;
#69189=CARTESIAN_POINT ( 'NONE',  ( 22.41861097278089332, 25.30861756478646996, -27.43527847615431625 ) ) ;
#69192=VERTEX_POINT ( 'NONE', #44368 ) ;
#69194=CARTESIAN_POINT ( 'NONE',  ( 29.00000000000000000, 42.00000000000000000, -89.00000000000000000 ) ) ;
#69195=( LENGTH_UNIT ( ) NAMED_UNIT ( * ) SI_UNIT ( .MILLI., .METRE. ) );
#69221=DIRECTION ( 'NONE',  ( 1.000000000000000000, -0.000000000000000000, -0.000000000000000000 ) ) ;
#69244=DIRECTION ( 'NONE',  ( 0.000000000000000000, -0.000000000000000000, -1.000000000000000000 ) ) ;
#69251=LINE ( 'NONE', #30902, #12838 ) ;
#69256=ORIENTED_EDGE ( 'NONE', *, *, #65764, .T. ) ;
#69261=ADVANCED_FACE ( 'NONE', ( #19296 ), #9820, .F. ) ;
#69262=DIRECTION ( 'NONE',  ( 2.168404344971007882E-16, 0.000000000000000000, 1.000000000000000000 ) ) ;
#69285=DIRECTION ( 'NONE',  ( 0.000000000000000000, 0.000000000000000000, 1.000000000000000000 ) ) ;
#69297=UNCERTAINTY_MEASURE_WITH_UNIT (LENGTH_MEASURE( 1.000000000000000082E-05 ), #28097, 'distance_accuracy_value', 'NONE');
#69299=PRESENTATION_STYLE_ASSIGNMENT (( #34162 ) ) ;
#69309=UNCERTAINTY_MEASURE_WITH_UNIT (LENGTH_MEASURE( 1.000000000000000082E-05 ), #59714, 'distance_accuracy_value', 'NONE');
#69316=CARTESIAN_POINT ( 'NONE',  ( 23.49527607712185073, 27.44009427658185984, 27.19000446309344809 ) ) ;
#69321=FILL_AREA_STYLE ('',( #63682 ) ) ;
#69322=DIRECTION ( 'NONE',  ( 0.000000000000000000, 0.000000000000000000, -1.000000000000000000 ) ) ;
#69325=VECTOR ( 'NONE', #61046, 1000.000000000000000 ) ;
#69366=FILL_AREA_STYLE ('',( #26433 ) ) ;
#69376=VERTEX_POINT ( 'NONE', #5199 ) ;
#69378=UNCERTAINTY_MEASURE_WITH_UNIT (LENGTH_MEASURE( 1.000000000000000082E-05 ), #7476, 'distance_accuracy_value', 'NONE');
#69379=COLOUR_RGB ( '', 0.31764706, 0.68627451, 0.89019608) ;
#69387=EDGE_LOOP ( 'NONE', ( #47250, #5409, #540, #7072 ) ) ;
#69398=SURFACE_STYLE_USAGE ( .BOTH. , #31054 ) ;
#69399=( NAMED_UNIT ( * ) SI_UNIT ( $, .STERADIAN. ) SOLID_ANGLE_UNIT ( ) );
#69401=FILL_AREA_STYLE ('',( #26475 ) ) ;
#69406=SURFACE_STYLE_FILL_AREA ( #53243 ) ;
#69410=VECTOR ( 'NONE', #29044, 1000.000000000000000 ) ;
#69422=FILL_AREA_STYLE ('',( #57836 ) ) ;
#69425=EDGE_CURVE ( 'NONE', #4771, #15447, #65652, .T. ) ;
#69431=FACE_OUTER_BOUND ( 'NONE', #23610, .T. ) ;
#69433=CARTESIAN_POINT ( 'NONE',  ( 22.99999999999999645, 0.000000000000000000, 24.00402776293825013 ) ) ;
#69436=ORIENTED_EDGE ( 'NONE', *, *, #37926, .T. ) ;
#69446=UNCERTAINTY_MEASURE_WITH_UNIT (LENGTH_MEASURE( 1.000000000000000082E-05 ), #45447, 'distance_accuracy_value', 'NONE');
#69447=CARTESIAN_POINT ( 'NONE',  ( 32.00000000000002132, 42.00000000000000000, 80.00402776293826435 ) ) ;
#69462=ORIENTED_EDGE ( 'NONE', *, *, #2368, .F. ) ;
#69465=( GEOMETRIC_REPRESENTATION_CONTEXT ( 3 ) GLOBAL_UNCERTAINTY_ASSIGNED_CONTEXT ( ( #23460 ) ) GLOBAL_UNIT_ASSIGNED_CONTEXT ( ( #45731, #9458, #47116 ) ) REPRESENTATION_CONTEXT ( 'NONE', 'WORKASPACE' ) );
#69479=PRESENTATION_STYLE_ASSIGNMENT (( #38562 ) ) ;
#69485=EDGE_CURVE ( 'NONE', #66860, #44068, #2657, .T. ) ;
#69500=EDGE_CURVE ( 'NONE', #67044, #49461, #28724, .T. ) ;
#69502=EDGE_CURVE ( 'NONE', #60615, #360, #43387, .T. ) ;
#69504=FACE_OUTER_BOUND ( 'NONE', #63715, .T. ) ;
#69505=STYLED_ITEM ( 'NONE', ( #41841 ), #68252 ) ;
#69507=( NAMED_UNIT ( * ) SI_UNIT ( $, .STERADIAN. ) SOLID_ANGLE_UNIT ( ) );
#69509=( LENGTH_UNIT ( ) NAMED_UNIT ( * ) SI_UNIT ( .MILLI., .METRE. ) );
#69514=EDGE_CURVE ( 'NONE', #1442, #2941, #6780, .T. ) ;
#69516=VECTOR ( 'NONE', #47029, 1000.000000000000000 ) ;
#69517=VERTEX_POINT ( 'NONE', #65680 ) ;
#69520=( NAMED_UNIT ( * ) PLANE_ANGLE_UNIT ( ) SI_UNIT ( $, .RADIAN. ) );
#69524=FILL_AREA_STYLE_COLOUR ( '', #29959 ) ;
#69537=( GEOMETRIC_REPRESENTATION_CONTEXT ( 3 ) GLOBAL_UNCERTAINTY_ASSIGNED_CONTEXT ( ( #46724 ) ) GLOBAL_UNIT_ASSIGNED_CONTEXT ( ( #25445, #42380, #52895 ) ) REPRESENTATION_CONTEXT ( 'NONE', 'WORKASPACE' ) );
#69539=SURFACE_STYLE_FILL_AREA ( #54046 ) ;
#69542=LINE ( 'NONE', #21346, #27873 ) ;
#69546=DIRECTION ( 'NONE',  ( 0.000000000000000000, 0.000000000000000000, -1.000000000000000000 ) ) ;
#69555=LINE ( 'NONE', #867, #16373 ) ;
#69563=DIRECTION ( 'NONE',  ( 0.000000000000000000, 1.000000000000000000, -0.000000000000000000 ) ) ;
#69575=COLOUR_RGB ( '', 0.40784314, 0.44705882, 0.49803922) ;
#69585=STYLED_ITEM ( 'NONE', ( #58532 ), #9331 ) ;
#69590=( NAMED_UNIT ( * ) PLANE_ANGLE_UNIT ( ) SI_UNIT ( $, .RADIAN. ) );
#69592=DIRECTION ( 'NONE',  ( 1.000000000000000000, 0.000000000000000000, -1.300977106640434891E-16 ) ) ;
#69604=CARTESIAN_POINT ( 'NONE',  ( 57.00000000000000000, 0.000000000000000000, 60.00402776293827145 ) ) ;
#69610=SURFACE_SIDE_STYLE ('',( #52433 ) ) ;
#69613=ADVANCED_FACE ( 'NONE', ( #62813 ), #24834, .F. ) ;
#69633=CARTESIAN_POINT ( 'NONE',  ( 6.516641522221523708, 43.00000000000000000, -28.13388297856903719 ) ) ;
#69640=CIRCLE ( 'NONE', #4493, 5.000000000000004441 ) ;
#69652=MECHANICAL_DESIGN_GEOMETRIC_PRESENTATION_REPRESENTATION('',(#28090),#6768);
#69656=ORIENTED_EDGE ( 'NONE', *, *, #31260, .T. ) ;
#69659=CARTESIAN_POINT ( 'NONE',  ( 31.00000000000000000, 15.00000000000000000, -80.00402776293826435 ) ) ;
#69677=AXIS2_PLACEMENT_3D ( 'NONE', #48182, #69592, #69262 ) ;
#69679=VECTOR ( 'NONE', #8052, 1000.000000000000000 ) ;
#69686=AXIS2_PLACEMENT_3D ( 'NONE', #30463, #31512, #25890 ) ;
#69690=DIRECTION ( 'NONE',  ( 0.000000000000000000, 1.000000000000000000, 0.000000000000000000 ) ) ;
ENDSEC;
END-ISO-10303-21;
